ISO-10303-21;
HEADER;
/* Generated by software containing ST-Developer
 * from STEP Tools, Inc. (www.steptools.com) 
 */

FILE_DESCRIPTION(
/* description */ (''),
/* implementation_level */ '2;1');

FILE_NAME(
/* name */ '17_Bed_Clamping_Bolt_ISO_4017_M16x40.step',
/* time_stamp */ '2026-10-26T03:50:32-07:00',
/* author */ (''),
/* organization */ (''),
/* preprocessor_version */ 'ST-DEVELOPER v20.2',
/* originating_system */ 'Autodesk Translation Framework v15.15.0.0',
/* authorisation */ '');

FILE_SCHEMA (('AUTOMOTIVE_DESIGN { 1 0 10303 214 3 1 1 }'));
ENDSEC;

DATA;
#10=MECHANICAL_DESIGN_GEOMETRIC_PRESENTATION_REPRESENTATION('',(#1053),#76660);
#123=(
BOUNDED_CURVE()
B_SPLINE_CURVE(2,(#63169,#63170,#63171),.UNSPECIFIED.,.F.,.F.)
B_SPLINE_CURVE_WITH_KNOTS((3,3),(0.0830692064483411,1.5163968327409),
 .UNSPECIFIED.)
CURVE()
GEOMETRIC_REPRESENTATION_ITEM()
RATIONAL_B_SPLINE_CURVE((1.01933756729741,1.17702963774851,1.01933756729741))
REPRESENTATION_ITEM('')
);
#124=(
BOUNDED_CURVE()
B_SPLINE_CURVE(2,(#63173,#63174,#63175),.UNSPECIFIED.,.F.,.F.)
B_SPLINE_CURVE_WITH_KNOTS((3,3),(0.0830692064483407,1.5163968327409),
 .UNSPECIFIED.)
CURVE()
GEOMETRIC_REPRESENTATION_ITEM()
RATIONAL_B_SPLINE_CURVE((1.01933756729741,1.17702963774851,1.01933756729741))
REPRESENTATION_ITEM('')
);
#125=(
BOUNDED_CURVE()
B_SPLINE_CURVE(2,(#63177,#63178,#63179),.UNSPECIFIED.,.F.,.F.)
B_SPLINE_CURVE_WITH_KNOTS((3,3),(0.0830692064483414,1.5163968327409),
 .UNSPECIFIED.)
CURVE()
GEOMETRIC_REPRESENTATION_ITEM()
RATIONAL_B_SPLINE_CURVE((1.01933756729741,1.17702963774851,1.01933756729741))
REPRESENTATION_ITEM('')
);
#126=(
BOUNDED_CURVE()
B_SPLINE_CURVE(2,(#63181,#63182,#63183),.UNSPECIFIED.,.F.,.F.)
B_SPLINE_CURVE_WITH_KNOTS((3,3),(0.0830692064483412,1.5163968327409),
 .UNSPECIFIED.)
CURVE()
GEOMETRIC_REPRESENTATION_ITEM()
RATIONAL_B_SPLINE_CURVE((1.01933756729741,1.17702963774851,1.01933756729741))
REPRESENTATION_ITEM('')
);
#127=(
BOUNDED_CURVE()
B_SPLINE_CURVE(2,(#63185,#63186,#63187),.UNSPECIFIED.,.F.,.F.)
B_SPLINE_CURVE_WITH_KNOTS((3,3),(0.799733019594622,1.5163968327409),
 .UNSPECIFIED.)
CURVE()
GEOMETRIC_REPRESENTATION_ITEM()
RATIONAL_B_SPLINE_CURVE((1.09818360252296,1.09818360252296,1.01933756729741))
REPRESENTATION_ITEM('')
);
#128=(
BOUNDED_CURVE()
B_SPLINE_CURVE(2,(#63192,#63193,#63194),.UNSPECIFIED.,.F.,.F.)
B_SPLINE_CURVE_WITH_KNOTS((3,3),(0.083069206448341,0.799733019594622),
 .UNSPECIFIED.)
CURVE()
GEOMETRIC_REPRESENTATION_ITEM()
RATIONAL_B_SPLINE_CURVE((1.01933756729741,1.09818360252296,1.09818360252296))
REPRESENTATION_ITEM('')
);
#129=(
BOUNDED_CURVE()
B_SPLINE_CURVE(2,(#63195,#63196,#63197),.UNSPECIFIED.,.F.,.F.)
B_SPLINE_CURVE_WITH_KNOTS((3,3),(0.0830692064483408,1.5163968327409),
 .UNSPECIFIED.)
CURVE()
GEOMETRIC_REPRESENTATION_ITEM()
RATIONAL_B_SPLINE_CURVE((1.01933756729741,1.17702963774851,1.01933756729741))
REPRESENTATION_ITEM('')
);
#166=B_SPLINE_SURFACE_WITH_KNOTS('',3,3,((#60732,#60733,#60734,#60735,#60736,
#60737,#60738,#60739,#60740,#60741,#60742,#60743,#60744,#60745,#60746,#60747,
#60748,#60749,#60750,#60751,#60752,#60753,#60754,#60755,#60756,#60757,#60758,
#60759,#60760,#60761,#60762,#60763,#60764,#60765,#60766,#60767,#60768,#60769,
#60770,#60771,#60772,#60773,#60774,#60775,#60776,#60777,#60778,#60779,#60780,
#60781,#60782,#60783,#60784,#60785,#60786,#60787,#60788,#60789,#60790,#60791,
#60792,#60793,#60794,#60795,#60796,#60797,#60798,#60799,#60800,#60801,#60802,
#60803,#60804,#60805,#60806,#60807,#60808,#60809,#60810,#60811,#60812,#60813,
#60814,#60815,#60816,#60817,#60818,#60819,#60820,#60821,#60822,#60823,#60824,
#60825,#60826,#60827,#60828,#60829,#60830,#60831,#60832,#60833,#60834,#60835,
#60836,#60837,#60838,#60839,#60840,#60841,#60842,#60843,#60844,#60845,#60846,
#60847,#60848,#60849,#60850,#60851,#60852,#60853,#60854,#60855,#60856,#60857,
#60858,#60859,#60860,#60861,#60862,#60863,#60864,#60865,#60866,#60867,#60868,
#60869,#60870,#60871,#60872,#60873,#60874,#60875,#60876,#60877,#60878,#60879,
#60880,#60881,#60882,#60883,#60884,#60885,#60886,#60887,#60888,#60889,#60890,
#60891,#60892,#60893,#60894,#60895,#60896,#60897,#60898,#60899,#60900,#60901,
#60902,#60903,#60904,#60905,#60906,#60907,#60908,#60909,#60910,#60911,#60912,
#60913,#60914,#60915,#60916,#60917,#60918,#60919,#60920,#60921,#60922,#60923,
#60924,#60925,#60926,#60927,#60928,#60929,#60930,#60931,#60932,#60933,#60934,
#60935,#60936,#60937,#60938,#60939,#60940,#60941,#60942,#60943,#60944,#60945,
#60946,#60947,#60948,#60949,#60950,#60951,#60952,#60953,#60954,#60955,#60956,
#60957,#60958,#60959,#60960,#60961,#60962,#60963,#60964,#60965,#60966,#60967,
#60968,#60969,#60970,#60971,#60972,#60973,#60974,#60975,#60976,#60977,#60978,
#60979,#60980,#60981,#60982,#60983,#60984,#60985,#60986,#60987,#60988),
(#60989,#60990,#60991,#60992,#60993,#60994,#60995,#60996,#60997,#60998,
#60999,#61000,#61001,#61002,#61003,#61004,#61005,#61006,#61007,#61008,#61009,
#61010,#61011,#61012,#61013,#61014,#61015,#61016,#61017,#61018,#61019,#61020,
#61021,#61022,#61023,#61024,#61025,#61026,#61027,#61028,#61029,#61030,#61031,
#61032,#61033,#61034,#61035,#61036,#61037,#61038,#61039,#61040,#61041,#61042,
#61043,#61044,#61045,#61046,#61047,#61048,#61049,#61050,#61051,#61052,#61053,
#61054,#61055,#61056,#61057,#61058,#61059,#61060,#61061,#61062,#61063,#61064,
#61065,#61066,#61067,#61068,#61069,#61070,#61071,#61072,#61073,#61074,#61075,
#61076,#61077,#61078,#61079,#61080,#61081,#61082,#61083,#61084,#61085,#61086,
#61087,#61088,#61089,#61090,#61091,#61092,#61093,#61094,#61095,#61096,#61097,
#61098,#61099,#61100,#61101,#61102,#61103,#61104,#61105,#61106,#61107,#61108,
#61109,#61110,#61111,#61112,#61113,#61114,#61115,#61116,#61117,#61118,#61119,
#61120,#61121,#61122,#61123,#61124,#61125,#61126,#61127,#61128,#61129,#61130,
#61131,#61132,#61133,#61134,#61135,#61136,#61137,#61138,#61139,#61140,#61141,
#61142,#61143,#61144,#61145,#61146,#61147,#61148,#61149,#61150,#61151,#61152,
#61153,#61154,#61155,#61156,#61157,#61158,#61159,#61160,#61161,#61162,#61163,
#61164,#61165,#61166,#61167,#61168,#61169,#61170,#61171,#61172,#61173,#61174,
#61175,#61176,#61177,#61178,#61179,#61180,#61181,#61182,#61183,#61184,#61185,
#61186,#61187,#61188,#61189,#61190,#61191,#61192,#61193,#61194,#61195,#61196,
#61197,#61198,#61199,#61200,#61201,#61202,#61203,#61204,#61205,#61206,#61207,
#61208,#61209,#61210,#61211,#61212,#61213,#61214,#61215,#61216,#61217,#61218,
#61219,#61220,#61221,#61222,#61223,#61224,#61225,#61226,#61227,#61228,#61229,
#61230,#61231,#61232,#61233,#61234,#61235,#61236,#61237,#61238,#61239,#61240,
#61241,#61242,#61243,#61244,#61245),(#61246,#61247,#61248,#61249,#61250,
#61251,#61252,#61253,#61254,#61255,#61256,#61257,#61258,#61259,#61260,#61261,
#61262,#61263,#61264,#61265,#61266,#61267,#61268,#61269,#61270,#61271,#61272,
#61273,#61274,#61275,#61276,#61277,#61278,#61279,#61280,#61281,#61282,#61283,
#61284,#61285,#61286,#61287,#61288,#61289,#61290,#61291,#61292,#61293,#61294,
#61295,#61296,#61297,#61298,#61299,#61300,#61301,#61302,#61303,#61304,#61305,
#61306,#61307,#61308,#61309,#61310,#61311,#61312,#61313,#61314,#61315,#61316,
#61317,#61318,#61319,#61320,#61321,#61322,#61323,#61324,#61325,#61326,#61327,
#61328,#61329,#61330,#61331,#61332,#61333,#61334,#61335,#61336,#61337,#61338,
#61339,#61340,#61341,#61342,#61343,#61344,#61345,#61346,#61347,#61348,#61349,
#61350,#61351,#61352,#61353,#61354,#61355,#61356,#61357,#61358,#61359,#61360,
#61361,#61362,#61363,#61364,#61365,#61366,#61367,#61368,#61369,#61370,#61371,
#61372,#61373,#61374,#61375,#61376,#61377,#61378,#61379,#61380,#61381,#61382,
#61383,#61384,#61385,#61386,#61387,#61388,#61389,#61390,#61391,#61392,#61393,
#61394,#61395,#61396,#61397,#61398,#61399,#61400,#61401,#61402,#61403,#61404,
#61405,#61406,#61407,#61408,#61409,#61410,#61411,#61412,#61413,#61414,#61415,
#61416,#61417,#61418,#61419,#61420,#61421,#61422,#61423,#61424,#61425,#61426,
#61427,#61428,#61429,#61430,#61431,#61432,#61433,#61434,#61435,#61436,#61437,
#61438,#61439,#61440,#61441,#61442,#61443,#61444,#61445,#61446,#61447,#61448,
#61449,#61450,#61451,#61452,#61453,#61454,#61455,#61456,#61457,#61458,#61459,
#61460,#61461,#61462,#61463,#61464,#61465,#61466,#61467,#61468,#61469,#61470,
#61471,#61472,#61473,#61474,#61475,#61476,#61477,#61478,#61479,#61480,#61481,
#61482,#61483,#61484,#61485,#61486,#61487,#61488,#61489,#61490,#61491,#61492,
#61493,#61494,#61495,#61496,#61497,#61498,#61499,#61500,#61501,#61502),
(#61503,#61504,#61505,#61506,#61507,#61508,#61509,#61510,#61511,#61512,
#61513,#61514,#61515,#61516,#61517,#61518,#61519,#61520,#61521,#61522,#61523,
#61524,#61525,#61526,#61527,#61528,#61529,#61530,#61531,#61532,#61533,#61534,
#61535,#61536,#61537,#61538,#61539,#61540,#61541,#61542,#61543,#61544,#61545,
#61546,#61547,#61548,#61549,#61550,#61551,#61552,#61553,#61554,#61555,#61556,
#61557,#61558,#61559,#61560,#61561,#61562,#61563,#61564,#61565,#61566,#61567,
#61568,#61569,#61570,#61571,#61572,#61573,#61574,#61575,#61576,#61577,#61578,
#61579,#61580,#61581,#61582,#61583,#61584,#61585,#61586,#61587,#61588,#61589,
#61590,#61591,#61592,#61593,#61594,#61595,#61596,#61597,#61598,#61599,#61600,
#61601,#61602,#61603,#61604,#61605,#61606,#61607,#61608,#61609,#61610,#61611,
#61612,#61613,#61614,#61615,#61616,#61617,#61618,#61619,#61620,#61621,#61622,
#61623,#61624,#61625,#61626,#61627,#61628,#61629,#61630,#61631,#61632,#61633,
#61634,#61635,#61636,#61637,#61638,#61639,#61640,#61641,#61642,#61643,#61644,
#61645,#61646,#61647,#61648,#61649,#61650,#61651,#61652,#61653,#61654,#61655,
#61656,#61657,#61658,#61659,#61660,#61661,#61662,#61663,#61664,#61665,#61666,
#61667,#61668,#61669,#61670,#61671,#61672,#61673,#61674,#61675,#61676,#61677,
#61678,#61679,#61680,#61681,#61682,#61683,#61684,#61685,#61686,#61687,#61688,
#61689,#61690,#61691,#61692,#61693,#61694,#61695,#61696,#61697,#61698,#61699,
#61700,#61701,#61702,#61703,#61704,#61705,#61706,#61707,#61708,#61709,#61710,
#61711,#61712,#61713,#61714,#61715,#61716,#61717,#61718,#61719,#61720,#61721,
#61722,#61723,#61724,#61725,#61726,#61727,#61728,#61729,#61730,#61731,#61732,
#61733,#61734,#61735,#61736,#61737,#61738,#61739,#61740,#61741,#61742,#61743,
#61744,#61745,#61746,#61747,#61748,#61749,#61750,#61751,#61752,#61753,#61754,
#61755,#61756,#61757,#61758,#61759)),.UNSPECIFIED.,.F.,.F.,.F.,(4,4),(4,
1,1,1,1,1,1,1,1,1,1,1,1,1,1,1,1,1,1,1,1,1,1,1,1,1,1,1,1,1,1,1,1,1,1,1,1,
1,1,1,1,1,1,1,1,1,1,1,1,1,1,1,1,1,1,1,1,1,1,1,1,1,1,1,1,1,1,1,1,1,1,1,1,
1,1,1,1,1,1,1,1,1,1,1,1,1,1,1,1,1,1,1,1,1,1,1,1,1,1,1,1,1,1,1,1,1,1,1,1,
1,1,1,1,1,1,1,1,1,1,1,1,1,1,1,1,1,1,1,1,1,1,1,1,1,1,1,1,1,1,1,1,1,1,1,1,
1,1,1,1,1,1,1,1,1,1,1,1,1,1,1,1,1,1,1,1,1,1,1,1,1,1,1,1,1,1,1,1,1,1,1,1,
1,1,1,1,1,1,1,1,1,1,1,1,1,1,1,1,1,1,1,1,1,1,1,1,1,1,1,1,1,1,1,1,1,1,1,1,
1,1,1,1,1,1,1,1,1,1,1,1,1,1,1,1,1,1,1,1,1,1,1,1,1,1,1,1,1,1,1,1,1,1,1,1,
1,4),(0.,0.132097741590587),(8.30112925462614,8.79771720254068,9.29430515045521,
9.79089309836974,10.2874810462843,10.7840689941988,11.2806569421133,11.7772448900279,
12.2738328379424,12.7704207858569,13.2670087337715,13.763596681686,14.2601846296005,
14.7567725775151,15.2533605254296,15.7499484733441,16.2465364212587,16.7431243691732,
17.2397123170877,17.7363002650023,18.2328882129168,18.7294761608313,19.2260641087459,
19.7226520566604,20.2192400045749,20.7158279524895,21.212415900404,21.7090038483185,
22.2055917962331,22.7021797441476,23.1987676920621,23.6953556399767,24.1919435878912,
24.6885315358057,25.1851194837203,25.6817074316348,26.1782953795493,26.6748833274639,
27.1714712753784,27.6680592232929,28.1646471712075,28.661235119122,29.1578230670365,
29.6544110149511,30.1509989628656,30.6475869107801,31.1441748586947,31.6407628066092,
32.1373507545237,32.6339387024382,33.1305266503528,33.6271145982673,34.1237025461818,
34.6202904940964,35.1168784420109,35.6134663899254,36.11005433784,36.6066422857545,
37.103230233669,37.5998181815836,38.0964061294981,38.5929940774126,39.0895820253272,
39.5861699732417,40.0827579211562,40.5793458690708,41.0759338169853,41.5725217648998,
42.0691097128144,42.5656976607289,43.0622856086434,43.558873556558,44.0554615044725,
44.552049452387,45.0486374003016,45.5452253482161,46.0418132961306,46.5384012440452,
47.0349891919597,47.5315771398742,48.0281650877888,48.5247530357033,49.0213409836178,
49.5179289315324,50.0145168794469,50.5111048273614,51.007692775276,51.5042807231905,
52.000868671105,52.4974566190196,52.9940445669341,53.4906325148486,53.9872204627632,
54.4838084106777,54.9803963585922,55.4769843065068,55.9735722544213,56.4701602023358,
56.9667481502504,57.4633360981649,57.9599240460794,58.456511993994,58.9530999419085,
59.449687889823,59.9462758377375,60.4428637856521,60.9394517335666,61.4360396814811,
61.9326276293957,62.4292155773102,62.9258035252248,63.4223914731393,63.9189794210538,
64.4155673689683,64.9121553168829,65.4087432647974,65.9053312127119,66.4019191606265,
66.898507108541,67.3950950564555,67.8916830043701,68.3882709522846,68.8848589001991,
69.3814468481137,69.8780347960282,70.3746227439427,70.8712106918573,71.3677986397718,
71.8643865876863,72.3609745356009,72.8575624835154,73.3541504314299,73.8507383793445,
74.347326327259,74.8439142751735,75.3405022230881,75.8370901710026,76.3336781189171,
76.8302660668317,77.3268540147462,77.8234419626607,78.3200299105753,78.8166178584898,
79.3132058064043,79.8097937543189,80.3063817022334,80.8029696501479,81.2995575980625,
81.796145545977,82.2927334938915,82.7893214418061,83.2859093897206,83.7824973376351,
84.2790852855497,84.7756732334642,85.2722611813787,85.7688491292933,86.2654370772078,
86.7620250251223,87.2586129730369,87.7552009209514,88.2517888688659,88.7483768167804,
89.244964764695,89.7415527126095,90.2381406605241,90.7347286084386,91.2313165563531,
91.7279045042677,92.2244924521822,92.7210804000967,93.2176683480112,93.7142562959258,
94.2108442438403,94.7074321917548,95.2040201396694,95.7006080875839,96.1971960354985,
96.693783983413,97.1903719313275,97.686959879242,98.1835478271566,98.6801357750711,
99.1767237229856,99.6733116709002,100.169899618815,100.666487566729,101.163075514644,
101.659663462558,102.156251410473,102.652839358387,103.149427306302,103.646015254216,
104.142603202131,104.639191150046,105.13577909796,105.632367045875,106.128954993789,
106.625542941704,107.122130889618,107.618718837533,108.115306785447,108.611894733362,
109.108482681276,109.605070629191,110.101658577105,110.59824652502,111.094834472934,
111.591422420849,112.088010368763,112.584598316678,113.081186264593,113.577774212507,
114.074362160422,114.570950108336,115.067538056251,115.564126004165,116.06071395208,
116.557301899994,117.053889847909,117.550477795823,118.047065743738,118.543653691652,
119.040241639567,119.536829587481,120.033417535396,120.530005483311,121.026593431225,
121.52318137914,122.019769327054,122.516357274969,123.012945222883,123.509533170798,
124.006121118712,124.502709066627,124.999297014541,125.495884962456,125.99247291037,
126.489060858285,126.985648806199,127.482236754114,127.978824702029,128.475412649943,
128.972000597858,129.468588545772,129.965176493687,130.461764441601,130.958352389516,
131.45494033743,131.951528285345,132.448116233259,132.944704181174,133.441292129088,
133.937880077003,134.434468024917),.UNSPECIFIED.);
#167=B_SPLINE_SURFACE_WITH_KNOTS('',3,3,((#62045,#62046,#62047,#62048,#62049,
#62050,#62051,#62052,#62053,#62054,#62055,#62056,#62057,#62058,#62059,#62060,
#62061,#62062,#62063,#62064,#62065,#62066,#62067,#62068,#62069,#62070,#62071,
#62072,#62073,#62074,#62075,#62076,#62077,#62078,#62079,#62080,#62081,#62082,
#62083,#62084,#62085,#62086,#62087,#62088,#62089,#62090,#62091,#62092,#62093,
#62094,#62095,#62096,#62097,#62098,#62099,#62100,#62101,#62102,#62103,#62104,
#62105,#62106,#62107,#62108,#62109,#62110,#62111,#62112,#62113,#62114,#62115,
#62116,#62117,#62118,#62119,#62120,#62121,#62122,#62123,#62124,#62125,#62126,
#62127,#62128,#62129,#62130,#62131,#62132,#62133,#62134,#62135,#62136,#62137,
#62138,#62139,#62140,#62141,#62142,#62143,#62144,#62145,#62146,#62147,#62148,
#62149,#62150,#62151,#62152,#62153,#62154,#62155,#62156,#62157,#62158,#62159,
#62160,#62161,#62162,#62163,#62164,#62165,#62166,#62167,#62168,#62169,#62170,
#62171,#62172,#62173,#62174,#62175,#62176,#62177,#62178,#62179,#62180,#62181,
#62182,#62183,#62184,#62185,#62186,#62187,#62188,#62189,#62190,#62191,#62192,
#62193,#62194,#62195,#62196,#62197,#62198,#62199,#62200,#62201,#62202,#62203,
#62204,#62205,#62206,#62207,#62208,#62209,#62210,#62211,#62212,#62213,#62214,
#62215,#62216,#62217,#62218,#62219,#62220,#62221,#62222,#62223,#62224,#62225,
#62226,#62227,#62228,#62229,#62230,#62231,#62232,#62233,#62234,#62235,#62236,
#62237,#62238,#62239,#62240,#62241,#62242,#62243,#62244,#62245,#62246,#62247,
#62248,#62249,#62250,#62251,#62252,#62253,#62254,#62255,#62256,#62257,#62258,
#62259,#62260,#62261,#62262,#62263,#62264,#62265,#62266,#62267,#62268,#62269,
#62270,#62271,#62272,#62273,#62274,#62275,#62276,#62277,#62278,#62279,#62280,
#62281,#62282,#62283,#62284,#62285,#62286,#62287,#62288,#62289,#62290,#62291,
#62292,#62293,#62294,#62295,#62296,#62297,#62298,#62299,#62300,#62301),
(#62302,#62303,#62304,#62305,#62306,#62307,#62308,#62309,#62310,#62311,
#62312,#62313,#62314,#62315,#62316,#62317,#62318,#62319,#62320,#62321,#62322,
#62323,#62324,#62325,#62326,#62327,#62328,#62329,#62330,#62331,#62332,#62333,
#62334,#62335,#62336,#62337,#62338,#62339,#62340,#62341,#62342,#62343,#62344,
#62345,#62346,#62347,#62348,#62349,#62350,#62351,#62352,#62353,#62354,#62355,
#62356,#62357,#62358,#62359,#62360,#62361,#62362,#62363,#62364,#62365,#62366,
#62367,#62368,#62369,#62370,#62371,#62372,#62373,#62374,#62375,#62376,#62377,
#62378,#62379,#62380,#62381,#62382,#62383,#62384,#62385,#62386,#62387,#62388,
#62389,#62390,#62391,#62392,#62393,#62394,#62395,#62396,#62397,#62398,#62399,
#62400,#62401,#62402,#62403,#62404,#62405,#62406,#62407,#62408,#62409,#62410,
#62411,#62412,#62413,#62414,#62415,#62416,#62417,#62418,#62419,#62420,#62421,
#62422,#62423,#62424,#62425,#62426,#62427,#62428,#62429,#62430,#62431,#62432,
#62433,#62434,#62435,#62436,#62437,#62438,#62439,#62440,#62441,#62442,#62443,
#62444,#62445,#62446,#62447,#62448,#62449,#62450,#62451,#62452,#62453,#62454,
#62455,#62456,#62457,#62458,#62459,#62460,#62461,#62462,#62463,#62464,#62465,
#62466,#62467,#62468,#62469,#62470,#62471,#62472,#62473,#62474,#62475,#62476,
#62477,#62478,#62479,#62480,#62481,#62482,#62483,#62484,#62485,#62486,#62487,
#62488,#62489,#62490,#62491,#62492,#62493,#62494,#62495,#62496,#62497,#62498,
#62499,#62500,#62501,#62502,#62503,#62504,#62505,#62506,#62507,#62508,#62509,
#62510,#62511,#62512,#62513,#62514,#62515,#62516,#62517,#62518,#62519,#62520,
#62521,#62522,#62523,#62524,#62525,#62526,#62527,#62528,#62529,#62530,#62531,
#62532,#62533,#62534,#62535,#62536,#62537,#62538,#62539,#62540,#62541,#62542,
#62543,#62544,#62545,#62546,#62547,#62548,#62549,#62550,#62551,#62552,#62553,
#62554,#62555,#62556,#62557,#62558),(#62559,#62560,#62561,#62562,#62563,
#62564,#62565,#62566,#62567,#62568,#62569,#62570,#62571,#62572,#62573,#62574,
#62575,#62576,#62577,#62578,#62579,#62580,#62581,#62582,#62583,#62584,#62585,
#62586,#62587,#62588,#62589,#62590,#62591,#62592,#62593,#62594,#62595,#62596,
#62597,#62598,#62599,#62600,#62601,#62602,#62603,#62604,#62605,#62606,#62607,
#62608,#62609,#62610,#62611,#62612,#62613,#62614,#62615,#62616,#62617,#62618,
#62619,#62620,#62621,#62622,#62623,#62624,#62625,#62626,#62627,#62628,#62629,
#62630,#62631,#62632,#62633,#62634,#62635,#62636,#62637,#62638,#62639,#62640,
#62641,#62642,#62643,#62644,#62645,#62646,#62647,#62648,#62649,#62650,#62651,
#62652,#62653,#62654,#62655,#62656,#62657,#62658,#62659,#62660,#62661,#62662,
#62663,#62664,#62665,#62666,#62667,#62668,#62669,#62670,#62671,#62672,#62673,
#62674,#62675,#62676,#62677,#62678,#62679,#62680,#62681,#62682,#62683,#62684,
#62685,#62686,#62687,#62688,#62689,#62690,#62691,#62692,#62693,#62694,#62695,
#62696,#62697,#62698,#62699,#62700,#62701,#62702,#62703,#62704,#62705,#62706,
#62707,#62708,#62709,#62710,#62711,#62712,#62713,#62714,#62715,#62716,#62717,
#62718,#62719,#62720,#62721,#62722,#62723,#62724,#62725,#62726,#62727,#62728,
#62729,#62730,#62731,#62732,#62733,#62734,#62735,#62736,#62737,#62738,#62739,
#62740,#62741,#62742,#62743,#62744,#62745,#62746,#62747,#62748,#62749,#62750,
#62751,#62752,#62753,#62754,#62755,#62756,#62757,#62758,#62759,#62760,#62761,
#62762,#62763,#62764,#62765,#62766,#62767,#62768,#62769,#62770,#62771,#62772,
#62773,#62774,#62775,#62776,#62777,#62778,#62779,#62780,#62781,#62782,#62783,
#62784,#62785,#62786,#62787,#62788,#62789,#62790,#62791,#62792,#62793,#62794,
#62795,#62796,#62797,#62798,#62799,#62800,#62801,#62802,#62803,#62804,#62805,
#62806,#62807,#62808,#62809,#62810,#62811,#62812,#62813,#62814,#62815),
(#62816,#62817,#62818,#62819,#62820,#62821,#62822,#62823,#62824,#62825,
#62826,#62827,#62828,#62829,#62830,#62831,#62832,#62833,#62834,#62835,#62836,
#62837,#62838,#62839,#62840,#62841,#62842,#62843,#62844,#62845,#62846,#62847,
#62848,#62849,#62850,#62851,#62852,#62853,#62854,#62855,#62856,#62857,#62858,
#62859,#62860,#62861,#62862,#62863,#62864,#62865,#62866,#62867,#62868,#62869,
#62870,#62871,#62872,#62873,#62874,#62875,#62876,#62877,#62878,#62879,#62880,
#62881,#62882,#62883,#62884,#62885,#62886,#62887,#62888,#62889,#62890,#62891,
#62892,#62893,#62894,#62895,#62896,#62897,#62898,#62899,#62900,#62901,#62902,
#62903,#62904,#62905,#62906,#62907,#62908,#62909,#62910,#62911,#62912,#62913,
#62914,#62915,#62916,#62917,#62918,#62919,#62920,#62921,#62922,#62923,#62924,
#62925,#62926,#62927,#62928,#62929,#62930,#62931,#62932,#62933,#62934,#62935,
#62936,#62937,#62938,#62939,#62940,#62941,#62942,#62943,#62944,#62945,#62946,
#62947,#62948,#62949,#62950,#62951,#62952,#62953,#62954,#62955,#62956,#62957,
#62958,#62959,#62960,#62961,#62962,#62963,#62964,#62965,#62966,#62967,#62968,
#62969,#62970,#62971,#62972,#62973,#62974,#62975,#62976,#62977,#62978,#62979,
#62980,#62981,#62982,#62983,#62984,#62985,#62986,#62987,#62988,#62989,#62990,
#62991,#62992,#62993,#62994,#62995,#62996,#62997,#62998,#62999,#63000,#63001,
#63002,#63003,#63004,#63005,#63006,#63007,#63008,#63009,#63010,#63011,#63012,
#63013,#63014,#63015,#63016,#63017,#63018,#63019,#63020,#63021,#63022,#63023,
#63024,#63025,#63026,#63027,#63028,#63029,#63030,#63031,#63032,#63033,#63034,
#63035,#63036,#63037,#63038,#63039,#63040,#63041,#63042,#63043,#63044,#63045,
#63046,#63047,#63048,#63049,#63050,#63051,#63052,#63053,#63054,#63055,#63056,
#63057,#63058,#63059,#63060,#63061,#63062,#63063,#63064,#63065,#63066,#63067,
#63068,#63069,#63070,#63071,#63072)),.UNSPECIFIED.,.F.,.F.,.F.,(4,4),(4,
1,1,1,1,1,1,1,1,1,1,1,1,1,1,1,1,1,1,1,1,1,1,1,1,1,1,1,1,1,1,1,1,1,1,1,1,
1,1,1,1,1,1,1,1,1,1,1,1,1,1,1,1,1,1,1,1,1,1,1,1,1,1,1,1,1,1,1,1,1,1,1,1,
1,1,1,1,1,1,1,1,1,1,1,1,1,1,1,1,1,1,1,1,1,1,1,1,1,1,1,1,1,1,1,1,1,1,1,1,
1,1,1,1,1,1,1,1,1,1,1,1,1,1,1,1,1,1,1,1,1,1,1,1,1,1,1,1,1,1,1,1,1,1,1,1,
1,1,1,1,1,1,1,1,1,1,1,1,1,1,1,1,1,1,1,1,1,1,1,1,1,1,1,1,1,1,1,1,1,1,1,1,
1,1,1,1,1,1,1,1,1,1,1,1,1,1,1,1,1,1,1,1,1,1,1,1,1,1,1,1,1,1,1,1,1,1,1,1,
1,1,1,1,1,1,1,1,1,1,1,1,1,1,1,1,1,1,1,1,1,1,1,1,1,1,1,1,1,1,1,1,1,1,1,1,
1,4),(0.,0.132097741590587),(11.6150328478182,12.1116207957327,12.6082087436472,
13.1047966915618,13.6013846394763,14.0979725873908,14.5945605353054,15.0911484832199,
15.5877364311344,16.084324379049,16.5809123269635,17.077500274878,17.5740882227926,
18.0706761707071,18.5672641186216,19.0638520665362,19.5604400144507,20.0570279623652,
20.5536159102798,21.0502038581943,21.5467918061088,22.0433797540234,22.5399677019379,
23.0365556498524,23.533143597767,24.0297315456815,24.526319493596,25.0229074415106,
25.5194953894251,26.0160833373396,26.5126712852542,27.0092592331687,27.5058471810832,
28.0024351289978,28.4990230769123,28.9956110248268,29.4921989727414,29.9887869206559,
30.4853748685704,30.981962816485,31.4785507643995,31.975138712314,32.4717266602286,
32.9683146081431,33.4649025560576,33.9614905039722,34.4580784518867,34.9546663998012,
35.4512543477158,35.9478422956303,36.4444302435448,36.9410181914593,37.4376061393739,
37.9341940872884,38.430782035203,38.9273699831175,39.423957931032,39.9205458789466,
40.4171338268611,40.9137217747756,41.4103097226902,41.9068976706047,42.4034856185192,
42.9000735664337,43.3966615143483,43.8932494622628,44.3898374101773,44.8864253580919,
45.3830133060064,45.8796012539209,46.3761892018355,46.87277714975,47.3693650976645,
47.8659530455791,48.3625409934936,48.8591289414081,49.3557168893227,49.8523048372372,
50.3488927851517,50.8454807330663,51.3420686809808,51.8386566288953,52.3352445768099,
52.8318325247244,53.3284204726389,53.8250084205535,54.321596368468,54.8181843163825,
55.3147722642971,55.8113602122116,56.3079481601261,56.8045361080407,57.3011240559552,
57.7977120038697,58.2942999517843,58.7908878996988,59.2874758476133,59.7840637955279,
60.2806517434424,60.7772396913569,61.2738276392715,61.770415587186,62.2670035351005,
62.7635914830151,63.2601794309296,63.7567673788441,64.2533553267587,64.7499432746732,
65.2465312225877,65.7431191705023,66.2397071184168,66.7362950663313,67.2328830142459,
67.7294709621604,68.2260589100749,68.7226468579895,69.219234805904,69.7158227538185,
70.2124107017331,70.7089986496476,71.2055865975621,71.7021745454767,72.1987624933912,
72.6953504413057,73.1919383892203,73.6885263371348,74.1851142850493,74.6817022329639,
75.1782901808784,75.6748781287929,76.1714660767074,76.668054024622,77.1646419725365,
77.661229920451,78.1578178683656,78.6544058162801,79.1509937641947,79.6475817121092,
80.1441696600237,80.6407576079382,81.1373455558528,81.6339335037673,82.1305214516818,
82.6271093995964,83.1236973475109,83.6202852954254,84.11687324334,84.6134611912545,
85.110049139169,85.6066370870836,86.1032250349981,86.5998129829126,87.0964009308272,
87.5929888787417,88.0895768266562,88.5861647745708,89.0827527224853,89.5793406703998,
90.0759286183144,90.5725165662289,91.0691045141434,91.565692462058,92.0622804099725,
92.558868357887,93.0554563058016,93.5520442537161,94.0486322016306,94.5452201495452,
95.0418080974597,95.5383960453742,96.0349839932888,96.5315719412033,97.0281598891178,
97.5247478370324,98.0213357849469,98.5179237328614,99.014511680776,99.5110996286905,
100.007687576605,100.50427552452,101.000863472434,101.497451420349,101.994039368263,
102.490627316178,102.987215264092,103.483803212007,103.980391159921,104.476979107836,
104.97356705575,105.470155003665,105.966742951579,106.463330899494,106.959918847408,
107.456506795323,107.953094743238,108.449682691152,108.946270639067,109.442858586981,
109.939446534896,110.43603448281,110.932622430725,111.429210378639,111.925798326554,
112.422386274468,112.918974222383,113.415562170297,113.912150118212,114.408738066126,
114.905326014041,115.401913961956,115.89850190987,116.395089857785,116.891677805699,
117.388265753614,117.884853701528,118.381441649443,118.878029597357,119.374617545272,
119.871205493186,120.367793441101,120.864381389015,121.36096933693,121.857557284844,
122.354145232759,122.850733180674,123.347321128588,123.843909076503,124.340497024417,
124.837084972332,125.333672920246,125.830260868161,126.326848816075,126.82343676399,
127.320024711904,127.816612659819,128.313200607733,128.809788555648,129.306376503562,
129.802964451477,130.299552399392,130.796140347306,131.292728295221,131.789316243135,
132.28590419105,132.782492138964,133.279080086879,133.775668034793,134.272255982708,
134.768843930622,135.265431878537,135.762019826451,136.258607774366,136.75519572228,
137.251783670195,137.74837161811),.UNSPECIFIED.);
#629=B_SPLINE_CURVE_WITH_KNOTS('',3,(#58316,#58317,#58318,#58319,#58320,
#58321,#58322,#58323,#58324,#58325,#58326,#58327,#58328,#58329,#58330,#58331),
 .UNSPECIFIED.,.F.,.F.,(4,3,3,3,3,4),(-4.09293042013071,-3.97270358331626,
-3.47611563540173,-2.9795276874872,-2.48293973957266,-2.074986472684),
 .UNSPECIFIED.);
#630=B_SPLINE_CURVE_WITH_KNOTS('',3,(#58334,#58335,#58336,#58337,#58338,
#58339,#58340,#58341,#58342,#58343),.UNSPECIFIED.,.F.,.F.,(4,3,3,4),(0.,
0.496587947914526,0.993175895829066,1.12364870614302),.UNSPECIFIED.);
#631=B_SPLINE_CURVE_WITH_KNOTS('',3,(#58348,#58349,#58350,#58351,#58352,
#58353,#58354,#58355,#58356,#58357,#58358,#58359,#58360,#58361,#58362,#58363,
#58364,#58365,#58366,#58367,#58368,#58369,#58370,#58371,#58372,#58373,#58374,
#58375,#58376,#58377,#58378,#58379,#58380,#58381,#58382,#58383,#58384,#58385,
#58386,#58387),.UNSPECIFIED.,.F.,.F.,(4,3,3,3,3,3,3,3,3,3,3,3,3,4),(-10.3761157273103,
-9.93175895829066,-9.43517101037613,-8.93858306246159,-8.44199511454706,
-7.94540716663253,-7.448819218718,-6.95223127080346,-6.45564332288893,-5.95905537497439,
-5.46246742705986,-4.96587947914533,-4.4692915312308,-4.09293042013071),
 .UNSPECIFIED.);
#632=B_SPLINE_CURVE_WITH_KNOTS('',3,(#58388,#58389,#58390,#58391,#58392,
#58393,#58394,#58395,#58396,#58397,#58398,#58399,#58400,#58401,#58402,#58403,
#58404,#58405,#58406,#58407,#58408,#58409,#58410,#58411,#58412,#58413,#58414,
#58415,#58416,#58417,#58418,#58419,#58420,#58421,#58422,#58423,#58424,#58425,
#58426,#58427),.UNSPECIFIED.,.F.,.F.,(4,3,3,3,3,3,3,3,3,3,3,3,3,4),(1.12364870614302,
1.4897638437436,1.98635179165813,2.48293973957267,2.9795276874872,3.47611563540173,
3.97270358331626,4.4692915312308,4.96587947914533,5.46246742705986,5.95905537497439,
6.45564332288893,6.95223127080346,7.40683401332261),.UNSPECIFIED.);
#633=B_SPLINE_CURVE_WITH_KNOTS('',3,(#58432,#58433,#58434,#58435,#58436,
#58437,#58438,#58439,#58440,#58441,#58442,#58443,#58444,#58445,#58446,#58447,
#58448,#58449,#58450,#58451,#58452,#58453,#58454,#58455,#58456,#58457,#58458,
#58459,#58460,#58461,#58462,#58463,#58464,#58465,#58466,#58467,#58468,#58469,
#58470,#58471,#58472,#58473,#58474),.UNSPECIFIED.,.F.,.F.,(4,3,3,3,3,3,
3,3,3,3,3,3,3,3,4),(-16.6593010344899,-16.3874022811796,-15.8908143332651,
-15.3942263853505,-14.897638437436,-14.4010504895215,-13.9044625416069,
-13.4078745936924,-12.9112866457779,-12.4146986978633,-11.9181107499488,
-11.4215228020343,-10.9249348541197,-10.4283469062052,-10.3761157273103),
 .UNSPECIFIED.);
#634=B_SPLINE_CURVE_WITH_KNOTS('',3,(#58475,#58476,#58477,#58478,#58479,
#58480,#58481,#58482,#58483,#58484,#58485,#58486,#58487,#58488,#58489,#58490,
#58491,#58492,#58493,#58494,#58495,#58496,#58497,#58498,#58499,#58500,#58501,
#58502,#58503,#58504,#58505,#58506,#58507,#58508,#58509,#58510,#58511,#58512,
#58513,#58514,#58515,#58516,#58517),.UNSPECIFIED.,.F.,.F.,(4,3,3,3,3,3,
3,3,3,3,3,3,3,3,4),(7.40683401332261,7.44881921871799,7.94540716663252,
8.44199511454706,8.93858306246159,9.43517101037612,9.93175895829065,10.4283469062052,
10.9249348541197,11.4215228020343,11.9181107499488,12.4146986978633,12.9112866457779,
13.4078745936924,13.6900193205022),.UNSPECIFIED.);
#635=B_SPLINE_CURVE_WITH_KNOTS('',3,(#58522,#58523,#58524,#58525,#58526,
#58527,#58528,#58529,#58530,#58531,#58532,#58533,#58534,#58535,#58536,#58537,
#58538,#58539,#58540,#58541,#58542,#58543,#58544,#58545,#58546,#58547,#58548,
#58549,#58550,#58551,#58552,#58553,#58554,#58555,#58556,#58557,#58558,#58559,
#58560,#58561,#58562,#58563,#58564),.UNSPECIFIED.,.F.,.F.,(4,3,3,3,3,3,
3,3,3,3,3,3,3,3,4),(-22.9424863416695,-22.8430456040685,-22.346457656154,
-21.8498697082395,-21.3532817603249,-20.8566938124104,-20.3601058644958,
-19.8635179165813,-19.3669299686668,-18.8703420207523,-18.3737540728377,
-17.8771661249232,-17.3805781770087,-16.8839902290941,-16.6593010344899),
 .UNSPECIFIED.);
#636=B_SPLINE_CURVE_WITH_KNOTS('',3,(#58565,#58566,#58567,#58568,#58569,
#58570,#58571,#58572,#58573,#58574,#58575,#58576,#58577,#58578,#58579,#58580,
#58581,#58582,#58583,#58584,#58585,#58586,#58587,#58588,#58589,#58590,#58591,
#58592,#58593,#58594,#58595,#58596,#58597,#58598,#58599,#58600,#58601,#58602,
#58603,#58604,#58605,#58606,#58607),.UNSPECIFIED.,.F.,.F.,(4,3,3,3,3,3,
3,3,3,3,3,3,3,3,4),(13.6900193205022,13.9044625416069,14.4010504895214,
14.897638437436,15.3942263853505,15.8908143332651,16.3874022811796,16.8839902290941,
17.3805781770086,17.8771661249232,18.3737540728377,18.8703420207522,19.3669299686668,
19.8635179165813,19.9732046276818),.UNSPECIFIED.);
#637=B_SPLINE_CURVE_WITH_KNOTS('',3,(#58612,#58613,#58614,#58615,#58616,
#58617,#58618,#58619,#58620,#58621,#58622,#58623,#58624,#58625,#58626,#58627,
#58628,#58629,#58630,#58631,#58632,#58633,#58634,#58635,#58636,#58637,#58638,
#58639,#58640,#58641,#58642,#58643,#58644,#58645,#58646,#58647,#58648,#58649,
#58650,#58651),.UNSPECIFIED.,.F.,.F.,(4,3,3,3,3,3,3,3,3,3,3,3,3,4),(-29.225671648849,
-28.8021009790429,-28.3055130311284,-27.8089250832139,-27.3123371352993,
-26.8157491873848,-26.3191612394702,-25.8225732915557,-25.3259853436412,
-24.8293973957266,-24.3328094478121,-23.8362214998976,-23.3396335519831,
-22.9424863416695),.UNSPECIFIED.);
#638=B_SPLINE_CURVE_WITH_KNOTS('',3,(#58652,#58653,#58654,#58655,#58656,
#58657,#58658,#58659,#58660,#58661,#58662,#58663,#58664,#58665,#58666,#58667,
#58668,#58669,#58670,#58671,#58672,#58673,#58674,#58675,#58676,#58677,#58678,
#58679,#58680,#58681,#58682,#58683,#58684,#58685,#58686,#58687,#58688,#58689,
#58690,#58691),.UNSPECIFIED.,.F.,.F.,(4,3,3,3,3,3,3,3,3,3,3,3,3,4),(19.9732046276818,
20.3601058644958,20.8566938124104,21.3532817603249,21.8498697082394,22.346457656154,
22.8430456040685,23.339633551983,23.8362214998976,24.3328094478121,24.8293973957266,
25.3259853436412,25.8225732915557,26.2563899348614),.UNSPECIFIED.);
#639=B_SPLINE_CURVE_WITH_KNOTS('',3,(#58696,#58697,#58698,#58699,#58700,
#58701,#58702,#58703,#58704,#58705,#58706,#58707,#58708,#58709,#58710,#58711,
#58712,#58713,#58714,#58715,#58716,#58717,#58718,#58719,#58720,#58721,#58722,
#58723,#58724,#58725,#58726,#58727,#58728,#58729,#58730,#58731,#58732,#58733,
#58734,#58735,#58736,#58737,#58738),.UNSPECIFIED.,.F.,.F.,(4,3,3,3,3,3,
3,3,3,3,3,3,3,3,4),(-35.5088569560286,-35.2577443019318,-34.7611563540173,
-34.2645684061028,-33.7679804581882,-33.2713925102737,-32.7748045623592,
-32.2782166144446,-31.7816286665301,-31.2850407186156,-30.788452770701,
-30.2918648227865,-29.795276874872,-29.2986889269574,-29.225671648849),
 .UNSPECIFIED.);
#640=B_SPLINE_CURVE_WITH_KNOTS('',3,(#58739,#58740,#58741,#58742,#58743,
#58744,#58745,#58746,#58747,#58748,#58749,#58750,#58751,#58752,#58753,#58754,
#58755,#58756,#58757,#58758,#58759,#58760,#58761,#58762,#58763,#58764,#58765,
#58766,#58767,#58768,#58769,#58770,#58771,#58772,#58773,#58774,#58775,#58776,
#58777,#58778,#58779,#58780,#58781),.UNSPECIFIED.,.F.,.F.,(4,3,3,3,3,3,
3,3,3,3,3,3,3,3,4),(26.2563899348614,26.3191612394702,26.8157491873848,
27.3123371352993,27.8089250832138,28.3055130311284,28.8021009790429,29.2986889269574,
29.795276874872,30.2918648227865,30.788452770701,31.2850407186156,31.7816286665301,
32.2782166144446,32.5395752420409),.UNSPECIFIED.);
#641=B_SPLINE_CURVE_WITH_KNOTS('',3,(#58786,#58787,#58788,#58789,#58790,
#58791,#58792,#58793,#58794,#58795,#58796,#58797,#58798,#58799,#58800,#58801,
#58802,#58803,#58804,#58805,#58806,#58807,#58808,#58809,#58810,#58811,#58812,
#58813,#58814,#58815,#58816,#58817,#58818,#58819,#58820,#58821,#58822,#58823,
#58824,#58825,#58826,#58827,#58828),.UNSPECIFIED.,.F.,.F.,(4,3,3,3,3,3,
3,3,3,3,3,3,3,3,4),(-41.7920422632082,-41.7133876248208,-41.2167996769062,
-40.7202117289917,-40.2236237810772,-39.7270358331626,-39.2304478852481,
-38.7338599373336,-38.237271989419,-37.7406840415045,-37.24409609359,-36.7475081456754,
-36.2509201977609,-35.7543322498464,-35.5088569560286),.UNSPECIFIED.);
#642=B_SPLINE_CURVE_WITH_KNOTS('',3,(#58829,#58830,#58831,#58832,#58833,
#58834,#58835,#58836,#58837,#58838,#58839,#58840,#58841,#58842,#58843,#58844,
#58845,#58846,#58847,#58848,#58849,#58850,#58851,#58852,#58853,#58854,#58855,
#58856,#58857,#58858,#58859,#58860,#58861,#58862,#58863,#58864,#58865,#58866,
#58867,#58868,#58869,#58870,#58871),.UNSPECIFIED.,.F.,.F.,(4,3,3,3,3,3,
3,3,3,3,3,3,3,3,4),(32.5395752420409,32.7748045623592,33.2713925102737,
33.7679804581882,34.2645684061028,34.7611563540173,35.2577443019318,35.7543322498464,
36.2509201977609,36.7475081456754,37.24409609359,37.7406840415045,38.237271989419,
38.7338599373336,38.8227605492205),.UNSPECIFIED.);
#643=B_SPLINE_CURVE_WITH_KNOTS('',3,(#58876,#58877,#58878,#58879,#58880,
#58881,#58882,#58883,#58884,#58885,#58886,#58887,#58888,#58889,#58890,#58891,
#58892,#58893,#58894,#58895,#58896,#58897,#58898,#58899,#58900,#58901,#58902,
#58903,#58904,#58905,#58906,#58907,#58908,#58909,#58910,#58911,#58912,#58913,
#58914,#58915),.UNSPECIFIED.,.F.,.F.,(4,3,3,3,3,3,3,3,3,3,3,3,3,4),(-48.0752275703878,
-47.6724429997952,-47.1758550518806,-46.6792671039661,-46.1826791560516,
-45.686091208137,-45.1895032602225,-44.692915312308,-44.1963273643934,-43.6997394164789,
-43.2031514685644,-42.7065635206498,-42.2099755727353,-41.7920422632082),
 .UNSPECIFIED.);
#644=B_SPLINE_CURVE_WITH_KNOTS('',3,(#58916,#58917,#58918,#58919,#58920,
#58921,#58922,#58923,#58924,#58925,#58926,#58927,#58928,#58929,#58930,#58931,
#58932,#58933,#58934,#58935,#58936,#58937,#58938,#58939,#58940,#58941,#58942,
#58943,#58944,#58945,#58946,#58947,#58948,#58949,#58950,#58951,#58952,#58953,
#58954,#58955),.UNSPECIFIED.,.F.,.F.,(4,3,3,3,3,3,3,3,3,3,3,3,3,4),(38.8227605492205,
39.2304478852481,39.7270358331626,40.2236237810772,40.7202117289917,41.2167996769062,
41.7133876248208,42.2099755727353,42.7065635206498,43.2031514685644,43.6997394164789,
44.1963273643934,44.692915312308,45.1059458564001),.UNSPECIFIED.);
#645=B_SPLINE_CURVE_WITH_KNOTS('',3,(#58960,#58961,#58962,#58963,#58964,
#58965,#58966,#58967,#58968,#58969,#58970,#58971,#58972,#58973,#58974,#58975,
#58976,#58977,#58978,#58979,#58980,#58981,#58982,#58983,#58984,#58985,#58986,
#58987,#58988,#58989,#58990,#58991,#58992,#58993,#58994,#58995,#58996,#58997,
#58998,#58999,#59000,#59001,#59002),.UNSPECIFIED.,.F.,.F.,(4,3,3,3,3,3,
3,3,3,3,3,3,3,3,4),(-54.3584128775674,-54.1280863226841,-53.6314983747696,
-53.134910426855,-52.6383224789405,-52.141734531026,-51.6451465831114,-51.1485586351969,
-50.6519706872824,-50.1553827393678,-49.6587947914533,-49.1622068435388,
-48.6656188956242,-48.1690309477097,-48.0752275703878),.UNSPECIFIED.);
#646=B_SPLINE_CURVE_WITH_KNOTS('',3,(#59003,#59004,#59005,#59006,#59007,
#59008,#59009,#59010,#59011,#59012,#59013,#59014,#59015,#59016,#59017,#59018,
#59019,#59020,#59021,#59022,#59023,#59024,#59025,#59026,#59027,#59028,#59029,
#59030,#59031,#59032,#59033,#59034,#59035,#59036,#59037,#59038,#59039,#59040,
#59041,#59042,#59043,#59044,#59045),.UNSPECIFIED.,.F.,.F.,(4,3,3,3,3,3,
3,3,3,3,3,3,3,3,4),(45.1059458564001,45.1895032602225,45.686091208137,46.1826791560515,
46.6792671039661,47.1758550518806,47.6724429997951,48.1690309477097,48.6656188956242,
49.1622068435387,49.6587947914533,50.1553827393678,50.6519706872824,51.1485586351969,
51.3891311635797),.UNSPECIFIED.);
#647=B_SPLINE_CURVE_WITH_KNOTS('',3,(#59050,#59051,#59052,#59053,#59054,
#59055,#59056,#59057,#59058,#59059,#59060,#59061,#59062,#59063,#59064,#59065,
#59066,#59067,#59068,#59069,#59070,#59071,#59072,#59073,#59074,#59075,#59076,
#59077,#59078,#59079,#59080,#59081,#59082,#59083,#59084,#59085,#59086,#59087,
#59088,#59089,#59090,#59091,#59092),.UNSPECIFIED.,.F.,.F.,(4,3,3,3,3,3,
3,3,3,3,3,3,3,3,4),(-60.641598184747,-60.583729645573,-60.0871416976585,
-59.590553749744,-59.0939658018294,-58.5973778539149,-58.1007899060003,
-57.6042019580858,-57.1076140101713,-56.6110260622567,-56.1144381143422,
-55.6178501664277,-55.1212622185132,-54.6246742705986,-54.3584128775674),
 .UNSPECIFIED.);
#648=B_SPLINE_CURVE_WITH_KNOTS('',3,(#59093,#59094,#59095,#59096,#59097,
#59098,#59099,#59100,#59101,#59102,#59103,#59104,#59105,#59106,#59107,#59108,
#59109,#59110,#59111,#59112,#59113,#59114,#59115,#59116,#59117,#59118,#59119,
#59120,#59121,#59122,#59123,#59124,#59125,#59126,#59127,#59128,#59129,#59130,
#59131,#59132,#59133,#59134,#59135),.UNSPECIFIED.,.F.,.F.,(4,3,3,3,3,3,
3,3,3,3,3,3,3,3,4),(51.3891311635797,51.6451465831114,52.1417345310259,
52.6383224789405,53.134910426855,53.6314983747695,54.1280863226841,54.6246742705986,
55.1212622185132,55.6178501664277,56.1144381143422,56.6110260622567,57.1076140101713,
57.6042019580858,57.6723164707593),.UNSPECIFIED.);
#649=B_SPLINE_CURVE_WITH_KNOTS('',3,(#59140,#59141,#59142,#59143,#59144,
#59145,#59146,#59147,#59148,#59149,#59150,#59151,#59152,#59153,#59154,#59155,
#59156,#59157,#59158,#59159,#59160,#59161,#59162,#59163,#59164,#59165,#59166,
#59167,#59168,#59169,#59170,#59171,#59172,#59173,#59174,#59175,#59176,#59177,
#59178,#59179),.UNSPECIFIED.,.F.,.F.,(4,3,3,3,3,3,3,3,3,3,3,3,3,4),(-66.9247834919266,
-66.5427850205474,-66.0461970726329,-65.5496091247183,-65.0530211768038,
-64.5564332288893,-64.0598452809748,-63.5632573330602,-63.0666693851457,
-62.5700814372311,-62.0734934893166,-61.5769055414021,-61.0803175934875,
-60.641598184747),.UNSPECIFIED.);
#650=B_SPLINE_CURVE_WITH_KNOTS('',3,(#59180,#59181,#59182,#59183,#59184,
#59185,#59186,#59187,#59188,#59189,#59190,#59191,#59192,#59193,#59194,#59195,
#59196,#59197,#59198,#59199,#59200,#59201,#59202,#59203,#59204,#59205,#59206,
#59207,#59208,#59209,#59210,#59211,#59212,#59213,#59214,#59215,#59216,#59217,
#59218,#59219),.UNSPECIFIED.,.F.,.F.,(4,3,3,3,3,3,3,3,3,3,3,3,3,4),(57.6723164707593,
58.1007899060003,58.5973778539149,59.0939658018294,59.5905537497439,60.0871416976585,
60.583729645573,61.0803175934875,61.5769055414021,62.0734934893166,62.5700814372311,
63.0666693851457,63.5632573330602,63.9555017779389),.UNSPECIFIED.);
#651=B_SPLINE_CURVE_WITH_KNOTS('',3,(#59224,#59225,#59226,#59227,#59228,
#59229,#59230,#59231,#59232,#59233,#59234,#59235,#59236,#59237,#59238,#59239,
#59240,#59241,#59242,#59243,#59244,#59245,#59246,#59247,#59248,#59249,#59250,
#59251,#59252,#59253,#59254,#59255,#59256,#59257,#59258,#59259,#59260,#59261,
#59262,#59263,#59264,#59265,#59266),.UNSPECIFIED.,.F.,.F.,(4,3,3,3,3,3,
3,3,3,3,3,3,3,3,4),(-73.2079687991062,-72.9984283434363,-72.5018403955218,
-72.0052524476073,-71.5086644996927,-71.0120765517782,-70.5154886038637,
-70.0189006559491,-69.5223127080346,-69.0257247601201,-68.5291368122056,
-68.032548864291,-67.5359609163765,-67.0393729684619,-66.9247834919266),
 .UNSPECIFIED.);
#652=B_SPLINE_CURVE_WITH_KNOTS('',3,(#59267,#59268,#59269,#59270,#59271,
#59272,#59273,#59274,#59275,#59276,#59277,#59278,#59279,#59280,#59281,#59282,
#59283,#59284,#59285,#59286,#59287,#59288,#59289,#59290,#59291,#59292,#59293,
#59294,#59295,#59296,#59297,#59298,#59299,#59300,#59301,#59302,#59303,#59304,
#59305,#59306,#59307,#59308,#59309),.UNSPECIFIED.,.F.,.F.,(4,3,3,3,3,3,
3,3,3,3,3,3,3,3,4),(63.9555017779389,64.0598452809747,64.5564332288893,
65.0530211768038,65.5496091247183,66.0461970726329,66.5427850205474,67.0393729684619,
67.5359609163765,68.032548864291,68.5291368122055,69.0257247601201,69.5223127080346,
70.0189006559491,70.2386870851185),.UNSPECIFIED.);
#653=B_SPLINE_CURVE_WITH_KNOTS('',3,(#59314,#59315,#59316,#59317,#59318,
#59319,#59320,#59321,#59322,#59323,#59324,#59325,#59326,#59327,#59328,#59329,
#59330,#59331,#59332,#59333,#59334,#59335,#59336,#59337,#59338,#59339,#59340,
#59341,#59342,#59343,#59344,#59345,#59346,#59347,#59348,#59349,#59350,#59351,
#59352,#59353,#59354,#59355,#59356),.UNSPECIFIED.,.F.,.F.,(4,3,3,3,3,3,
3,3,3,3,3,3,3,3,4),(-79.4911541062858,-79.4540716663253,-78.9574837184107,
-78.4608957704962,-77.9643078225817,-77.4677198746671,-76.9711319267526,
-76.4745439788381,-75.9779560309235,-75.481368083009,-74.9847801350945,
-74.4881921871799,-73.9916042392654,-73.4950162913509,-73.2079687991062),
 .UNSPECIFIED.);
#654=B_SPLINE_CURVE_WITH_KNOTS('',3,(#59357,#59358,#59359,#59360,#59361,
#59362,#59363,#59364,#59365,#59366,#59367,#59368,#59369,#59370,#59371,#59372,
#59373,#59374,#59375,#59376,#59377,#59378,#59379,#59380,#59381,#59382,#59383,
#59384,#59385,#59386,#59387,#59388,#59389,#59390,#59391,#59392,#59393,#59394,
#59395,#59396,#59397,#59398,#59399),.UNSPECIFIED.,.F.,.F.,(4,3,3,3,3,3,
3,3,3,3,3,3,3,3,4),(70.2386870851185,70.5154886038637,71.0120765517782,
71.5086644996927,72.0052524476073,72.5018403955218,72.9984283434363,73.4950162913509,
73.9916042392654,74.4881921871799,74.9847801350944,75.481368083009,75.9779560309235,
76.474543978838,76.5218723922981),.UNSPECIFIED.);
#655=B_SPLINE_CURVE_WITH_KNOTS('',3,(#59404,#59405,#59406,#59407,#59408,
#59409,#59410,#59411,#59412,#59413,#59414,#59415,#59416,#59417,#59418,#59419,
#59420,#59421,#59422,#59423,#59424,#59425,#59426,#59427,#59428,#59429,#59430,
#59431,#59432,#59433,#59434,#59435,#59436,#59437,#59438,#59439,#59440,#59441,
#59442,#59443),.UNSPECIFIED.,.F.,.F.,(4,3,3,3,3,3,3,3,3,3,3,3,3,4),(-85.7743394134654,
-85.4131270412997,-84.9165390933851,-84.4199511454706,-83.9233631975561,
-83.4267752496415,-82.930187301727,-82.4335993538125,-81.9370114058979,
-81.4404234579834,-80.9438355100689,-80.4472475621543,-79.9506596142398,
-79.4911541062858),.UNSPECIFIED.);
#656=B_SPLINE_CURVE_WITH_KNOTS('',3,(#59444,#59445,#59446,#59447,#59448,
#59449,#59450,#59451,#59452,#59453,#59454,#59455,#59456,#59457,#59458,#59459,
#59460,#59461,#59462,#59463,#59464,#59465,#59466,#59467,#59468,#59469,#59470,
#59471,#59472,#59473,#59474,#59475,#59476,#59477,#59478,#59479,#59480,#59481,
#59482,#59483),.UNSPECIFIED.,.F.,.F.,(4,3,3,3,3,3,3,3,3,3,3,3,3,4),(76.5218723922981,
76.9711319267526,77.4677198746671,77.9643078225816,78.4608957704962,78.9574837184107,
79.4540716663252,79.9506596142398,80.4472475621543,80.9438355100688,81.4404234579834,
81.9370114058979,82.4335993538124,82.8050576994777),.UNSPECIFIED.);
#657=B_SPLINE_CURVE_WITH_KNOTS('',3,(#59488,#59489,#59490,#59491,#59492,
#59493,#59494,#59495,#59496,#59497,#59498,#59499,#59500,#59501,#59502,#59503,
#59504,#59505,#59506,#59507,#59508,#59509,#59510,#59511,#59512,#59513,#59514,
#59515,#59516,#59517,#59518,#59519,#59520,#59521,#59522,#59523,#59524,#59525,
#59526,#59527,#59528,#59529,#59530),.UNSPECIFIED.,.F.,.F.,(4,3,3,3,3,3,
3,3,3,3,3,3,3,3,4),(-92.057524720645,-91.8687703641886,-91.3721824162741,
-90.8755944683595,-90.379006520445,-89.8824185725305,-89.3858306246159,
-88.8892426767014,-88.3926547287869,-87.8960667808723,-87.3994788329578,
-86.9028908850433,-86.4063029371287,-85.9097149892142,-85.7743394134654),
 .UNSPECIFIED.);
#658=B_SPLINE_CURVE_WITH_KNOTS('',3,(#59531,#59532,#59533,#59534,#59535,
#59536,#59537,#59538,#59539,#59540,#59541,#59542,#59543,#59544,#59545,#59546,
#59547,#59548,#59549,#59550,#59551,#59552,#59553,#59554,#59555,#59556,#59557,
#59558,#59559,#59560,#59561,#59562,#59563,#59564,#59565,#59566,#59567,#59568,
#59569,#59570,#59571,#59572,#59573),.UNSPECIFIED.,.F.,.F.,(4,3,3,3,3,3,
3,3,3,3,3,3,3,3,4),(82.8050576994777,82.930187301727,83.4267752496415,83.923363197556,
84.4199511454706,84.9165390933851,85.4131270412996,85.9097149892142,86.4063029371287,
86.9028908850432,87.3994788329578,87.8960667808723,88.3926547287869,88.8892426767014,
89.0882430066573),.UNSPECIFIED.);
#659=B_SPLINE_CURVE_WITH_KNOTS('',3,(#59578,#59579,#59580,#59581,#59582,
#59583,#59584,#59585,#59586,#59587,#59588,#59589,#59590,#59591,#59592,#59593,
#59594,#59595,#59596,#59597,#59598,#59599,#59600,#59601,#59602,#59603,#59604,
#59605,#59606,#59607,#59608,#59609,#59610,#59611,#59612,#59613,#59614,#59615,
#59616,#59617,#59618,#59619,#59620),.UNSPECIFIED.,.F.,.F.,(4,3,3,3,3,3,
3,3,3,3,3,3,3,3,4),(-98.3407100278246,-98.3244136870775,-97.827825739163,
-97.3312377912485,-96.8346498433339,-96.3380618954194,-95.8414739475049,
-95.3448859995903,-94.8482980516758,-94.3517101037612,-93.8551221558467,
-93.3585342079322,-92.8619462600177,-92.3653583121031,-92.057524720645),
 .UNSPECIFIED.);
#660=B_SPLINE_CURVE_WITH_KNOTS('',3,(#59621,#59622,#59623,#59624,#59625,
#59626,#59627,#59628,#59629,#59630,#59631,#59632,#59633,#59634,#59635,#59636,
#59637,#59638,#59639,#59640,#59641,#59642,#59643,#59644,#59645,#59646,#59647,
#59648,#59649,#59650,#59651,#59652,#59653,#59654,#59655,#59656,#59657,#59658,
#59659,#59660,#59661,#59662,#59663),.UNSPECIFIED.,.F.,.F.,(4,3,3,3,3,3,
3,3,3,3,3,3,3,3,4),(89.0882430066573,89.3858306246159,89.8824185725304,
90.379006520445,90.8755944683595,91.372182416274,91.8687703641886,92.3653583121031,
92.8619462600176,93.3585342079322,93.8551221558467,94.3517101037612,94.8482980516758,
95.3448859995903,95.3714283138369),.UNSPECIFIED.);
#661=B_SPLINE_CURVE_WITH_KNOTS('',3,(#59668,#59669,#59670,#59671,#59672,
#59673,#59674,#59675,#59676,#59677,#59678,#59679,#59680,#59681,#59682,#59683,
#59684,#59685,#59686,#59687,#59688,#59689,#59690,#59691,#59692,#59693,#59694,
#59695,#59696,#59697,#59698,#59699,#59700,#59701,#59702,#59703,#59704,#59705,
#59706,#59707),.UNSPECIFIED.,.F.,.F.,(4,3,3,3,3,3,3,3,3,3,3,3,3,4),(-104.623895335004,
-104.283469062052,-103.786881114137,-103.290293166223,-102.793705218308,
-102.297117270394,-101.800529322479,-101.303941374565,-100.80735342665,
-100.310765478736,-99.8141775308211,-99.3175895829066,-98.821001634992,
-98.3407100278246),.UNSPECIFIED.);
#662=B_SPLINE_CURVE_WITH_KNOTS('',3,(#59708,#59709,#59710,#59711,#59712,
#59713,#59714,#59715,#59716,#59717,#59718,#59719,#59720,#59721,#59722,#59723,
#59724,#59725,#59726,#59727,#59728,#59729,#59730,#59731,#59732,#59733,#59734,
#59735,#59736,#59737,#59738,#59739,#59740,#59741,#59742,#59743,#59744,#59745,
#59746,#59747),.UNSPECIFIED.,.F.,.F.,(4,3,3,3,3,3,3,3,3,3,3,3,3,4),(95.3714283138369,
95.8414739475048,96.3380618954194,96.8346498433339,97.3312377912484,97.827825739163,
98.3244136870775,98.821001634992,99.3175895829065,99.8141775308211,100.310765478736,
100.80735342665,101.303941374565,101.654613621016),.UNSPECIFIED.);
#663=B_SPLINE_CURVE_WITH_KNOTS('',3,(#59752,#59753,#59754,#59755,#59756,
#59757,#59758,#59759,#59760,#59761,#59762,#59763,#59764,#59765,#59766,#59767,
#59768,#59769,#59770,#59771,#59772,#59773,#59774,#59775,#59776,#59777,#59778,
#59779,#59780,#59781,#59782,#59783,#59784,#59785,#59786,#59787,#59788,#59789,
#59790,#59791,#59792,#59793,#59794),.UNSPECIFIED.,.F.,.F.,(4,3,3,3,3,3,
3,3,3,3,3,3,3,3,4),(-110.907080642184,-110.739112384941,-110.242524437026,
-109.745936489112,-109.249348541197,-108.752760593283,-108.256172645368,
-107.759584697454,-107.262996749539,-106.766408801625,-106.26982085371,
-105.773232905796,-105.276644957881,-104.780057009966,-104.623895335004),
 .UNSPECIFIED.);
#664=B_SPLINE_CURVE_WITH_KNOTS('',3,(#59795,#59796,#59797,#59798,#59799,
#59800,#59801,#59802,#59803,#59804,#59805,#59806,#59807,#59808,#59809,#59810,
#59811,#59812,#59813,#59814,#59815,#59816,#59817,#59818,#59819,#59820,#59821,
#59822,#59823,#59824,#59825,#59826,#59827,#59828,#59829,#59830,#59831,#59832,
#59833,#59834,#59835,#59836,#59837),.UNSPECIFIED.,.F.,.F.,(4,3,3,3,3,3,
3,3,3,3,3,3,3,3,4),(101.654613621016,101.800529322479,102.297117270394,
102.793705218308,103.290293166223,103.786881114137,104.283469062052,104.780057009966,
105.276644957881,105.773232905795,106.26982085371,106.766408801625,107.262996749539,
107.759584697454,107.937798928196),.UNSPECIFIED.);
#665=B_SPLINE_CURVE_WITH_KNOTS('',3,(#59842,#59843,#59844,#59845,#59846,
#59847,#59848,#59849,#59850,#59851,#59852,#59853,#59854,#59855,#59856,#59857,
#59858,#59859,#59860,#59861,#59862,#59863,#59864,#59865,#59866,#59867,#59868,
#59869,#59870,#59871,#59872,#59873,#59874,#59875,#59876,#59877,#59878,#59879,
#59880,#59881),.UNSPECIFIED.,.F.,.F.,(4,3,3,3,3,3,3,3,3,3,3,3,3,4),(-117.190265949363,
-116.698167759915,-116.201579812001,-115.704991864086,-115.208403916172,
-114.711815968257,-114.215228020343,-113.718640072428,-113.222052124514,
-112.725464176599,-112.228876228684,-111.73228828077,-111.235700332855,
-110.907080642184),.UNSPECIFIED.);
#666=B_SPLINE_CURVE_WITH_KNOTS('',3,(#59882,#59883,#59884,#59885,#59886,
#59887,#59888,#59889,#59890,#59891,#59892,#59893,#59894,#59895,#59896,#59897,
#59898,#59899,#59900,#59901,#59902,#59903,#59904,#59905,#59906,#59907,#59908,
#59909,#59910,#59911,#59912,#59913,#59914,#59915,#59916,#59917,#59918,#59919,
#59920,#59921,#59922,#59923,#59924),.UNSPECIFIED.,.F.,.F.,(4,3,3,3,3,3,
3,3,3,3,3,3,3,3,4),(107.937798928196,108.256172645368,108.752760593283,
109.249348541197,109.745936489112,110.242524437026,110.739112384941,111.235700332855,
111.73228828077,112.228876228684,112.725464176599,113.222052124513,113.718640072428,
114.215228020343,114.220984235376),.UNSPECIFIED.);
#667=B_SPLINE_CURVE_WITH_KNOTS('',3,(#59929,#59930,#59931,#59932,#59933,
#59934,#59935,#59936,#59937,#59938,#59939,#59940,#59941,#59942,#59943,#59944,
#59945,#59946,#59947,#59948,#59949,#59950,#59951,#59952,#59953,#59954,#59955,
#59956,#59957,#59958,#59959,#59960,#59961,#59962,#59963,#59964,#59965,#59966,
#59967,#59968,#59969,#59970,#59971),.UNSPECIFIED.,.F.,.F.,(4,3,3,3,3,3,
3,3,3,3,3,3,3,3,4),(-123.473451256543,-123.153811082804,-122.65722313489,
-122.160635186975,-121.664047239061,-121.167459291146,-120.670871343231,
-120.174283395317,-119.677695447402,-119.181107499488,-118.684519551573,
-118.187931603659,-117.691343655744,-117.19475570783,-117.190265949363),
 .UNSPECIFIED.);
#668=B_SPLINE_CURVE_WITH_KNOTS('',3,(#59972,#59973,#59974,#59975,#59976,
#59977,#59978,#59979,#59980,#59981,#59982,#59983,#59984,#59985,#59986,#59987,
#59988,#59989,#59990,#59991,#59992,#59993,#59994,#59995,#59996,#59997,#59998,
#59999,#60000,#60001,#60002,#60003,#60004,#60005,#60006,#60007,#60008,#60009,
#60010,#60011),.UNSPECIFIED.,.F.,.F.,(4,3,3,3,3,3,3,3,3,3,3,3,3,4),(114.220984235376,
114.711815968257,115.208403916172,115.704991864086,116.201579812001,116.698167759915,
117.19475570783,117.691343655744,118.187931603659,118.684519551573,119.181107499488,
119.677695447402,120.174283395317,120.504169542555),.UNSPECIFIED.);
#669=B_SPLINE_CURVE_WITH_KNOTS('',3,(#60017,#60018,#60019,#60020,#60021),
 .UNSPECIFIED.,.F.,.F.,(4,1,4),(135.088484104361,135.265431878537,135.673385145426),
 .UNSPECIFIED.);
#670=B_SPLINE_CURVE_WITH_KNOTS('',3,(#60027,#60028,#60029,#60030,#60031,
#60032,#60033,#60034,#60035,#60036,#60037,#60038,#60039,#60040,#60041,#60042,
#60043),.UNSPECIFIED.,.F.,.F.,(4,1,1,1,1,1,1,1,1,1,1,1,1,1,4),(128.805298797182,
128.809788555648,129.306376503562,129.802964451477,130.299552399392,130.796140347306,
131.292728295221,131.789316243135,132.28590419105,132.782492138964,133.279080086879,
133.775668034793,134.272255982708,134.768843930622,135.088484104361),
 .UNSPECIFIED.);
#671=B_SPLINE_CURVE_WITH_KNOTS('',3,(#60046,#60047,#60048,#60049,#60050,
#60051,#60052,#60053,#60054,#60055,#60056,#60057,#60058,#60059,#60060),
 .UNSPECIFIED.,.F.,.F.,(4,1,1,1,1,1,1,1,1,1,1,1,4),(128.805298797182,128.972000597858,
129.468588545772,129.965176493687,130.461764441601,130.958352389516,131.45494033743,
131.951528285345,132.448116233259,132.944704181174,133.441292129088,133.937880077003,
134.434468024917),.UNSPECIFIED.);
#672=B_SPLINE_CURVE_WITH_KNOTS('',3,(#60065,#60066,#60067,#60068,#60069,
#60070,#60071,#60072,#60073,#60074,#60075,#60076,#60077,#60078,#60079,#60080),
 .UNSPECIFIED.,.F.,.F.,(4,1,1,1,1,1,1,1,1,1,1,1,1,4),(122.522113490002,
122.850733180674,123.347321128588,123.843909076503,124.340497024417,124.837084972332,
125.333672920246,125.830260868161,126.326848816075,126.82343676399,127.320024711904,
127.816612659819,128.313200607733,128.805298797182),.UNSPECIFIED.);
#673=B_SPLINE_CURVE_WITH_KNOTS('',3,(#60081,#60082,#60083,#60084,#60085,
#60086,#60087,#60088,#60089,#60090,#60091,#60092,#60093,#60094,#60095,#60096),
 .UNSPECIFIED.,.F.,.F.,(4,1,1,1,1,1,1,1,1,1,1,1,1,4),(122.522113490002,
123.012945222883,123.509533170798,124.006121118712,124.502709066627,124.999297014541,
125.495884962456,125.99247291037,126.489060858285,126.985648806199,127.482236754114,
127.978824702029,128.475412649943,128.805298797182),.UNSPECIFIED.);
#674=B_SPLINE_CURVE_WITH_KNOTS('',3,(#60101,#60102,#60103,#60104,#60105,
#60106,#60107,#60108,#60109,#60110,#60111,#60112,#60113,#60114,#60115,#60116,
#60117),.UNSPECIFIED.,.F.,.F.,(4,1,1,1,1,1,1,1,1,1,1,1,1,1,4),(116.238928182822,
116.395089857785,116.891677805699,117.388265753614,117.884853701528,118.381441649443,
118.878029597357,119.374617545272,119.871205493186,120.367793441101,120.864381389015,
121.36096933693,121.857557284844,122.354145232759,122.522113490002),
 .UNSPECIFIED.);
#675=B_SPLINE_CURVE_WITH_KNOTS('',3,(#60118,#60119,#60120,#60121,#60122,
#60123,#60124,#60125,#60126,#60127,#60128,#60129,#60130,#60131,#60132,#60133,
#60134),.UNSPECIFIED.,.F.,.F.,(4,1,1,1,1,1,1,1,1,1,1,1,1,1,4),(116.238928182822,
116.557301899994,117.053889847909,117.550477795823,118.047065743738,118.543653691652,
119.040241639567,119.536829587481,120.033417535396,120.530005483311,121.026593431225,
121.52318137914,122.019769327054,122.516357274969,122.522113490002),
 .UNSPECIFIED.);
#676=B_SPLINE_CURVE_WITH_KNOTS('',3,(#60139,#60140,#60141,#60142,#60143,
#60144,#60145,#60146,#60147,#60148,#60149,#60150,#60151,#60152,#60153,#60154),
 .UNSPECIFIED.,.F.,.F.,(4,1,1,1,1,1,1,1,1,1,1,1,1,4),(109.955742875643,
110.43603448281,110.932622430725,111.429210378639,111.925798326554,112.422386274468,
112.918974222383,113.415562170297,113.912150118212,114.408738066126,114.905326014041,
115.401913961956,115.89850190987,116.238928182822),.UNSPECIFIED.);
#677=B_SPLINE_CURVE_WITH_KNOTS('',3,(#60155,#60156,#60157,#60158,#60159,
#60160,#60161,#60162,#60163,#60164,#60165,#60166,#60167,#60168,#60169,#60170,
#60171),.UNSPECIFIED.,.F.,.F.,(4,1,1,1,1,1,1,1,1,1,1,1,1,1,4),(109.955742875643,
110.101658577105,110.59824652502,111.094834472934,111.591422420849,112.088010368763,
112.584598316678,113.081186264593,113.577774212507,114.074362160422,114.570950108336,
115.067538056251,115.564126004165,116.06071395208,116.238928182822),
 .UNSPECIFIED.);
#678=B_SPLINE_CURVE_WITH_KNOTS('',3,(#60176,#60177,#60178,#60179,#60180,
#60181,#60182,#60183,#60184,#60185,#60186,#60187,#60188,#60189,#60190,#60191,
#60192),.UNSPECIFIED.,.F.,.F.,(4,1,1,1,1,1,1,1,1,1,1,1,1,1,4),(103.672557568463,
103.980391159921,104.476979107836,104.97356705575,105.470155003665,105.966742951579,
106.463330899494,106.959918847408,107.456506795323,107.953094743238,108.449682691152,
108.946270639067,109.442858586981,109.939446534896,109.955742875643),
 .UNSPECIFIED.);
#679=B_SPLINE_CURVE_WITH_KNOTS('',3,(#60193,#60194,#60195,#60196,#60197,
#60198,#60199,#60200,#60201,#60202,#60203,#60204,#60205,#60206,#60207,#60208),
 .UNSPECIFIED.,.F.,.F.,(4,1,1,1,1,1,1,1,1,1,1,1,1,4),(103.672557568463,
104.142603202131,104.639191150046,105.13577909796,105.632367045875,106.128954993789,
106.625542941704,107.122130889618,107.618718837533,108.115306785447,108.611894733362,
109.108482681276,109.605070629191,109.955742875643),.UNSPECIFIED.);
#680=B_SPLINE_CURVE_WITH_KNOTS('',3,(#60213,#60214,#60215,#60216,#60217,
#60218,#60219,#60220,#60221,#60222,#60223,#60224,#60225,#60226,#60227,#60228,
#60229),.UNSPECIFIED.,.F.,.F.,(4,1,1,1,1,1,1,1,1,1,1,1,1,1,4),(97.3893722612836,
97.5247478370324,98.0213357849469,98.5179237328614,99.014511680776,99.5110996286905,
100.007687576605,100.50427552452,101.000863472434,101.497451420349,101.994039368263,
102.490627316178,102.987215264092,103.483803212007,103.672557568463),
 .UNSPECIFIED.);
#681=B_SPLINE_CURVE_WITH_KNOTS('',3,(#60230,#60231,#60232,#60233,#60234,
#60235,#60236,#60237,#60238,#60239,#60240,#60241,#60242,#60243,#60244,#60245,
#60246),.UNSPECIFIED.,.F.,.F.,(4,1,1,1,1,1,1,1,1,1,1,1,1,1,4),(97.3893722612835,
97.686959879242,98.1835478271566,98.6801357750711,99.1767237229856,99.6733116709002,
100.169899618815,100.666487566729,101.163075514644,101.659663462558,102.156251410473,
102.652839358387,103.149427306302,103.646015254216,103.672557568463),
 .UNSPECIFIED.);
#682=B_SPLINE_CURVE_WITH_KNOTS('',3,(#60251,#60252,#60253,#60254,#60255,
#60256,#60257,#60258,#60259,#60260,#60261,#60262,#60263,#60264,#60265,#60266),
 .UNSPECIFIED.,.F.,.F.,(4,1,1,1,1,1,1,1,1,1,1,1,1,4),(91.106186954104,91.565692462058,
92.0622804099725,92.558868357887,93.0554563058016,93.5520442537161,94.0486322016306,
94.5452201495452,95.0418080974597,95.5383960453742,96.0349839932888,96.5315719412033,
97.0281598891178,97.3893722612836),.UNSPECIFIED.);
#683=B_SPLINE_CURVE_WITH_KNOTS('',3,(#60267,#60268,#60269,#60270,#60271,
#60272,#60273,#60274,#60275,#60276,#60277,#60278,#60279,#60280,#60281,#60282,
#60283),.UNSPECIFIED.,.F.,.F.,(4,1,1,1,1,1,1,1,1,1,1,1,1,1,4),(91.106186954104,
91.2313165563531,91.7279045042677,92.2244924521822,92.7210804000967,93.2176683480112,
93.7142562959258,94.2108442438403,94.7074321917548,95.2040201396694,95.7006080875839,
96.1971960354985,96.693783983413,97.1903719313275,97.3893722612835),
 .UNSPECIFIED.);
#684=B_SPLINE_CURVE_WITH_KNOTS('',3,(#60288,#60289,#60290,#60291,#60292,
#60293,#60294,#60295,#60296,#60297,#60298,#60299,#60300,#60301,#60302,#60303,
#60304),.UNSPECIFIED.,.F.,.F.,(4,1,1,1,1,1,1,1,1,1,1,1,1,1,4),(84.8230016469244,
85.110049139169,85.6066370870836,86.1032250349981,86.5998129829126,87.0964009308272,
87.5929888787417,88.0895768266562,88.5861647745708,89.0827527224853,89.5793406703998,
90.0759286183144,90.5725165662289,91.0691045141434,91.106186954104),
 .UNSPECIFIED.);
#685=B_SPLINE_CURVE_WITH_KNOTS('',3,(#60305,#60306,#60307,#60308,#60309,
#60310,#60311,#60312,#60313,#60314,#60315,#60316,#60317,#60318,#60319,#60320),
 .UNSPECIFIED.,.F.,.F.,(4,1,1,1,1,1,1,1,1,1,1,1,1,4),(84.8230016469244,
85.2722611813787,85.7688491292933,86.2654370772078,86.7620250251223,87.2586129730369,
87.7552009209514,88.2517888688659,88.7483768167804,89.244964764695,89.7415527126095,
90.2381406605241,90.7347286084386,91.106186954104),.UNSPECIFIED.);
#686=B_SPLINE_CURVE_WITH_KNOTS('',3,(#60325,#60326,#60327,#60328,#60329,
#60330,#60331,#60332,#60333,#60334,#60335,#60336,#60337,#60338,#60339,#60340,
#60341),.UNSPECIFIED.,.F.,.F.,(4,1,1,1,1,1,1,1,1,1,1,1,1,1,4),(78.5398163397448,
78.6544058162801,79.1509937641947,79.6475817121092,80.1441696600237,80.6407576079382,
81.1373455558528,81.6339335037673,82.1305214516818,82.6271093995964,83.1236973475109,
83.6202852954254,84.11687324334,84.6134611912545,84.8230016469244),
 .UNSPECIFIED.);
#687=B_SPLINE_CURVE_WITH_KNOTS('',3,(#60342,#60343,#60344,#60345,#60346,
#60347,#60348,#60349,#60350,#60351,#60352,#60353,#60354,#60355,#60356,#60357,
#60358),.UNSPECIFIED.,.F.,.F.,(4,1,1,1,1,1,1,1,1,1,1,1,1,1,4),(78.5398163397448,
78.8166178584898,79.3132058064043,79.8097937543189,80.3063817022334,80.8029696501479,
81.2995575980625,81.796145545977,82.2927334938915,82.7893214418061,83.2859093897206,
83.7824973376351,84.2790852855497,84.7756732334642,84.8230016469244),
 .UNSPECIFIED.);
#688=B_SPLINE_CURVE_WITH_KNOTS('',3,(#60363,#60364,#60365,#60366,#60367,
#60368,#60369,#60370,#60371,#60372,#60373,#60374,#60375,#60376,#60377,#60378),
 .UNSPECIFIED.,.F.,.F.,(4,1,1,1,1,1,1,1,1,1,1,1,1,4),(72.2566310325652,
72.6953504413057,73.1919383892203,73.6885263371348,74.1851142850493,74.6817022329639,
75.1782901808784,75.6748781287929,76.1714660767074,76.668054024622,77.1646419725365,
77.661229920451,78.1578178683656,78.5398163397448),.UNSPECIFIED.);
#689=B_SPLINE_CURVE_WITH_KNOTS('',3,(#60379,#60380,#60381,#60382,#60383,
#60384,#60385,#60386,#60387,#60388,#60389,#60390,#60391,#60392,#60393,#60394,
#60395),.UNSPECIFIED.,.F.,.F.,(4,1,1,1,1,1,1,1,1,1,1,1,1,1,4),(72.2566310325652,
72.3609745356009,72.8575624835154,73.3541504314299,73.8507383793445,74.347326327259,
74.8439142751735,75.3405022230881,75.8370901710026,76.3336781189171,76.8302660668317,
77.3268540147462,77.8234419626607,78.3200299105753,78.5398163397448),
 .UNSPECIFIED.);
#690=B_SPLINE_CURVE_WITH_KNOTS('',3,(#60400,#60401,#60402,#60403,#60404,
#60405,#60406,#60407,#60408,#60409,#60410,#60411,#60412,#60413,#60414,#60415,
#60416),.UNSPECIFIED.,.F.,.F.,(4,1,1,1,1,1,1,1,1,1,1,1,1,1,4),(65.9734457253856,
66.2397071184168,66.7362950663313,67.2328830142459,67.7294709621604,68.2260589100749,
68.7226468579895,69.219234805904,69.7158227538185,70.2124107017331,70.7089986496476,
71.2055865975621,71.7021745454767,72.1987624933912,72.2566310325652),
 .UNSPECIFIED.);
#691=B_SPLINE_CURVE_WITH_KNOTS('',3,(#60417,#60418,#60419,#60420,#60421,
#60422,#60423,#60424,#60425,#60426,#60427,#60428,#60429,#60430,#60431,#60432),
 .UNSPECIFIED.,.F.,.F.,(4,1,1,1,1,1,1,1,1,1,1,1,1,4),(65.9734457253856,
66.4019191606265,66.898507108541,67.3950950564555,67.8916830043701,68.3882709522846,
68.8848589001991,69.3814468481137,69.8780347960282,70.3746227439427,70.8712106918573,
71.3677986397718,71.8643865876863,72.2566310325652),.UNSPECIFIED.);
#692=B_SPLINE_CURVE_WITH_KNOTS('',3,(#60437,#60438,#60439,#60440,#60441,
#60442,#60443,#60444,#60445,#60446,#60447,#60448,#60449,#60450,#60451,#60452,
#60453),.UNSPECIFIED.,.F.,.F.,(4,1,1,1,1,1,1,1,1,1,1,1,1,1,4),(59.690260418206,
59.7840637955279,60.2806517434424,60.7772396913569,61.2738276392715,61.770415587186,
62.2670035351005,62.7635914830151,63.2601794309296,63.7567673788441,64.2533553267587,
64.7499432746732,65.2465312225877,65.7431191705023,65.9734457253856),
 .UNSPECIFIED.);
#693=B_SPLINE_CURVE_WITH_KNOTS('',3,(#60454,#60455,#60456,#60457,#60458,
#60459,#60460,#60461,#60462,#60463,#60464,#60465,#60466,#60467,#60468,#60469,
#60470),.UNSPECIFIED.,.F.,.F.,(4,1,1,1,1,1,1,1,1,1,1,1,1,1,4),(59.690260418206,
59.9462758377375,60.4428637856521,60.9394517335666,61.4360396814811,61.9326276293957,
62.4292155773102,62.9258035252248,63.4223914731393,63.9189794210538,64.4155673689683,
64.9121553168829,65.4087432647974,65.9053312127119,65.9734457253856),
 .UNSPECIFIED.);
#694=B_SPLINE_CURVE_WITH_KNOTS('',3,(#60475,#60476,#60477,#60478,#60479,
#60480,#60481,#60482,#60483,#60484,#60485,#60486,#60487,#60488,#60489,#60490),
 .UNSPECIFIED.,.F.,.F.,(4,1,1,1,1,1,1,1,1,1,1,1,1,4),(53.4070751110264,
53.8250084205535,54.321596368468,54.8181843163825,55.3147722642971,55.8113602122116,
56.3079481601261,56.8045361080407,57.3011240559552,57.7977120038697,58.2942999517843,
58.7908878996988,59.2874758476133,59.690260418206),.UNSPECIFIED.);
#695=B_SPLINE_CURVE_WITH_KNOTS('',3,(#60491,#60492,#60493,#60494,#60495,
#60496,#60497,#60498,#60499,#60500,#60501,#60502,#60503,#60504,#60505,#60506,
#60507),.UNSPECIFIED.,.F.,.F.,(4,1,1,1,1,1,1,1,1,1,1,1,1,1,4),(53.4070751110264,
53.4906325148486,53.9872204627632,54.4838084106777,54.9803963585922,55.4769843065068,
55.9735722544213,56.4701602023358,56.9667481502504,57.4633360981649,57.9599240460794,
58.456511993994,58.9530999419085,59.449687889823,59.690260418206),
 .UNSPECIFIED.);
#696=B_SPLINE_CURVE_WITH_KNOTS('',3,(#60512,#60513,#60514,#60515,#60516,
#60517,#60518,#60519,#60520,#60521,#60522,#60523,#60524,#60525,#60526,#60527,
#60528),.UNSPECIFIED.,.F.,.F.,(4,1,1,1,1,1,1,1,1,1,1,1,1,1,4),(47.1238898038468,
47.3693650976645,47.8659530455791,48.3625409934936,48.8591289414081,49.3557168893227,
49.8523048372372,50.3488927851517,50.8454807330663,51.3420686809808,51.8386566288953,
52.3352445768099,52.8318325247244,53.3284204726389,53.4070751110264),
 .UNSPECIFIED.);
#697=B_SPLINE_CURVE_WITH_KNOTS('',3,(#60529,#60530,#60531,#60532,#60533,
#60534,#60535,#60536,#60537,#60538,#60539,#60540,#60541,#60542,#60543,#60544),
 .UNSPECIFIED.,.F.,.F.,(4,1,1,1,1,1,1,1,1,1,1,1,1,4),(47.1238898038468,
47.5315771398742,48.0281650877888,48.5247530357033,49.0213409836178,49.5179289315324,
50.0145168794469,50.5111048273614,51.007692775276,51.5042807231905,52.000868671105,
52.4974566190196,52.9940445669341,53.4070751110264),.UNSPECIFIED.);
#698=B_SPLINE_CURVE_WITH_KNOTS('',3,(#60549,#60550,#60551,#60552,#60553,
#60554,#60555,#60556,#60557,#60558,#60559,#60560,#60561,#60562,#60563,#60564,
#60565),.UNSPECIFIED.,.F.,.F.,(4,1,1,1,1,1,1,1,1,1,1,1,1,1,4),(40.8407044966673,
40.9137217747756,41.4103097226902,41.9068976706047,42.4034856185192,42.9000735664337,
43.3966615143483,43.8932494622628,44.3898374101773,44.8864253580919,45.3830133060064,
45.8796012539209,46.3761892018355,46.87277714975,47.1238898038468),
 .UNSPECIFIED.);
#699=B_SPLINE_CURVE_WITH_KNOTS('',3,(#60566,#60567,#60568,#60569,#60570,
#60571,#60572,#60573,#60574,#60575,#60576,#60577,#60578,#60579,#60580,#60581,
#60582),.UNSPECIFIED.,.F.,.F.,(4,1,1,1,1,1,1,1,1,1,1,1,1,1,4),(40.8407044966672,
41.0759338169853,41.5725217648998,42.0691097128144,42.5656976607289,43.0622856086434,
43.558873556558,44.0554615044725,44.552049452387,45.0486374003016,45.5452253482161,
46.0418132961306,46.5384012440452,47.0349891919597,47.1238898038468),
 .UNSPECIFIED.);
#700=B_SPLINE_CURVE_WITH_KNOTS('',3,(#60587,#60588,#60589,#60590,#60591,
#60592,#60593,#60594,#60595,#60596,#60597,#60598,#60599,#60600,#60601,#60602),
 .UNSPECIFIED.,.F.,.F.,(4,1,1,1,1,1,1,1,1,1,1,1,1,4),(34.5575191894877,
34.9546663998012,35.4512543477158,35.9478422956303,36.4444302435448,36.9410181914593,
37.4376061393739,37.9341940872884,38.430782035203,38.9273699831175,39.423957931032,
39.9205458789466,40.4171338268611,40.8407044966673),.UNSPECIFIED.);
#701=B_SPLINE_CURVE_WITH_KNOTS('',3,(#60603,#60604,#60605,#60606,#60607,
#60608,#60609,#60610,#60611,#60612,#60613,#60614,#60615,#60616,#60617,#60618,
#60619),.UNSPECIFIED.,.F.,.F.,(4,1,1,1,1,1,1,1,1,1,1,1,1,1,4),(34.5575191894876,
34.6202904940964,35.1168784420109,35.6134663899254,36.11005433784,36.6066422857545,
37.103230233669,37.5998181815836,38.0964061294981,38.5929940774126,39.0895820253272,
39.5861699732417,40.0827579211562,40.5793458690708,40.8407044966672),
 .UNSPECIFIED.);
#702=B_SPLINE_CURVE_WITH_KNOTS('',3,(#60624,#60625,#60626,#60627,#60628,
#60629,#60630,#60631,#60632,#60633,#60634,#60635,#60636,#60637,#60638,#60639,
#60640),.UNSPECIFIED.,.F.,.F.,(4,1,1,1,1,1,1,1,1,1,1,1,1,1,4),(28.2743338823081,
28.4990230769123,28.9956110248268,29.4921989727414,29.9887869206559,30.4853748685704,
30.981962816485,31.4785507643995,31.975138712314,32.4717266602286,32.9683146081431,
33.4649025560576,33.9614905039722,34.4580784518867,34.5575191894877),
 .UNSPECIFIED.);
#703=B_SPLINE_CURVE_WITH_KNOTS('',3,(#60641,#60642,#60643,#60644,#60645,
#60646,#60647,#60648,#60649,#60650,#60651,#60652,#60653,#60654,#60655,#60656),
 .UNSPECIFIED.,.F.,.F.,(4,1,1,1,1,1,1,1,1,1,1,1,1,4),(28.274333882308,28.661235119122,
29.1578230670365,29.6544110149511,30.1509989628656,30.6475869107801,31.1441748586947,
31.6407628066092,32.1373507545237,32.6339387024382,33.1305266503528,33.6271145982673,
34.1237025461818,34.5575191894876),.UNSPECIFIED.);
#704=B_SPLINE_CURVE_WITH_KNOTS('',3,(#60661,#60662,#60663,#60664,#60665,
#60666,#60667,#60668,#60669,#60670,#60671,#60672,#60673,#60674,#60675,#60676,
#60677),.UNSPECIFIED.,.F.,.F.,(4,1,1,1,1,1,1,1,1,1,1,1,1,1,4),(21.9911485751285,
22.0433797540234,22.5399677019379,23.0365556498524,23.533143597767,24.0297315456815,
24.526319493596,25.0229074415106,25.5194953894251,26.0160833373396,26.5126712852542,
27.0092592331687,27.5058471810832,28.0024351289978,28.2743338823081),
 .UNSPECIFIED.);
#705=B_SPLINE_CURVE_WITH_KNOTS('',3,(#60678,#60679,#60680,#60681,#60682,
#60683,#60684,#60685,#60686,#60687,#60688,#60689,#60690,#60691,#60692,#60693,
#60694),.UNSPECIFIED.,.F.,.F.,(4,1,1,1,1,1,1,1,1,1,1,1,1,1,4),(21.9911485751285,
22.2055917962331,22.7021797441476,23.1987676920621,23.6953556399767,24.1919435878912,
24.6885315358057,25.1851194837203,25.6817074316348,26.1782953795493,26.6748833274639,
27.1714712753784,27.6680592232929,28.1646471712075,28.274333882308),
 .UNSPECIFIED.);
#706=B_SPLINE_CURVE_WITH_KNOTS('',3,(#60699,#60700,#60701,#60702,#60703,
#60704,#60705,#60706,#60707,#60708,#60709,#60710,#60711,#60712,#60713,#60714),
 .UNSPECIFIED.,.F.,.F.,(4,1,1,1,1,1,1,1,1,1,1,1,1,4),(15.7079632679489,
16.084324379049,16.5809123269635,17.077500274878,17.5740882227926,18.0706761707071,
18.5672641186216,19.0638520665362,19.5604400144507,20.0570279623652,20.5536159102798,
21.0502038581943,21.5467918061088,21.9911485751285),.UNSPECIFIED.);
#707=B_SPLINE_CURVE_WITH_KNOTS('',3,(#60715,#60716,#60717,#60718,#60719,
#60720,#60721,#60722,#60723,#60724,#60725,#60726,#60727,#60728,#60729,#60730,
#60731),.UNSPECIFIED.,.F.,.F.,(4,1,1,1,1,1,1,1,1,1,1,1,1,1,4),(15.7079632679489,
15.7499484733441,16.2465364212587,16.7431243691732,17.2397123170877,17.7363002650023,
18.2328882129168,18.7294761608313,19.2260641087459,19.7226520566604,20.2192400045749,
20.7158279524895,21.212415900404,21.7090038483185,21.9911485751285),
 .UNSPECIFIED.);
#708=B_SPLINE_CURVE_WITH_KNOTS('',3,(#61761,#61762,#61763,#61764,#61765,
#61766,#61767,#61768,#61769,#61770,#61771,#61772,#61773,#61774,#61775,#61776,
#61777,#61778,#61779,#61780,#61781,#61782,#61783,#61784,#61785,#61786,#61787,
#61788,#61789,#61790,#61791,#61792,#61793,#61794,#61795,#61796,#61797,#61798,
#61799,#61800,#61801,#61802,#61803,#61804,#61805,#61806,#61807,#61808,#61809,
#61810,#61811,#61812,#61813,#61814,#61815,#61816,#61817,#61818,#61819,#61820,
#61821,#61822,#61823,#61824,#61825,#61826,#61827,#61828,#61829,#61830,#61831,
#61832,#61833,#61834,#61835,#61836),.UNSPECIFIED.,.F.,.F.,(4,3,3,3,3,3,
3,3,3,3,3,3,3,3,3,3,3,3,3,3,3,3,3,3,3,4),(-1.52870610664534,-1.45875428118923,
-1.36271669471793,-1.32921490599004,-1.30256164282083,-1.18858278906243,
-1.14799636029883,-1.11926343500615,-1.09549660338738,-1.07460393530403,
-0.96768361724423,-0.861785228504725,-0.833450674047083,-0.811863192114468,
-0.703084143195483,-0.61351376138071,-0.562609972317118,-0.542202235390156,
-0.440214809144416,-0.344802615936392,-0.29702980114962,-0.270112033817159,
-0.247220523001207,-0.1471419036383,-0.0490185288914403,0.),
 .UNSPECIFIED.);
#709=B_SPLINE_CURVE_WITH_KNOTS('',3,(#61837,#61838,#61839,#61840,#61841,
#61842,#61843,#61844,#61845,#61846,#61847,#61848,#61849,#61850,#61851,#61852,
#61853,#61854,#61855,#61856,#61857,#61858,#61859,#61860,#61861),
 .UNSPECIFIED.,.F.,.F.,(4,3,3,3,3,3,3,3,4),(120.504169542555,120.670871343231,
121.167459291146,121.664047239061,122.160635186975,122.65722313489,123.153811082804,
123.650399030719,124.058352297607),.UNSPECIFIED.);
#710=B_SPLINE_CURVE_WITH_KNOTS('',3,(#61863,#61864,#61865,#61866,#61867,
#61868,#61869,#61870,#61871,#61872,#61873,#61874,#61875,#61876,#61877,#61878,
#61879,#61880,#61881,#61882,#61883,#61884,#61885,#61886,#61887,#61888,#61889,
#61890,#61891,#61892,#61893,#61894,#61895,#61896,#61897,#61898,#61899,#61900,
#61901,#61902,#61903,#61904,#61905,#61906,#61907,#61908,#61909,#61910,#61911,
#61912,#61913,#61914,#61915,#61916,#61917,#61918,#61919,#61920,#61921,#61922,
#61923,#61924,#61925,#61926,#61927,#61928,#61929,#61930,#61931,#61932,#61933,
#61934,#61935),.UNSPECIFIED.,.F.,.F.,(4,3,3,3,3,3,3,3,3,3,3,3,3,3,3,3,3,
3,3,3,3,3,3,3,4),(-1.5337369924875,-1.47310339793522,-1.38616089135255,
-1.35553579127592,-1.32729232344809,-1.22631284752631,-1.18227376682654,
-1.1511716128867,-1.12533337160453,-1.02273077361868,-0.95087425227154,
-0.895171890823101,-0.873398340368991,-0.763527429133733,-0.669727116015181,
-0.613941195435186,-0.58473597398091,-0.476777077099686,-0.388326176659527,
-0.338096679615524,-0.310206788241938,-0.28811604023779,-0.178935998268544,
-0.0688709899600637,0.),.UNSPECIFIED.);
#711=B_SPLINE_CURVE_WITH_KNOTS('',3,(#61936,#61937,#61938,#61939,#61940,
#61941,#61942,#61943,#61944,#61945,#61946,#61947,#61948,#61949),
 .UNSPECIFIED.,.F.,.F.,(4,1,1,1,1,1,1,1,1,1,1,4),(10.3761157273101,10.7840689941988,
11.2806569421133,11.7772448900279,12.2738328379424,12.7704207858569,13.2670087337715,
13.763596681686,14.2601846296005,14.7567725775151,15.2533605254296,15.7079632679489),
 .UNSPECIFIED.);
#712=B_SPLINE_CURVE_WITH_KNOTS('',3,(#61955,#61956,#61957,#61958,#61959,
#61960,#61961,#61962,#61963,#61964,#61965,#61966,#61967,#61968,#61969,#61970,
#61971,#61972,#61973,#61974,#61975,#61976,#61977,#61978,#61979,#61980,#61981,
#61982,#61983,#61984,#61985,#61986,#61987,#61988,#61989,#61990,#61991,#61992,
#61993,#61994,#61995,#61996,#61997,#61998,#61999,#62000,#62001,#62002,#62003,
#62004,#62005,#62006,#62007,#62008,#62009,#62010,#62011,#62012,#62013,#62014,
#62015,#62016,#62017,#62018,#62019,#62020,#62021,#62022,#62023,#62024,#62025,
#62026,#62027,#62028,#62029,#62030),.UNSPECIFIED.,.F.,.F.,(4,3,3,3,3,3,
3,3,3,3,3,3,3,3,3,3,3,3,3,3,3,3,3,3,3,4),(-1.52870610664514,-1.45875428118896,
-1.36271669471769,-1.32921490384452,-1.30256164016884,-1.18858278773635,
-1.1479963595685,-1.11926343453104,-1.09549660342904,-1.07460393530387,
-0.967683620479759,-0.861785252473329,-0.833450706753318,-0.811863217327338,
-0.70308414319544,-0.613513761380673,-0.562609973423642,-0.542202235080821,
-0.440214783048228,-0.344802615936372,-0.29702979072875,-0.270111989456298,
-0.247220519065303,-0.147141901650714,-0.0490185840864301,0.),
 .UNSPECIFIED.);
#713=B_SPLINE_CURVE_WITH_KNOTS('',3,(#62033,#62034,#62035,#62036,#62037,
#62038,#62039,#62040,#62041,#62042,#62043,#62044),.UNSPECIFIED.,.F.,.F.,
(4,1,1,1,1,1,1,1,1,4),(11.6150328478182,12.1116207957327,12.6082087436472,
13.1047966915618,13.6013846394763,14.0979725873908,14.5945605353054,15.0911484832199,
15.5877364311344,15.7079632679489),.UNSPECIFIED.);
#714=B_SPLINE_CURVE_WITH_KNOTS('',3,(#63074,#63075,#63076,#63077,#63078,
#63079,#63080,#63081,#63082,#63083,#63084,#63085,#63086,#63087,#63088,#63089,
#63090,#63091,#63092,#63093,#63094,#63095,#63096,#63097,#63098,#63099,#63100,
#63101,#63102,#63103,#63104,#63105,#63106,#63107,#63108,#63109,#63110,#63111,
#63112,#63113,#63114,#63115,#63116,#63117,#63118,#63119,#63120,#63121,#63122,
#63123,#63124,#63125,#63126,#63127,#63128,#63129,#63130,#63131,#63132,#63133,
#63134,#63135,#63136,#63137,#63138,#63139,#63140,#63141,#63142,#63143,#63144,
#63145,#63146),.UNSPECIFIED.,.F.,.F.,(4,3,3,3,3,3,3,3,3,3,3,3,3,3,3,3,3,
3,3,3,3,3,3,3,4),(-1.5337369924876,-1.47310339793536,-1.38616089135267,
-1.35553578686801,-1.32729232205323,-1.22631284682892,-1.18227376953103,
-1.15117161312205,-1.12533337160461,-1.02273077778506,-0.950874246236159,
-0.895171881876995,-0.873398336433576,-0.763527429133767,-0.669727116015206,
-0.613941186551684,-0.584735970127757,-0.476777077545073,-0.388326176659522,
-0.338096682547795,-0.310206794898333,-0.288116047041532,-0.178935969781343,
-0.0688709821527319,0.),.UNSPECIFIED.);
#715=B_SPLINE_CURVE_WITH_KNOTS('',3,(#63147,#63148,#63149,#63150,#63151,
#63152,#63153,#63154,#63155,#63156,#63157,#63158,#63159,#63160,#63161,#63162,
#63163,#63164,#63165),.UNSPECIFIED.,.F.,.F.,(4,3,3,3,3,3,4),(-126.133338770291,
-125.636750822377,-125.140162874462,-124.643574926548,-124.146986978633,
-123.650399030719,-123.473451256543),.UNSPECIFIED.);
#1013=SHAPE_REPRESENTATION_RELATIONSHIP('SRR','None',#76750,#1033);
#1033=ADVANCED_BREP_SHAPE_REPRESENTATION('',(#1073),#76654);
#1053=STYLED_ITEM('',(#76913),#1073);
#1073=MANIFOLD_SOLID_BREP('Hex screw',#26678);
#1359=CYLINDRICAL_SURFACE('',#28364,0.7911);
#1360=CYLINDRICAL_SURFACE('',#28366,0.7911);
#1361=CYLINDRICAL_SURFACE('',#28367,0.7911);
#1362=CYLINDRICAL_SURFACE('',#28368,0.7911);
#1363=CYLINDRICAL_SURFACE('',#28369,0.7911);
#1364=CYLINDRICAL_SURFACE('',#28370,0.7911);
#1365=CYLINDRICAL_SURFACE('',#28371,0.7911);
#1366=CYLINDRICAL_SURFACE('',#28372,0.7911);
#1367=CYLINDRICAL_SURFACE('',#28373,0.7911);
#1368=CYLINDRICAL_SURFACE('',#28374,0.7911);
#1369=CYLINDRICAL_SURFACE('',#28375,0.7911);
#1370=CYLINDRICAL_SURFACE('',#28376,0.7911);
#1371=CYLINDRICAL_SURFACE('',#28377,0.7911);
#1372=CYLINDRICAL_SURFACE('',#28378,0.7911);
#1373=CYLINDRICAL_SURFACE('',#28379,0.7911);
#1374=CYLINDRICAL_SURFACE('',#28380,0.7911);
#1375=CYLINDRICAL_SURFACE('',#28381,0.7911);
#1376=CYLINDRICAL_SURFACE('',#28382,0.7911);
#1377=CYLINDRICAL_SURFACE('',#28383,0.7911);
#1378=CYLINDRICAL_SURFACE('',#28384,0.7911);
#1379=CYLINDRICAL_SURFACE('',#28385,0.6767);
#1380=CYLINDRICAL_SURFACE('',#28387,0.6767);
#1381=CYLINDRICAL_SURFACE('',#28389,0.6767);
#1382=CYLINDRICAL_SURFACE('',#28390,0.6767);
#1383=CYLINDRICAL_SURFACE('',#28391,0.6767);
#1384=CYLINDRICAL_SURFACE('',#28392,0.6767);
#1385=CYLINDRICAL_SURFACE('',#28393,0.6767);
#1386=CYLINDRICAL_SURFACE('',#28394,0.6767);
#1387=CYLINDRICAL_SURFACE('',#28395,0.6767);
#1388=CYLINDRICAL_SURFACE('',#28396,0.6767);
#1389=CYLINDRICAL_SURFACE('',#28397,0.6767);
#1390=CYLINDRICAL_SURFACE('',#28398,0.6767);
#1391=CYLINDRICAL_SURFACE('',#28399,0.6767);
#1392=CYLINDRICAL_SURFACE('',#28400,0.6767);
#1393=CYLINDRICAL_SURFACE('',#28401,0.6767);
#1394=CYLINDRICAL_SURFACE('',#28402,0.6767);
#1395=CYLINDRICAL_SURFACE('',#28403,0.6767);
#1396=CYLINDRICAL_SURFACE('',#28404,0.6767);
#1397=CYLINDRICAL_SURFACE('',#28405,0.6767);
#1398=CYLINDRICAL_SURFACE('',#28406,0.6767);
#1399=CYLINDRICAL_SURFACE('',#28411,0.6767);
#1400=CYLINDRICAL_SURFACE('',#28426,0.7911);
#1401=CYLINDRICAL_SURFACE('',#28430,1.125);
#1640=FACE_BOUND('',#5142,.T.);
#1641=FACE_BOUND('',#5151,.T.);
#2148=PLANE('',#28407);
#2149=PLANE('',#28414);
#2150=PLANE('',#28415);
#2151=PLANE('',#28416);
#2152=PLANE('',#28417);
#2153=PLANE('',#28419);
#2154=PLANE('',#28420);
#2155=PLANE('',#28421);
#2156=PLANE('',#28422);
#2157=PLANE('',#28423);
#2158=PLANE('',#28428);
#3454=FACE_OUTER_BOUND('',#5093,.T.);
#3455=FACE_OUTER_BOUND('',#5094,.T.);
#3456=FACE_OUTER_BOUND('',#5095,.T.);
#3457=FACE_OUTER_BOUND('',#5096,.T.);
#3458=FACE_OUTER_BOUND('',#5097,.T.);
#3459=FACE_OUTER_BOUND('',#5098,.T.);
#3460=FACE_OUTER_BOUND('',#5099,.T.);
#3461=FACE_OUTER_BOUND('',#5100,.T.);
#3462=FACE_OUTER_BOUND('',#5101,.T.);
#3463=FACE_OUTER_BOUND('',#5102,.T.);
#3464=FACE_OUTER_BOUND('',#5103,.T.);
#3465=FACE_OUTER_BOUND('',#5104,.T.);
#3466=FACE_OUTER_BOUND('',#5105,.T.);
#3467=FACE_OUTER_BOUND('',#5106,.T.);
#3468=FACE_OUTER_BOUND('',#5107,.T.);
#3469=FACE_OUTER_BOUND('',#5108,.T.);
#3470=FACE_OUTER_BOUND('',#5109,.T.);
#3471=FACE_OUTER_BOUND('',#5110,.T.);
#3472=FACE_OUTER_BOUND('',#5111,.T.);
#3473=FACE_OUTER_BOUND('',#5112,.T.);
#3474=FACE_OUTER_BOUND('',#5113,.T.);
#3475=FACE_OUTER_BOUND('',#5114,.T.);
#3476=FACE_OUTER_BOUND('',#5115,.T.);
#3477=FACE_OUTER_BOUND('',#5116,.T.);
#3478=FACE_OUTER_BOUND('',#5117,.T.);
#3479=FACE_OUTER_BOUND('',#5118,.T.);
#3480=FACE_OUTER_BOUND('',#5119,.T.);
#3481=FACE_OUTER_BOUND('',#5120,.T.);
#3482=FACE_OUTER_BOUND('',#5121,.T.);
#3483=FACE_OUTER_BOUND('',#5122,.T.);
#3484=FACE_OUTER_BOUND('',#5123,.T.);
#3485=FACE_OUTER_BOUND('',#5124,.T.);
#3486=FACE_OUTER_BOUND('',#5125,.T.);
#3487=FACE_OUTER_BOUND('',#5126,.T.);
#3488=FACE_OUTER_BOUND('',#5127,.T.);
#3489=FACE_OUTER_BOUND('',#5128,.T.);
#3490=FACE_OUTER_BOUND('',#5129,.T.);
#3491=FACE_OUTER_BOUND('',#5130,.T.);
#3492=FACE_OUTER_BOUND('',#5131,.T.);
#3493=FACE_OUTER_BOUND('',#5132,.T.);
#3494=FACE_OUTER_BOUND('',#5133,.T.);
#3495=FACE_OUTER_BOUND('',#5134,.T.);
#3496=FACE_OUTER_BOUND('',#5135,.T.);
#3497=FACE_OUTER_BOUND('',#5136,.T.);
#3498=FACE_OUTER_BOUND('',#5137,.T.);
#3499=FACE_OUTER_BOUND('',#5138,.T.);
#3500=FACE_OUTER_BOUND('',#5139,.T.);
#3501=FACE_OUTER_BOUND('',#5140,.T.);
#3502=FACE_OUTER_BOUND('',#5141,.T.);
#3503=FACE_OUTER_BOUND('',#5143,.T.);
#3504=FACE_OUTER_BOUND('',#5144,.T.);
#3505=FACE_OUTER_BOUND('',#5145,.T.);
#3506=FACE_OUTER_BOUND('',#5146,.T.);
#3507=FACE_OUTER_BOUND('',#5147,.T.);
#3508=FACE_OUTER_BOUND('',#5148,.T.);
#3509=FACE_OUTER_BOUND('',#5149,.T.);
#3510=FACE_OUTER_BOUND('',#5150,.T.);
#3511=FACE_OUTER_BOUND('',#5152,.T.);
#5093=EDGE_LOOP('',(#21801,#21802,#21803,#21804));
#5094=EDGE_LOOP('',(#21805,#21806,#21807,#21808));
#5095=EDGE_LOOP('',(#21809,#21810,#21811,#21812));
#5096=EDGE_LOOP('',(#21813,#21814,#21815,#21816));
#5097=EDGE_LOOP('',(#21817,#21818,#21819,#21820));
#5098=EDGE_LOOP('',(#21821,#21822,#21823,#21824));
#5099=EDGE_LOOP('',(#21825,#21826,#21827,#21828));
#5100=EDGE_LOOP('',(#21829,#21830,#21831,#21832));
#5101=EDGE_LOOP('',(#21833,#21834,#21835,#21836));
#5102=EDGE_LOOP('',(#21837,#21838,#21839,#21840));
#5103=EDGE_LOOP('',(#21841,#21842,#21843,#21844));
#5104=EDGE_LOOP('',(#21845,#21846,#21847,#21848));
#5105=EDGE_LOOP('',(#21849,#21850,#21851,#21852));
#5106=EDGE_LOOP('',(#21853,#21854,#21855,#21856));
#5107=EDGE_LOOP('',(#21857,#21858,#21859,#21860));
#5108=EDGE_LOOP('',(#21861,#21862,#21863,#21864));
#5109=EDGE_LOOP('',(#21865,#21866,#21867,#21868));
#5110=EDGE_LOOP('',(#21869,#21870,#21871,#21872));
#5111=EDGE_LOOP('',(#21873,#21874,#21875,#21876));
#5112=EDGE_LOOP('',(#21877,#21878,#21879,#21880));
#5113=EDGE_LOOP('',(#21881,#21882,#21883));
#5114=EDGE_LOOP('',(#21884,#21885,#21886,#21887,#21888));
#5115=EDGE_LOOP('',(#21889,#21890,#21891,#21892));
#5116=EDGE_LOOP('',(#21893,#21894,#21895,#21896));
#5117=EDGE_LOOP('',(#21897,#21898,#21899,#21900));
#5118=EDGE_LOOP('',(#21901,#21902,#21903,#21904));
#5119=EDGE_LOOP('',(#21905,#21906,#21907,#21908));
#5120=EDGE_LOOP('',(#21909,#21910,#21911,#21912));
#5121=EDGE_LOOP('',(#21913,#21914,#21915,#21916));
#5122=EDGE_LOOP('',(#21917,#21918,#21919,#21920));
#5123=EDGE_LOOP('',(#21921,#21922,#21923,#21924));
#5124=EDGE_LOOP('',(#21925,#21926,#21927,#21928));
#5125=EDGE_LOOP('',(#21929,#21930,#21931,#21932));
#5126=EDGE_LOOP('',(#21933,#21934,#21935,#21936));
#5127=EDGE_LOOP('',(#21937,#21938,#21939,#21940));
#5128=EDGE_LOOP('',(#21941,#21942,#21943,#21944));
#5129=EDGE_LOOP('',(#21945,#21946,#21947,#21948));
#5130=EDGE_LOOP('',(#21949,#21950,#21951,#21952));
#5131=EDGE_LOOP('',(#21953,#21954,#21955,#21956));
#5132=EDGE_LOOP('',(#21957,#21958,#21959,#21960));
#5133=EDGE_LOOP('',(#21961,#21962,#21963,#21964,#21965,#21966,#21967,#21968,
#21969,#21970,#21971,#21972,#21973,#21974,#21975,#21976,#21977,#21978,#21979,
#21980,#21981,#21982,#21983,#21984,#21985,#21986,#21987,#21988,#21989,#21990,
#21991,#21992,#21993,#21994,#21995,#21996,#21997,#21998,#21999,#22000,#22001,
#22002,#22003));
#5134=EDGE_LOOP('',(#22004,#22005,#22006,#22007,#22008));
#5135=EDGE_LOOP('',(#22009,#22010,#22011,#22012));
#5136=EDGE_LOOP('',(#22013,#22014,#22015,#22016,#22017,#22018,#22019,#22020,
#22021,#22022,#22023,#22024,#22025,#22026,#22027,#22028,#22029,#22030,#22031,
#22032,#22033,#22034,#22035,#22036,#22037,#22038,#22039,#22040,#22041,#22042,
#22043,#22044,#22045,#22046,#22047,#22048,#22049,#22050,#22051,#22052,#22053,
#22054,#22055,#22056));
#5137=EDGE_LOOP('',(#22057,#22058,#22059,#22060,#22061,#22062,#22063,#22064,
#22065,#22066));
#5138=EDGE_LOOP('',(#22067,#22068,#22069,#22070));
#5139=EDGE_LOOP('',(#22071,#22072,#22073,#22074));
#5140=EDGE_LOOP('',(#22075,#22076,#22077,#22078));
#5141=EDGE_LOOP('',(#22079,#22080,#22081,#22082,#22083,#22084));
#5142=EDGE_LOOP('',(#22085));
#5143=EDGE_LOOP('',(#22086,#22087,#22088,#22089));
#5144=EDGE_LOOP('',(#22090,#22091,#22092,#22093));
#5145=EDGE_LOOP('',(#22094,#22095,#22096,#22097,#22098));
#5146=EDGE_LOOP('',(#22099));
#5147=EDGE_LOOP('',(#22100));
#5148=EDGE_LOOP('',(#22101,#22102,#22103,#22104,#22105,#22106));
#5149=EDGE_LOOP('',(#22107,#22108,#22109,#22110));
#5150=EDGE_LOOP('',(#22111));
#5151=EDGE_LOOP('',(#22112,#22113,#22114,#22115,#22116));
#5152=EDGE_LOOP('',(#22117,#22118,#22119,#22120));
#6258=CIRCLE('',#28365,0.7911);
#6259=CIRCLE('',#28386,0.6767);
#6260=CIRCLE('',#28388,0.6767);
#6261=CIRCLE('',#28408,0.7911);
#6262=CIRCLE('',#28409,0.7911);
#6263=CIRCLE('',#28410,0.6767);
#6264=CIRCLE('',#28413,1.14);
#6265=CIRCLE('',#28418,1.125);
#6266=CIRCLE('',#28424,0.74);
#6267=CIRCLE('',#28427,0.7911);
#6268=CIRCLE('',#28429,1.125);
#7904=LINE('',#58314,#10060);
#7905=LINE('',#58347,#10061);
#7906=LINE('',#58431,#10062);
#7907=LINE('',#58521,#10063);
#7908=LINE('',#58611,#10064);
#7909=LINE('',#58695,#10065);
#7910=LINE('',#58785,#10066);
#7911=LINE('',#58875,#10067);
#7912=LINE('',#58959,#10068);
#7913=LINE('',#59049,#10069);
#7914=LINE('',#59139,#10070);
#7915=LINE('',#59223,#10071);
#7916=LINE('',#59313,#10072);
#7917=LINE('',#59403,#10073);
#7918=LINE('',#59487,#10074);
#7919=LINE('',#59577,#10075);
#7920=LINE('',#59667,#10076);
#7921=LINE('',#59751,#10077);
#7922=LINE('',#59841,#10078);
#7923=LINE('',#59928,#10079);
#7924=LINE('',#60015,#10080);
#7925=LINE('',#60026,#10081);
#7926=LINE('',#60064,#10082);
#7927=LINE('',#60100,#10083);
#7928=LINE('',#60138,#10084);
#7929=LINE('',#60175,#10085);
#7930=LINE('',#60212,#10086);
#7931=LINE('',#60250,#10087);
#7932=LINE('',#60287,#10088);
#7933=LINE('',#60324,#10089);
#7934=LINE('',#60362,#10090);
#7935=LINE('',#60399,#10091);
#7936=LINE('',#60436,#10092);
#7937=LINE('',#60474,#10093);
#7938=LINE('',#60511,#10094);
#7939=LINE('',#60548,#10095);
#7940=LINE('',#60586,#10096);
#7941=LINE('',#60623,#10097);
#7942=LINE('',#60660,#10098);
#7943=LINE('',#60698,#10099);
#7944=LINE('',#63189,#10100);
#7945=LINE('',#63200,#10101);
#7946=LINE('',#63202,#10102);
#7947=LINE('',#63203,#10103);
#7948=LINE('',#63206,#10104);
#7949=LINE('',#63207,#10105);
#7950=LINE('',#63210,#10106);
#7951=LINE('',#63211,#10107);
#7952=LINE('',#63214,#10108);
#7953=LINE('',#63216,#10109);
#7954=LINE('',#63217,#10110);
#7955=LINE('',#63221,#10111);
#7956=LINE('',#63223,#10112);
#7957=LINE('',#63230,#10113);
#7958=LINE('',#63237,#10114);
#10060=VECTOR('',#33577,0.8);
#10061=VECTOR('',#33582,0.8);
#10062=VECTOR('',#33585,0.8);
#10063=VECTOR('',#33588,0.8);
#10064=VECTOR('',#33591,0.8);
#10065=VECTOR('',#33594,0.8);
#10066=VECTOR('',#33597,0.8);
#10067=VECTOR('',#33600,0.8);
#10068=VECTOR('',#33603,0.8);
#10069=VECTOR('',#33606,0.8);
#10070=VECTOR('',#33609,0.8);
#10071=VECTOR('',#33612,0.8);
#10072=VECTOR('',#33615,0.8);
#10073=VECTOR('',#33618,0.8);
#10074=VECTOR('',#33621,0.8);
#10075=VECTOR('',#33624,0.8);
#10076=VECTOR('',#33627,0.8);
#10077=VECTOR('',#33630,0.8);
#10078=VECTOR('',#33633,0.8);
#10079=VECTOR('',#33636,0.8);
#10080=VECTOR('',#33639,0.6767);
#10081=VECTOR('',#33644,0.6767);
#10082=VECTOR('',#33649,0.6767);
#10083=VECTOR('',#33652,0.6767);
#10084=VECTOR('',#33655,0.6767);
#10085=VECTOR('',#33658,0.6767);
#10086=VECTOR('',#33661,0.6767);
#10087=VECTOR('',#33664,0.6767);
#10088=VECTOR('',#33667,0.6767);
#10089=VECTOR('',#33670,0.6767);
#10090=VECTOR('',#33673,0.6767);
#10091=VECTOR('',#33676,0.6767);
#10092=VECTOR('',#33679,0.6767);
#10093=VECTOR('',#33682,0.6767);
#10094=VECTOR('',#33685,0.6767);
#10095=VECTOR('',#33688,0.6767);
#10096=VECTOR('',#33691,0.6767);
#10097=VECTOR('',#33694,0.6767);
#10098=VECTOR('',#33697,0.6767);
#10099=VECTOR('',#33700,0.6767);
#10100=VECTOR('',#33713,1.28782032302755);
#10101=VECTOR('',#33718,1.);
#10102=VECTOR('',#33719,1.);
#10103=VECTOR('',#33720,1.);
#10104=VECTOR('',#33723,1.);
#10105=VECTOR('',#33724,1.);
#10106=VECTOR('',#33727,1.);
#10107=VECTOR('',#33728,1.);
#10108=VECTOR('',#33731,1.);
#10109=VECTOR('',#33732,1.);
#10110=VECTOR('',#33733,1.);
#10111=VECTOR('',#33738,1.);
#10112=VECTOR('',#33741,1.);
#10113=VECTOR('',#33752,0.77);
#10114=VECTOR('',#33763,1.125);
#12351=VERTEX_POINT('',#58312);
#12352=VERTEX_POINT('',#58313);
#12353=VERTEX_POINT('',#58315);
#12354=VERTEX_POINT('',#58332);
#12355=VERTEX_POINT('',#58345);
#12356=VERTEX_POINT('',#58346);
#12357=VERTEX_POINT('',#58429);
#12358=VERTEX_POINT('',#58430);
#12359=VERTEX_POINT('',#58519);
#12360=VERTEX_POINT('',#58520);
#12361=VERTEX_POINT('',#58609);
#12362=VERTEX_POINT('',#58610);
#12363=VERTEX_POINT('',#58693);
#12364=VERTEX_POINT('',#58694);
#12365=VERTEX_POINT('',#58783);
#12366=VERTEX_POINT('',#58784);
#12367=VERTEX_POINT('',#58873);
#12368=VERTEX_POINT('',#58874);
#12369=VERTEX_POINT('',#58957);
#12370=VERTEX_POINT('',#58958);
#12371=VERTEX_POINT('',#59047);
#12372=VERTEX_POINT('',#59048);
#12373=VERTEX_POINT('',#59137);
#12374=VERTEX_POINT('',#59138);
#12375=VERTEX_POINT('',#59221);
#12376=VERTEX_POINT('',#59222);
#12377=VERTEX_POINT('',#59311);
#12378=VERTEX_POINT('',#59312);
#12379=VERTEX_POINT('',#59401);
#12380=VERTEX_POINT('',#59402);
#12381=VERTEX_POINT('',#59485);
#12382=VERTEX_POINT('',#59486);
#12383=VERTEX_POINT('',#59575);
#12384=VERTEX_POINT('',#59576);
#12385=VERTEX_POINT('',#59665);
#12386=VERTEX_POINT('',#59666);
#12387=VERTEX_POINT('',#59749);
#12388=VERTEX_POINT('',#59750);
#12389=VERTEX_POINT('',#59839);
#12390=VERTEX_POINT('',#59840);
#12391=VERTEX_POINT('',#59926);
#12392=VERTEX_POINT('',#59927);
#12393=VERTEX_POINT('',#60013);
#12394=VERTEX_POINT('',#60014);
#12395=VERTEX_POINT('',#60016);
#12396=VERTEX_POINT('',#60024);
#12397=VERTEX_POINT('',#60025);
#12398=VERTEX_POINT('',#60044);
#12399=VERTEX_POINT('',#60062);
#12400=VERTEX_POINT('',#60063);
#12401=VERTEX_POINT('',#60098);
#12402=VERTEX_POINT('',#60099);
#12403=VERTEX_POINT('',#60136);
#12404=VERTEX_POINT('',#60137);
#12405=VERTEX_POINT('',#60173);
#12406=VERTEX_POINT('',#60174);
#12407=VERTEX_POINT('',#60210);
#12408=VERTEX_POINT('',#60211);
#12409=VERTEX_POINT('',#60248);
#12410=VERTEX_POINT('',#60249);
#12411=VERTEX_POINT('',#60285);
#12412=VERTEX_POINT('',#60286);
#12413=VERTEX_POINT('',#60322);
#12414=VERTEX_POINT('',#60323);
#12415=VERTEX_POINT('',#60360);
#12416=VERTEX_POINT('',#60361);
#12417=VERTEX_POINT('',#60397);
#12418=VERTEX_POINT('',#60398);
#12419=VERTEX_POINT('',#60434);
#12420=VERTEX_POINT('',#60435);
#12421=VERTEX_POINT('',#60472);
#12422=VERTEX_POINT('',#60473);
#12423=VERTEX_POINT('',#60509);
#12424=VERTEX_POINT('',#60510);
#12425=VERTEX_POINT('',#60546);
#12426=VERTEX_POINT('',#60547);
#12427=VERTEX_POINT('',#60584);
#12428=VERTEX_POINT('',#60585);
#12429=VERTEX_POINT('',#60621);
#12430=VERTEX_POINT('',#60622);
#12431=VERTEX_POINT('',#60658);
#12432=VERTEX_POINT('',#60659);
#12433=VERTEX_POINT('',#60696);
#12434=VERTEX_POINT('',#60697);
#12435=VERTEX_POINT('',#61760);
#12436=VERTEX_POINT('',#61862);
#12437=VERTEX_POINT('',#61951);
#12438=VERTEX_POINT('',#61954);
#12439=VERTEX_POINT('',#63073);
#12440=VERTEX_POINT('',#63167);
#12441=VERTEX_POINT('',#63168);
#12442=VERTEX_POINT('',#63172);
#12443=VERTEX_POINT('',#63176);
#12444=VERTEX_POINT('',#63180);
#12445=VERTEX_POINT('',#63184);
#12446=VERTEX_POINT('',#63188);
#12447=VERTEX_POINT('',#63191);
#12448=VERTEX_POINT('',#63199);
#12449=VERTEX_POINT('',#63201);
#12450=VERTEX_POINT('',#63205);
#12451=VERTEX_POINT('',#63209);
#12452=VERTEX_POINT('',#63213);
#12453=VERTEX_POINT('',#63215);
#12454=VERTEX_POINT('',#63218);
#12455=VERTEX_POINT('',#63227);
#12456=VERTEX_POINT('',#63234);
#15623=EDGE_CURVE('',#12351,#12352,#7904,.T.);
#15624=EDGE_CURVE('',#12351,#12353,#629,.T.);
#15625=EDGE_CURVE('',#12353,#12354,#6258,.T.);
#15626=EDGE_CURVE('',#12354,#12352,#630,.T.);
#15627=EDGE_CURVE('',#12355,#12356,#7905,.T.);
#15628=EDGE_CURVE('',#12355,#12351,#631,.T.);
#15629=EDGE_CURVE('',#12352,#12356,#632,.T.);
#15630=EDGE_CURVE('',#12357,#12358,#7906,.T.);
#15631=EDGE_CURVE('',#12357,#12355,#633,.T.);
#15632=EDGE_CURVE('',#12356,#12358,#634,.T.);
#15633=EDGE_CURVE('',#12359,#12360,#7907,.T.);
#15634=EDGE_CURVE('',#12359,#12357,#635,.T.);
#15635=EDGE_CURVE('',#12358,#12360,#636,.T.);
#15636=EDGE_CURVE('',#12361,#12362,#7908,.T.);
#15637=EDGE_CURVE('',#12361,#12359,#637,.T.);
#15638=EDGE_CURVE('',#12360,#12362,#638,.T.);
#15639=EDGE_CURVE('',#12363,#12364,#7909,.T.);
#15640=EDGE_CURVE('',#12363,#12361,#639,.T.);
#15641=EDGE_CURVE('',#12362,#12364,#640,.T.);
#15642=EDGE_CURVE('',#12365,#12366,#7910,.T.);
#15643=EDGE_CURVE('',#12365,#12363,#641,.T.);
#15644=EDGE_CURVE('',#12364,#12366,#642,.T.);
#15645=EDGE_CURVE('',#12367,#12368,#7911,.T.);
#15646=EDGE_CURVE('',#12367,#12365,#643,.T.);
#15647=EDGE_CURVE('',#12366,#12368,#644,.T.);
#15648=EDGE_CURVE('',#12369,#12370,#7912,.T.);
#15649=EDGE_CURVE('',#12369,#12367,#645,.T.);
#15650=EDGE_CURVE('',#12368,#12370,#646,.T.);
#15651=EDGE_CURVE('',#12371,#12372,#7913,.T.);
#15652=EDGE_CURVE('',#12371,#12369,#647,.T.);
#15653=EDGE_CURVE('',#12370,#12372,#648,.T.);
#15654=EDGE_CURVE('',#12373,#12374,#7914,.T.);
#15655=EDGE_CURVE('',#12373,#12371,#649,.T.);
#15656=EDGE_CURVE('',#12372,#12374,#650,.T.);
#15657=EDGE_CURVE('',#12375,#12376,#7915,.T.);
#15658=EDGE_CURVE('',#12375,#12373,#651,.T.);
#15659=EDGE_CURVE('',#12374,#12376,#652,.T.);
#15660=EDGE_CURVE('',#12377,#12378,#7916,.T.);
#15661=EDGE_CURVE('',#12377,#12375,#653,.T.);
#15662=EDGE_CURVE('',#12376,#12378,#654,.T.);
#15663=EDGE_CURVE('',#12379,#12380,#7917,.T.);
#15664=EDGE_CURVE('',#12379,#12377,#655,.T.);
#15665=EDGE_CURVE('',#12378,#12380,#656,.T.);
#15666=EDGE_CURVE('',#12381,#12382,#7918,.T.);
#15667=EDGE_CURVE('',#12381,#12379,#657,.T.);
#15668=EDGE_CURVE('',#12380,#12382,#658,.T.);
#15669=EDGE_CURVE('',#12383,#12384,#7919,.T.);
#15670=EDGE_CURVE('',#12383,#12381,#659,.T.);
#15671=EDGE_CURVE('',#12382,#12384,#660,.T.);
#15672=EDGE_CURVE('',#12385,#12386,#7920,.T.);
#15673=EDGE_CURVE('',#12385,#12383,#661,.T.);
#15674=EDGE_CURVE('',#12384,#12386,#662,.T.);
#15675=EDGE_CURVE('',#12387,#12388,#7921,.T.);
#15676=EDGE_CURVE('',#12387,#12385,#663,.T.);
#15677=EDGE_CURVE('',#12386,#12388,#664,.T.);
#15678=EDGE_CURVE('',#12389,#12390,#7922,.T.);
#15679=EDGE_CURVE('',#12389,#12387,#665,.T.);
#15680=EDGE_CURVE('',#12388,#12390,#666,.T.);
#15681=EDGE_CURVE('',#12391,#12392,#7923,.T.);
#15682=EDGE_CURVE('',#12391,#12389,#667,.T.);
#15683=EDGE_CURVE('',#12390,#12392,#668,.T.);
#15684=EDGE_CURVE('',#12393,#12394,#7924,.T.);
#15685=EDGE_CURVE('',#12393,#12395,#669,.T.);
#15686=EDGE_CURVE('',#12394,#12395,#6259,.T.);
#15687=EDGE_CURVE('',#12396,#12397,#7925,.T.);
#15688=EDGE_CURVE('',#12396,#12393,#670,.T.);
#15689=EDGE_CURVE('',#12398,#12394,#6260,.T.);
#15690=EDGE_CURVE('',#12397,#12398,#671,.T.);
#15691=EDGE_CURVE('',#12399,#12400,#7926,.T.);
#15692=EDGE_CURVE('',#12399,#12396,#672,.T.);
#15693=EDGE_CURVE('',#12400,#12397,#673,.T.);
#15694=EDGE_CURVE('',#12401,#12402,#7927,.T.);
#15695=EDGE_CURVE('',#12401,#12399,#674,.T.);
#15696=EDGE_CURVE('',#12402,#12400,#675,.T.);
#15697=EDGE_CURVE('',#12403,#12404,#7928,.T.);
#15698=EDGE_CURVE('',#12403,#12401,#676,.T.);
#15699=EDGE_CURVE('',#12404,#12402,#677,.T.);
#15700=EDGE_CURVE('',#12405,#12406,#7929,.T.);
#15701=EDGE_CURVE('',#12405,#12403,#678,.T.);
#15702=EDGE_CURVE('',#12406,#12404,#679,.T.);
#15703=EDGE_CURVE('',#12407,#12408,#7930,.T.);
#15704=EDGE_CURVE('',#12407,#12405,#680,.T.);
#15705=EDGE_CURVE('',#12408,#12406,#681,.T.);
#15706=EDGE_CURVE('',#12409,#12410,#7931,.T.);
#15707=EDGE_CURVE('',#12409,#12407,#682,.T.);
#15708=EDGE_CURVE('',#12410,#12408,#683,.T.);
#15709=EDGE_CURVE('',#12411,#12412,#7932,.T.);
#15710=EDGE_CURVE('',#12411,#12409,#684,.T.);
#15711=EDGE_CURVE('',#12412,#12410,#685,.T.);
#15712=EDGE_CURVE('',#12413,#12414,#7933,.T.);
#15713=EDGE_CURVE('',#12413,#12411,#686,.T.);
#15714=EDGE_CURVE('',#12414,#12412,#687,.T.);
#15715=EDGE_CURVE('',#12415,#12416,#7934,.T.);
#15716=EDGE_CURVE('',#12415,#12413,#688,.T.);
#15717=EDGE_CURVE('',#12416,#12414,#689,.T.);
#15718=EDGE_CURVE('',#12417,#12418,#7935,.T.);
#15719=EDGE_CURVE('',#12417,#12415,#690,.T.);
#15720=EDGE_CURVE('',#12418,#12416,#691,.T.);
#15721=EDGE_CURVE('',#12419,#12420,#7936,.T.);
#15722=EDGE_CURVE('',#12419,#12417,#692,.T.);
#15723=EDGE_CURVE('',#12420,#12418,#693,.T.);
#15724=EDGE_CURVE('',#12421,#12422,#7937,.T.);
#15725=EDGE_CURVE('',#12421,#12419,#694,.T.);
#15726=EDGE_CURVE('',#12422,#12420,#695,.T.);
#15727=EDGE_CURVE('',#12423,#12424,#7938,.T.);
#15728=EDGE_CURVE('',#12423,#12421,#696,.T.);
#15729=EDGE_CURVE('',#12424,#12422,#697,.T.);
#15730=EDGE_CURVE('',#12425,#12426,#7939,.T.);
#15731=EDGE_CURVE('',#12425,#12423,#698,.T.);
#15732=EDGE_CURVE('',#12426,#12424,#699,.T.);
#15733=EDGE_CURVE('',#12427,#12428,#7940,.T.);
#15734=EDGE_CURVE('',#12427,#12425,#700,.T.);
#15735=EDGE_CURVE('',#12428,#12426,#701,.T.);
#15736=EDGE_CURVE('',#12429,#12430,#7941,.T.);
#15737=EDGE_CURVE('',#12429,#12427,#702,.T.);
#15738=EDGE_CURVE('',#12430,#12428,#703,.T.);
#15739=EDGE_CURVE('',#12431,#12432,#7942,.T.);
#15740=EDGE_CURVE('',#12431,#12429,#704,.T.);
#15741=EDGE_CURVE('',#12432,#12430,#705,.T.);
#15742=EDGE_CURVE('',#12433,#12434,#7943,.T.);
#15743=EDGE_CURVE('',#12433,#12431,#706,.T.);
#15744=EDGE_CURVE('',#12434,#12432,#707,.T.);
#15745=EDGE_CURVE('',#12435,#12398,#708,.T.);
#15746=EDGE_CURVE('',#12392,#12435,#709,.T.);
#15747=EDGE_CURVE('',#12436,#12354,#710,.T.);
#15748=EDGE_CURVE('',#12436,#12434,#711,.T.);
#15749=EDGE_CURVE('',#12354,#12437,#6261,.T.);
#15750=EDGE_CURVE('',#12437,#12353,#6262,.T.);
#15751=EDGE_CURVE('',#12353,#12438,#712,.T.);
#15752=EDGE_CURVE('',#12438,#12436,#6263,.T.);
#15753=EDGE_CURVE('',#12438,#12433,#713,.T.);
#15754=EDGE_CURVE('',#12395,#12439,#714,.T.);
#15755=EDGE_CURVE('',#12439,#12391,#715,.T.);
#15756=EDGE_CURVE('',#12440,#12441,#123,.T.);
#15757=EDGE_CURVE('',#12442,#12440,#124,.T.);
#15758=EDGE_CURVE('',#12443,#12442,#125,.T.);
#15759=EDGE_CURVE('',#12444,#12443,#126,.T.);
#15760=EDGE_CURVE('',#12445,#12444,#127,.T.);
#15761=EDGE_CURVE('',#12445,#12446,#7944,.T.);
#15762=EDGE_CURVE('',#12446,#12446,#6264,.T.);
#15763=EDGE_CURVE('',#12447,#12445,#128,.T.);
#15764=EDGE_CURVE('',#12441,#12447,#129,.T.);
#15765=EDGE_CURVE('',#12448,#12443,#7945,.T.);
#15766=EDGE_CURVE('',#12448,#12449,#7946,.T.);
#15767=EDGE_CURVE('',#12449,#12444,#7947,.T.);
#15768=EDGE_CURVE('',#12450,#12442,#7948,.T.);
#15769=EDGE_CURVE('',#12450,#12448,#7949,.T.);
#15770=EDGE_CURVE('',#12451,#12440,#7950,.T.);
#15771=EDGE_CURVE('',#12451,#12450,#7951,.T.);
#15772=EDGE_CURVE('',#12452,#12451,#7952,.T.);
#15773=EDGE_CURVE('',#12453,#12452,#7953,.T.);
#15774=EDGE_CURVE('',#12449,#12453,#7954,.T.);
#15775=EDGE_CURVE('',#12454,#12454,#6265,.T.);
#15776=EDGE_CURVE('',#12452,#12441,#7955,.T.);
#15777=EDGE_CURVE('',#12453,#12447,#7956,.T.);
#15778=EDGE_CURVE('',#12455,#12455,#6266,.T.);
#15779=EDGE_CURVE('',#12437,#12455,#7957,.T.);
#15780=EDGE_CURVE('',#12439,#12435,#6267,.T.);
#15781=EDGE_CURVE('',#12456,#12456,#6268,.T.);
#15782=EDGE_CURVE('',#12454,#12456,#7958,.T.);
#21801=ORIENTED_EDGE('',*,*,#15623,.F.);
#21802=ORIENTED_EDGE('',*,*,#15624,.T.);
#21803=ORIENTED_EDGE('',*,*,#15625,.T.);
#21804=ORIENTED_EDGE('',*,*,#15626,.T.);
#21805=ORIENTED_EDGE('',*,*,#15627,.F.);
#21806=ORIENTED_EDGE('',*,*,#15628,.T.);
#21807=ORIENTED_EDGE('',*,*,#15623,.T.);
#21808=ORIENTED_EDGE('',*,*,#15629,.T.);
#21809=ORIENTED_EDGE('',*,*,#15630,.F.);
#21810=ORIENTED_EDGE('',*,*,#15631,.T.);
#21811=ORIENTED_EDGE('',*,*,#15627,.T.);
#21812=ORIENTED_EDGE('',*,*,#15632,.T.);
#21813=ORIENTED_EDGE('',*,*,#15633,.F.);
#21814=ORIENTED_EDGE('',*,*,#15634,.T.);
#21815=ORIENTED_EDGE('',*,*,#15630,.T.);
#21816=ORIENTED_EDGE('',*,*,#15635,.T.);
#21817=ORIENTED_EDGE('',*,*,#15636,.F.);
#21818=ORIENTED_EDGE('',*,*,#15637,.T.);
#21819=ORIENTED_EDGE('',*,*,#15633,.T.);
#21820=ORIENTED_EDGE('',*,*,#15638,.T.);
#21821=ORIENTED_EDGE('',*,*,#15639,.F.);
#21822=ORIENTED_EDGE('',*,*,#15640,.T.);
#21823=ORIENTED_EDGE('',*,*,#15636,.T.);
#21824=ORIENTED_EDGE('',*,*,#15641,.T.);
#21825=ORIENTED_EDGE('',*,*,#15642,.F.);
#21826=ORIENTED_EDGE('',*,*,#15643,.T.);
#21827=ORIENTED_EDGE('',*,*,#15639,.T.);
#21828=ORIENTED_EDGE('',*,*,#15644,.T.);
#21829=ORIENTED_EDGE('',*,*,#15645,.F.);
#21830=ORIENTED_EDGE('',*,*,#15646,.T.);
#21831=ORIENTED_EDGE('',*,*,#15642,.T.);
#21832=ORIENTED_EDGE('',*,*,#15647,.T.);
#21833=ORIENTED_EDGE('',*,*,#15648,.F.);
#21834=ORIENTED_EDGE('',*,*,#15649,.T.);
#21835=ORIENTED_EDGE('',*,*,#15645,.T.);
#21836=ORIENTED_EDGE('',*,*,#15650,.T.);
#21837=ORIENTED_EDGE('',*,*,#15651,.F.);
#21838=ORIENTED_EDGE('',*,*,#15652,.T.);
#21839=ORIENTED_EDGE('',*,*,#15648,.T.);
#21840=ORIENTED_EDGE('',*,*,#15653,.T.);
#21841=ORIENTED_EDGE('',*,*,#15654,.F.);
#21842=ORIENTED_EDGE('',*,*,#15655,.T.);
#21843=ORIENTED_EDGE('',*,*,#15651,.T.);
#21844=ORIENTED_EDGE('',*,*,#15656,.T.);
#21845=ORIENTED_EDGE('',*,*,#15657,.F.);
#21846=ORIENTED_EDGE('',*,*,#15658,.T.);
#21847=ORIENTED_EDGE('',*,*,#15654,.T.);
#21848=ORIENTED_EDGE('',*,*,#15659,.T.);
#21849=ORIENTED_EDGE('',*,*,#15660,.F.);
#21850=ORIENTED_EDGE('',*,*,#15661,.T.);
#21851=ORIENTED_EDGE('',*,*,#15657,.T.);
#21852=ORIENTED_EDGE('',*,*,#15662,.T.);
#21853=ORIENTED_EDGE('',*,*,#15663,.F.);
#21854=ORIENTED_EDGE('',*,*,#15664,.T.);
#21855=ORIENTED_EDGE('',*,*,#15660,.T.);
#21856=ORIENTED_EDGE('',*,*,#15665,.T.);
#21857=ORIENTED_EDGE('',*,*,#15666,.F.);
#21858=ORIENTED_EDGE('',*,*,#15667,.T.);
#21859=ORIENTED_EDGE('',*,*,#15663,.T.);
#21860=ORIENTED_EDGE('',*,*,#15668,.T.);
#21861=ORIENTED_EDGE('',*,*,#15669,.F.);
#21862=ORIENTED_EDGE('',*,*,#15670,.T.);
#21863=ORIENTED_EDGE('',*,*,#15666,.T.);
#21864=ORIENTED_EDGE('',*,*,#15671,.T.);
#21865=ORIENTED_EDGE('',*,*,#15672,.F.);
#21866=ORIENTED_EDGE('',*,*,#15673,.T.);
#21867=ORIENTED_EDGE('',*,*,#15669,.T.);
#21868=ORIENTED_EDGE('',*,*,#15674,.T.);
#21869=ORIENTED_EDGE('',*,*,#15675,.F.);
#21870=ORIENTED_EDGE('',*,*,#15676,.T.);
#21871=ORIENTED_EDGE('',*,*,#15672,.T.);
#21872=ORIENTED_EDGE('',*,*,#15677,.T.);
#21873=ORIENTED_EDGE('',*,*,#15678,.F.);
#21874=ORIENTED_EDGE('',*,*,#15679,.T.);
#21875=ORIENTED_EDGE('',*,*,#15675,.T.);
#21876=ORIENTED_EDGE('',*,*,#15680,.T.);
#21877=ORIENTED_EDGE('',*,*,#15681,.F.);
#21878=ORIENTED_EDGE('',*,*,#15682,.T.);
#21879=ORIENTED_EDGE('',*,*,#15678,.T.);
#21880=ORIENTED_EDGE('',*,*,#15683,.T.);
#21881=ORIENTED_EDGE('',*,*,#15684,.F.);
#21882=ORIENTED_EDGE('',*,*,#15685,.T.);
#21883=ORIENTED_EDGE('',*,*,#15686,.F.);
#21884=ORIENTED_EDGE('',*,*,#15687,.F.);
#21885=ORIENTED_EDGE('',*,*,#15688,.T.);
#21886=ORIENTED_EDGE('',*,*,#15684,.T.);
#21887=ORIENTED_EDGE('',*,*,#15689,.F.);
#21888=ORIENTED_EDGE('',*,*,#15690,.F.);
#21889=ORIENTED_EDGE('',*,*,#15691,.F.);
#21890=ORIENTED_EDGE('',*,*,#15692,.T.);
#21891=ORIENTED_EDGE('',*,*,#15687,.T.);
#21892=ORIENTED_EDGE('',*,*,#15693,.F.);
#21893=ORIENTED_EDGE('',*,*,#15694,.F.);
#21894=ORIENTED_EDGE('',*,*,#15695,.T.);
#21895=ORIENTED_EDGE('',*,*,#15691,.T.);
#21896=ORIENTED_EDGE('',*,*,#15696,.F.);
#21897=ORIENTED_EDGE('',*,*,#15697,.F.);
#21898=ORIENTED_EDGE('',*,*,#15698,.T.);
#21899=ORIENTED_EDGE('',*,*,#15694,.T.);
#21900=ORIENTED_EDGE('',*,*,#15699,.F.);
#21901=ORIENTED_EDGE('',*,*,#15700,.F.);
#21902=ORIENTED_EDGE('',*,*,#15701,.T.);
#21903=ORIENTED_EDGE('',*,*,#15697,.T.);
#21904=ORIENTED_EDGE('',*,*,#15702,.F.);
#21905=ORIENTED_EDGE('',*,*,#15703,.F.);
#21906=ORIENTED_EDGE('',*,*,#15704,.T.);
#21907=ORIENTED_EDGE('',*,*,#15700,.T.);
#21908=ORIENTED_EDGE('',*,*,#15705,.F.);
#21909=ORIENTED_EDGE('',*,*,#15706,.F.);
#21910=ORIENTED_EDGE('',*,*,#15707,.T.);
#21911=ORIENTED_EDGE('',*,*,#15703,.T.);
#21912=ORIENTED_EDGE('',*,*,#15708,.F.);
#21913=ORIENTED_EDGE('',*,*,#15709,.F.);
#21914=ORIENTED_EDGE('',*,*,#15710,.T.);
#21915=ORIENTED_EDGE('',*,*,#15706,.T.);
#21916=ORIENTED_EDGE('',*,*,#15711,.F.);
#21917=ORIENTED_EDGE('',*,*,#15712,.F.);
#21918=ORIENTED_EDGE('',*,*,#15713,.T.);
#21919=ORIENTED_EDGE('',*,*,#15709,.T.);
#21920=ORIENTED_EDGE('',*,*,#15714,.F.);
#21921=ORIENTED_EDGE('',*,*,#15715,.F.);
#21922=ORIENTED_EDGE('',*,*,#15716,.T.);
#21923=ORIENTED_EDGE('',*,*,#15712,.T.);
#21924=ORIENTED_EDGE('',*,*,#15717,.F.);
#21925=ORIENTED_EDGE('',*,*,#15718,.F.);
#21926=ORIENTED_EDGE('',*,*,#15719,.T.);
#21927=ORIENTED_EDGE('',*,*,#15715,.T.);
#21928=ORIENTED_EDGE('',*,*,#15720,.F.);
#21929=ORIENTED_EDGE('',*,*,#15721,.F.);
#21930=ORIENTED_EDGE('',*,*,#15722,.T.);
#21931=ORIENTED_EDGE('',*,*,#15718,.T.);
#21932=ORIENTED_EDGE('',*,*,#15723,.F.);
#21933=ORIENTED_EDGE('',*,*,#15724,.F.);
#21934=ORIENTED_EDGE('',*,*,#15725,.T.);
#21935=ORIENTED_EDGE('',*,*,#15721,.T.);
#21936=ORIENTED_EDGE('',*,*,#15726,.F.);
#21937=ORIENTED_EDGE('',*,*,#15727,.F.);
#21938=ORIENTED_EDGE('',*,*,#15728,.T.);
#21939=ORIENTED_EDGE('',*,*,#15724,.T.);
#21940=ORIENTED_EDGE('',*,*,#15729,.F.);
#21941=ORIENTED_EDGE('',*,*,#15730,.F.);
#21942=ORIENTED_EDGE('',*,*,#15731,.T.);
#21943=ORIENTED_EDGE('',*,*,#15727,.T.);
#21944=ORIENTED_EDGE('',*,*,#15732,.F.);
#21945=ORIENTED_EDGE('',*,*,#15733,.F.);
#21946=ORIENTED_EDGE('',*,*,#15734,.T.);
#21947=ORIENTED_EDGE('',*,*,#15730,.T.);
#21948=ORIENTED_EDGE('',*,*,#15735,.F.);
#21949=ORIENTED_EDGE('',*,*,#15736,.F.);
#21950=ORIENTED_EDGE('',*,*,#15737,.T.);
#21951=ORIENTED_EDGE('',*,*,#15733,.T.);
#21952=ORIENTED_EDGE('',*,*,#15738,.F.);
#21953=ORIENTED_EDGE('',*,*,#15739,.F.);
#21954=ORIENTED_EDGE('',*,*,#15740,.T.);
#21955=ORIENTED_EDGE('',*,*,#15736,.T.);
#21956=ORIENTED_EDGE('',*,*,#15741,.F.);
#21957=ORIENTED_EDGE('',*,*,#15742,.F.);
#21958=ORIENTED_EDGE('',*,*,#15743,.T.);
#21959=ORIENTED_EDGE('',*,*,#15739,.T.);
#21960=ORIENTED_EDGE('',*,*,#15744,.F.);
#21961=ORIENTED_EDGE('',*,*,#15745,.F.);
#21962=ORIENTED_EDGE('',*,*,#15746,.F.);
#21963=ORIENTED_EDGE('',*,*,#15683,.F.);
#21964=ORIENTED_EDGE('',*,*,#15680,.F.);
#21965=ORIENTED_EDGE('',*,*,#15677,.F.);
#21966=ORIENTED_EDGE('',*,*,#15674,.F.);
#21967=ORIENTED_EDGE('',*,*,#15671,.F.);
#21968=ORIENTED_EDGE('',*,*,#15668,.F.);
#21969=ORIENTED_EDGE('',*,*,#15665,.F.);
#21970=ORIENTED_EDGE('',*,*,#15662,.F.);
#21971=ORIENTED_EDGE('',*,*,#15659,.F.);
#21972=ORIENTED_EDGE('',*,*,#15656,.F.);
#21973=ORIENTED_EDGE('',*,*,#15653,.F.);
#21974=ORIENTED_EDGE('',*,*,#15650,.F.);
#21975=ORIENTED_EDGE('',*,*,#15647,.F.);
#21976=ORIENTED_EDGE('',*,*,#15644,.F.);
#21977=ORIENTED_EDGE('',*,*,#15641,.F.);
#21978=ORIENTED_EDGE('',*,*,#15638,.F.);
#21979=ORIENTED_EDGE('',*,*,#15635,.F.);
#21980=ORIENTED_EDGE('',*,*,#15632,.F.);
#21981=ORIENTED_EDGE('',*,*,#15629,.F.);
#21982=ORIENTED_EDGE('',*,*,#15626,.F.);
#21983=ORIENTED_EDGE('',*,*,#15747,.F.);
#21984=ORIENTED_EDGE('',*,*,#15748,.T.);
#21985=ORIENTED_EDGE('',*,*,#15744,.T.);
#21986=ORIENTED_EDGE('',*,*,#15741,.T.);
#21987=ORIENTED_EDGE('',*,*,#15738,.T.);
#21988=ORIENTED_EDGE('',*,*,#15735,.T.);
#21989=ORIENTED_EDGE('',*,*,#15732,.T.);
#21990=ORIENTED_EDGE('',*,*,#15729,.T.);
#21991=ORIENTED_EDGE('',*,*,#15726,.T.);
#21992=ORIENTED_EDGE('',*,*,#15723,.T.);
#21993=ORIENTED_EDGE('',*,*,#15720,.T.);
#21994=ORIENTED_EDGE('',*,*,#15717,.T.);
#21995=ORIENTED_EDGE('',*,*,#15714,.T.);
#21996=ORIENTED_EDGE('',*,*,#15711,.T.);
#21997=ORIENTED_EDGE('',*,*,#15708,.T.);
#21998=ORIENTED_EDGE('',*,*,#15705,.T.);
#21999=ORIENTED_EDGE('',*,*,#15702,.T.);
#22000=ORIENTED_EDGE('',*,*,#15699,.T.);
#22001=ORIENTED_EDGE('',*,*,#15696,.T.);
#22002=ORIENTED_EDGE('',*,*,#15693,.T.);
#22003=ORIENTED_EDGE('',*,*,#15690,.T.);
#22004=ORIENTED_EDGE('',*,*,#15749,.T.);
#22005=ORIENTED_EDGE('',*,*,#15750,.T.);
#22006=ORIENTED_EDGE('',*,*,#15751,.T.);
#22007=ORIENTED_EDGE('',*,*,#15752,.T.);
#22008=ORIENTED_EDGE('',*,*,#15747,.T.);
#22009=ORIENTED_EDGE('',*,*,#15742,.T.);
#22010=ORIENTED_EDGE('',*,*,#15748,.F.);
#22011=ORIENTED_EDGE('',*,*,#15752,.F.);
#22012=ORIENTED_EDGE('',*,*,#15753,.T.);
#22013=ORIENTED_EDGE('',*,*,#15754,.F.);
#22014=ORIENTED_EDGE('',*,*,#15685,.F.);
#22015=ORIENTED_EDGE('',*,*,#15688,.F.);
#22016=ORIENTED_EDGE('',*,*,#15692,.F.);
#22017=ORIENTED_EDGE('',*,*,#15695,.F.);
#22018=ORIENTED_EDGE('',*,*,#15698,.F.);
#22019=ORIENTED_EDGE('',*,*,#15701,.F.);
#22020=ORIENTED_EDGE('',*,*,#15704,.F.);
#22021=ORIENTED_EDGE('',*,*,#15707,.F.);
#22022=ORIENTED_EDGE('',*,*,#15710,.F.);
#22023=ORIENTED_EDGE('',*,*,#15713,.F.);
#22024=ORIENTED_EDGE('',*,*,#15716,.F.);
#22025=ORIENTED_EDGE('',*,*,#15719,.F.);
#22026=ORIENTED_EDGE('',*,*,#15722,.F.);
#22027=ORIENTED_EDGE('',*,*,#15725,.F.);
#22028=ORIENTED_EDGE('',*,*,#15728,.F.);
#22029=ORIENTED_EDGE('',*,*,#15731,.F.);
#22030=ORIENTED_EDGE('',*,*,#15734,.F.);
#22031=ORIENTED_EDGE('',*,*,#15737,.F.);
#22032=ORIENTED_EDGE('',*,*,#15740,.F.);
#22033=ORIENTED_EDGE('',*,*,#15743,.F.);
#22034=ORIENTED_EDGE('',*,*,#15753,.F.);
#22035=ORIENTED_EDGE('',*,*,#15751,.F.);
#22036=ORIENTED_EDGE('',*,*,#15624,.F.);
#22037=ORIENTED_EDGE('',*,*,#15628,.F.);
#22038=ORIENTED_EDGE('',*,*,#15631,.F.);
#22039=ORIENTED_EDGE('',*,*,#15634,.F.);
#22040=ORIENTED_EDGE('',*,*,#15637,.F.);
#22041=ORIENTED_EDGE('',*,*,#15640,.F.);
#22042=ORIENTED_EDGE('',*,*,#15643,.F.);
#22043=ORIENTED_EDGE('',*,*,#15646,.F.);
#22044=ORIENTED_EDGE('',*,*,#15649,.F.);
#22045=ORIENTED_EDGE('',*,*,#15652,.F.);
#22046=ORIENTED_EDGE('',*,*,#15655,.F.);
#22047=ORIENTED_EDGE('',*,*,#15658,.F.);
#22048=ORIENTED_EDGE('',*,*,#15661,.F.);
#22049=ORIENTED_EDGE('',*,*,#15664,.F.);
#22050=ORIENTED_EDGE('',*,*,#15667,.F.);
#22051=ORIENTED_EDGE('',*,*,#15670,.F.);
#22052=ORIENTED_EDGE('',*,*,#15673,.F.);
#22053=ORIENTED_EDGE('',*,*,#15676,.F.);
#22054=ORIENTED_EDGE('',*,*,#15679,.F.);
#22055=ORIENTED_EDGE('',*,*,#15682,.F.);
#22056=ORIENTED_EDGE('',*,*,#15755,.F.);
#22057=ORIENTED_EDGE('',*,*,#15756,.F.);
#22058=ORIENTED_EDGE('',*,*,#15757,.F.);
#22059=ORIENTED_EDGE('',*,*,#15758,.F.);
#22060=ORIENTED_EDGE('',*,*,#15759,.F.);
#22061=ORIENTED_EDGE('',*,*,#15760,.F.);
#22062=ORIENTED_EDGE('',*,*,#15761,.T.);
#22063=ORIENTED_EDGE('',*,*,#15762,.F.);
#22064=ORIENTED_EDGE('',*,*,#15761,.F.);
#22065=ORIENTED_EDGE('',*,*,#15763,.F.);
#22066=ORIENTED_EDGE('',*,*,#15764,.F.);
#22067=ORIENTED_EDGE('',*,*,#15759,.T.);
#22068=ORIENTED_EDGE('',*,*,#15765,.F.);
#22069=ORIENTED_EDGE('',*,*,#15766,.T.);
#22070=ORIENTED_EDGE('',*,*,#15767,.T.);
#22071=ORIENTED_EDGE('',*,*,#15758,.T.);
#22072=ORIENTED_EDGE('',*,*,#15768,.F.);
#22073=ORIENTED_EDGE('',*,*,#15769,.T.);
#22074=ORIENTED_EDGE('',*,*,#15765,.T.);
#22075=ORIENTED_EDGE('',*,*,#15757,.T.);
#22076=ORIENTED_EDGE('',*,*,#15770,.F.);
#22077=ORIENTED_EDGE('',*,*,#15771,.T.);
#22078=ORIENTED_EDGE('',*,*,#15768,.T.);
#22079=ORIENTED_EDGE('',*,*,#15771,.F.);
#22080=ORIENTED_EDGE('',*,*,#15772,.F.);
#22081=ORIENTED_EDGE('',*,*,#15773,.F.);
#22082=ORIENTED_EDGE('',*,*,#15774,.F.);
#22083=ORIENTED_EDGE('',*,*,#15766,.F.);
#22084=ORIENTED_EDGE('',*,*,#15769,.F.);
#22085=ORIENTED_EDGE('',*,*,#15775,.T.);
#22086=ORIENTED_EDGE('',*,*,#15756,.T.);
#22087=ORIENTED_EDGE('',*,*,#15776,.F.);
#22088=ORIENTED_EDGE('',*,*,#15772,.T.);
#22089=ORIENTED_EDGE('',*,*,#15770,.T.);
#22090=ORIENTED_EDGE('',*,*,#15764,.T.);
#22091=ORIENTED_EDGE('',*,*,#15777,.F.);
#22092=ORIENTED_EDGE('',*,*,#15773,.T.);
#22093=ORIENTED_EDGE('',*,*,#15776,.T.);
#22094=ORIENTED_EDGE('',*,*,#15763,.T.);
#22095=ORIENTED_EDGE('',*,*,#15760,.T.);
#22096=ORIENTED_EDGE('',*,*,#15767,.F.);
#22097=ORIENTED_EDGE('',*,*,#15774,.T.);
#22098=ORIENTED_EDGE('',*,*,#15777,.T.);
#22099=ORIENTED_EDGE('',*,*,#15762,.T.);
#22100=ORIENTED_EDGE('',*,*,#15778,.F.);
#22101=ORIENTED_EDGE('',*,*,#15749,.F.);
#22102=ORIENTED_EDGE('',*,*,#15625,.F.);
#22103=ORIENTED_EDGE('',*,*,#15750,.F.);
#22104=ORIENTED_EDGE('',*,*,#15779,.T.);
#22105=ORIENTED_EDGE('',*,*,#15778,.T.);
#22106=ORIENTED_EDGE('',*,*,#15779,.F.);
#22107=ORIENTED_EDGE('',*,*,#15681,.T.);
#22108=ORIENTED_EDGE('',*,*,#15746,.T.);
#22109=ORIENTED_EDGE('',*,*,#15780,.F.);
#22110=ORIENTED_EDGE('',*,*,#15755,.T.);
#22111=ORIENTED_EDGE('',*,*,#15781,.F.);
#22112=ORIENTED_EDGE('',*,*,#15780,.T.);
#22113=ORIENTED_EDGE('',*,*,#15745,.T.);
#22114=ORIENTED_EDGE('',*,*,#15689,.T.);
#22115=ORIENTED_EDGE('',*,*,#15686,.T.);
#22116=ORIENTED_EDGE('',*,*,#15754,.T.);
#22117=ORIENTED_EDGE('',*,*,#15775,.F.);
#22118=ORIENTED_EDGE('',*,*,#15782,.T.);
#22119=ORIENTED_EDGE('',*,*,#15781,.T.);
#22120=ORIENTED_EDGE('',*,*,#15782,.F.);
#25070=CONICAL_SURFACE('',#28412,1.28782032302755,1.0471975511966);
#25071=CONICAL_SURFACE('',#28425,0.77,0.785398163397448);
#26042=ADVANCED_FACE('',(#3454),#1359,.T.);
#26043=ADVANCED_FACE('',(#3455),#1360,.T.);
#26044=ADVANCED_FACE('',(#3456),#1361,.T.);
#26045=ADVANCED_FACE('',(#3457),#1362,.T.);
#26046=ADVANCED_FACE('',(#3458),#1363,.T.);
#26047=ADVANCED_FACE('',(#3459),#1364,.T.);
#26048=ADVANCED_FACE('',(#3460),#1365,.T.);
#26049=ADVANCED_FACE('',(#3461),#1366,.T.);
#26050=ADVANCED_FACE('',(#3462),#1367,.T.);
#26051=ADVANCED_FACE('',(#3463),#1368,.T.);
#26052=ADVANCED_FACE('',(#3464),#1369,.T.);
#26053=ADVANCED_FACE('',(#3465),#1370,.T.);
#26054=ADVANCED_FACE('',(#3466),#1371,.T.);
#26055=ADVANCED_FACE('',(#3467),#1372,.T.);
#26056=ADVANCED_FACE('',(#3468),#1373,.T.);
#26057=ADVANCED_FACE('',(#3469),#1374,.T.);
#26058=ADVANCED_FACE('',(#3470),#1375,.T.);
#26059=ADVANCED_FACE('',(#3471),#1376,.T.);
#26060=ADVANCED_FACE('',(#3472),#1377,.T.);
#26061=ADVANCED_FACE('',(#3473),#1378,.T.);
#26062=ADVANCED_FACE('',(#3474),#1379,.T.);
#26063=ADVANCED_FACE('',(#3475),#1380,.T.);
#26064=ADVANCED_FACE('',(#3476),#1381,.T.);
#26065=ADVANCED_FACE('',(#3477),#1382,.T.);
#26066=ADVANCED_FACE('',(#3478),#1383,.T.);
#26067=ADVANCED_FACE('',(#3479),#1384,.T.);
#26068=ADVANCED_FACE('',(#3480),#1385,.T.);
#26069=ADVANCED_FACE('',(#3481),#1386,.T.);
#26070=ADVANCED_FACE('',(#3482),#1387,.T.);
#26071=ADVANCED_FACE('',(#3483),#1388,.T.);
#26072=ADVANCED_FACE('',(#3484),#1389,.T.);
#26073=ADVANCED_FACE('',(#3485),#1390,.T.);
#26074=ADVANCED_FACE('',(#3486),#1391,.T.);
#26075=ADVANCED_FACE('',(#3487),#1392,.T.);
#26076=ADVANCED_FACE('',(#3488),#1393,.T.);
#26077=ADVANCED_FACE('',(#3489),#1394,.T.);
#26078=ADVANCED_FACE('',(#3490),#1395,.T.);
#26079=ADVANCED_FACE('',(#3491),#1396,.T.);
#26080=ADVANCED_FACE('',(#3492),#1397,.T.);
#26081=ADVANCED_FACE('',(#3493),#1398,.T.);
#26082=ADVANCED_FACE('',(#3494),#166,.F.);
#26083=ADVANCED_FACE('',(#3495),#2148,.T.);
#26084=ADVANCED_FACE('',(#3496),#1399,.T.);
#26085=ADVANCED_FACE('',(#3497),#167,.F.);
#26086=ADVANCED_FACE('',(#3498),#25070,.T.);
#26087=ADVANCED_FACE('',(#3499),#2149,.T.);
#26088=ADVANCED_FACE('',(#3500),#2150,.T.);
#26089=ADVANCED_FACE('',(#3501),#2151,.T.);
#26090=ADVANCED_FACE('',(#3502,#1640),#2152,.F.);
#26091=ADVANCED_FACE('',(#3503),#2153,.T.);
#26092=ADVANCED_FACE('',(#3504),#2154,.T.);
#26093=ADVANCED_FACE('',(#3505),#2155,.T.);
#26094=ADVANCED_FACE('',(#3506),#2156,.T.);
#26095=ADVANCED_FACE('',(#3507),#2157,.T.);
#26096=ADVANCED_FACE('',(#3508),#25071,.T.);
#26097=ADVANCED_FACE('',(#3509),#1400,.T.);
#26098=ADVANCED_FACE('',(#3510,#1641),#2158,.T.);
#26099=ADVANCED_FACE('',(#3511),#1401,.T.);
#26678=CLOSED_SHELL('',(#26042,#26043,#26044,#26045,#26046,#26047,#26048,
#26049,#26050,#26051,#26052,#26053,#26054,#26055,#26056,#26057,#26058,#26059,
#26060,#26061,#26062,#26063,#26064,#26065,#26066,#26067,#26068,#26069,#26070,
#26071,#26072,#26073,#26074,#26075,#26076,#26077,#26078,#26079,#26080,#26081,
#26082,#26083,#26084,#26085,#26086,#26087,#26088,#26089,#26090,#26091,#26092,
#26093,#26094,#26095,#26096,#26097,#26098,#26099));
#28363=AXIS2_PLACEMENT_3D('',#58310,#33573,#33574);
#28364=AXIS2_PLACEMENT_3D('',#58311,#33575,#33576);
#28365=AXIS2_PLACEMENT_3D('',#58333,#33578,#33579);
#28366=AXIS2_PLACEMENT_3D('',#58344,#33580,#33581);
#28367=AXIS2_PLACEMENT_3D('',#58428,#33583,#33584);
#28368=AXIS2_PLACEMENT_3D('',#58518,#33586,#33587);
#28369=AXIS2_PLACEMENT_3D('',#58608,#33589,#33590);
#28370=AXIS2_PLACEMENT_3D('',#58692,#33592,#33593);
#28371=AXIS2_PLACEMENT_3D('',#58782,#33595,#33596);
#28372=AXIS2_PLACEMENT_3D('',#58872,#33598,#33599);
#28373=AXIS2_PLACEMENT_3D('',#58956,#33601,#33602);
#28374=AXIS2_PLACEMENT_3D('',#59046,#33604,#33605);
#28375=AXIS2_PLACEMENT_3D('',#59136,#33607,#33608);
#28376=AXIS2_PLACEMENT_3D('',#59220,#33610,#33611);
#28377=AXIS2_PLACEMENT_3D('',#59310,#33613,#33614);
#28378=AXIS2_PLACEMENT_3D('',#59400,#33616,#33617);
#28379=AXIS2_PLACEMENT_3D('',#59484,#33619,#33620);
#28380=AXIS2_PLACEMENT_3D('',#59574,#33622,#33623);
#28381=AXIS2_PLACEMENT_3D('',#59664,#33625,#33626);
#28382=AXIS2_PLACEMENT_3D('',#59748,#33628,#33629);
#28383=AXIS2_PLACEMENT_3D('',#59838,#33631,#33632);
#28384=AXIS2_PLACEMENT_3D('',#59925,#33634,#33635);
#28385=AXIS2_PLACEMENT_3D('',#60012,#33637,#33638);
#28386=AXIS2_PLACEMENT_3D('',#60022,#33640,#33641);
#28387=AXIS2_PLACEMENT_3D('',#60023,#33642,#33643);
#28388=AXIS2_PLACEMENT_3D('',#60045,#33645,#33646);
#28389=AXIS2_PLACEMENT_3D('',#60061,#33647,#33648);
#28390=AXIS2_PLACEMENT_3D('',#60097,#33650,#33651);
#28391=AXIS2_PLACEMENT_3D('',#60135,#33653,#33654);
#28392=AXIS2_PLACEMENT_3D('',#60172,#33656,#33657);
#28393=AXIS2_PLACEMENT_3D('',#60209,#33659,#33660);
#28394=AXIS2_PLACEMENT_3D('',#60247,#33662,#33663);
#28395=AXIS2_PLACEMENT_3D('',#60284,#33665,#33666);
#28396=AXIS2_PLACEMENT_3D('',#60321,#33668,#33669);
#28397=AXIS2_PLACEMENT_3D('',#60359,#33671,#33672);
#28398=AXIS2_PLACEMENT_3D('',#60396,#33674,#33675);
#28399=AXIS2_PLACEMENT_3D('',#60433,#33677,#33678);
#28400=AXIS2_PLACEMENT_3D('',#60471,#33680,#33681);
#28401=AXIS2_PLACEMENT_3D('',#60508,#33683,#33684);
#28402=AXIS2_PLACEMENT_3D('',#60545,#33686,#33687);
#28403=AXIS2_PLACEMENT_3D('',#60583,#33689,#33690);
#28404=AXIS2_PLACEMENT_3D('',#60620,#33692,#33693);
#28405=AXIS2_PLACEMENT_3D('',#60657,#33695,#33696);
#28406=AXIS2_PLACEMENT_3D('',#60695,#33698,#33699);
#28407=AXIS2_PLACEMENT_3D('',#61950,#33701,#33702);
#28408=AXIS2_PLACEMENT_3D('',#61952,#33703,#33704);
#28409=AXIS2_PLACEMENT_3D('',#61953,#33705,#33706);
#28410=AXIS2_PLACEMENT_3D('',#62031,#33707,#33708);
#28411=AXIS2_PLACEMENT_3D('',#62032,#33709,#33710);
#28412=AXIS2_PLACEMENT_3D('',#63166,#33711,#33712);
#28413=AXIS2_PLACEMENT_3D('',#63190,#33714,#33715);
#28414=AXIS2_PLACEMENT_3D('',#63198,#33716,#33717);
#28415=AXIS2_PLACEMENT_3D('',#63204,#33721,#33722);
#28416=AXIS2_PLACEMENT_3D('',#63208,#33725,#33726);
#28417=AXIS2_PLACEMENT_3D('',#63212,#33729,#33730);
#28418=AXIS2_PLACEMENT_3D('',#63219,#33734,#33735);
#28419=AXIS2_PLACEMENT_3D('',#63220,#33736,#33737);
#28420=AXIS2_PLACEMENT_3D('',#63222,#33739,#33740);
#28421=AXIS2_PLACEMENT_3D('',#63224,#33742,#33743);
#28422=AXIS2_PLACEMENT_3D('',#63225,#33744,#33745);
#28423=AXIS2_PLACEMENT_3D('',#63226,#33746,#33747);
#28424=AXIS2_PLACEMENT_3D('',#63228,#33748,#33749);
#28425=AXIS2_PLACEMENT_3D('',#63229,#33750,#33751);
#28426=AXIS2_PLACEMENT_3D('',#63231,#33753,#33754);
#28427=AXIS2_PLACEMENT_3D('',#63232,#33755,#33756);
#28428=AXIS2_PLACEMENT_3D('',#63233,#33757,#33758);
#28429=AXIS2_PLACEMENT_3D('',#63235,#33759,#33760);
#28430=AXIS2_PLACEMENT_3D('',#63236,#33761,#33762);
#33573=DIRECTION('axis',(0.,0.,1.));
#33574=DIRECTION('refdir',(1.,0.,0.));
#33575=DIRECTION('center_axis',(0.,0.,1.));
#33576=DIRECTION('ref_axis',(1.,0.,0.));
#33577=DIRECTION('',(0.,0.,-1.));
#33578=DIRECTION('center_axis',(0.,0.,1.));
#33579=DIRECTION('ref_axis',(1.,0.,0.));
#33580=DIRECTION('center_axis',(0.,0.,1.));
#33581=DIRECTION('ref_axis',(1.,0.,0.));
#33582=DIRECTION('',(0.,0.,-1.));
#33583=DIRECTION('center_axis',(0.,0.,1.));
#33584=DIRECTION('ref_axis',(1.,0.,0.));
#33585=DIRECTION('',(0.,0.,-1.));
#33586=DIRECTION('center_axis',(0.,0.,1.));
#33587=DIRECTION('ref_axis',(1.,0.,0.));
#33588=DIRECTION('',(0.,0.,-1.));
#33589=DIRECTION('center_axis',(0.,0.,1.));
#33590=DIRECTION('ref_axis',(1.,0.,0.));
#33591=DIRECTION('',(0.,0.,-1.));
#33592=DIRECTION('center_axis',(0.,0.,1.));
#33593=DIRECTION('ref_axis',(1.,0.,0.));
#33594=DIRECTION('',(0.,0.,-1.));
#33595=DIRECTION('center_axis',(0.,0.,1.));
#33596=DIRECTION('ref_axis',(1.,0.,0.));
#33597=DIRECTION('',(0.,0.,-1.));
#33598=DIRECTION('center_axis',(0.,0.,1.));
#33599=DIRECTION('ref_axis',(1.,0.,0.));
#33600=DIRECTION('',(0.,0.,-1.));
#33601=DIRECTION('center_axis',(0.,0.,1.));
#33602=DIRECTION('ref_axis',(1.,0.,0.));
#33603=DIRECTION('',(0.,0.,-1.));
#33604=DIRECTION('center_axis',(0.,0.,1.));
#33605=DIRECTION('ref_axis',(1.,0.,0.));
#33606=DIRECTION('',(0.,0.,-1.));
#33607=DIRECTION('center_axis',(0.,0.,1.));
#33608=DIRECTION('ref_axis',(1.,0.,0.));
#33609=DIRECTION('',(0.,0.,-1.));
#33610=DIRECTION('center_axis',(0.,0.,1.));
#33611=DIRECTION('ref_axis',(1.,0.,0.));
#33612=DIRECTION('',(0.,0.,-1.));
#33613=DIRECTION('center_axis',(0.,0.,1.));
#33614=DIRECTION('ref_axis',(1.,0.,0.));
#33615=DIRECTION('',(0.,0.,-1.));
#33616=DIRECTION('center_axis',(0.,0.,1.));
#33617=DIRECTION('ref_axis',(1.,0.,0.));
#33618=DIRECTION('',(0.,0.,-1.));
#33619=DIRECTION('center_axis',(0.,0.,1.));
#33620=DIRECTION('ref_axis',(1.,0.,0.));
#33621=DIRECTION('',(0.,0.,-1.));
#33622=DIRECTION('center_axis',(0.,0.,1.));
#33623=DIRECTION('ref_axis',(1.,0.,0.));
#33624=DIRECTION('',(0.,0.,-1.));
#33625=DIRECTION('center_axis',(0.,0.,1.));
#33626=DIRECTION('ref_axis',(1.,0.,0.));
#33627=DIRECTION('',(0.,0.,-1.));
#33628=DIRECTION('center_axis',(0.,0.,1.));
#33629=DIRECTION('ref_axis',(1.,0.,0.));
#33630=DIRECTION('',(0.,0.,-1.));
#33631=DIRECTION('center_axis',(0.,0.,1.));
#33632=DIRECTION('ref_axis',(1.,0.,0.));
#33633=DIRECTION('',(0.,0.,-1.));
#33634=DIRECTION('center_axis',(0.,0.,1.));
#33635=DIRECTION('ref_axis',(1.,0.,0.));
#33636=DIRECTION('',(0.,0.,-1.));
#33637=DIRECTION('center_axis',(0.,0.,1.));
#33638=DIRECTION('ref_axis',(1.,1.08272661726521E-13,0.));
#33639=DIRECTION('',(0.,0.,1.));
#33640=DIRECTION('center_axis',(0.,0.,1.));
#33641=DIRECTION('ref_axis',(1.,1.08272661726521E-13,0.));
#33642=DIRECTION('center_axis',(0.,0.,1.));
#33643=DIRECTION('ref_axis',(1.,1.08272661726521E-13,0.));
#33644=DIRECTION('',(0.,0.,1.));
#33645=DIRECTION('center_axis',(0.,0.,1.));
#33646=DIRECTION('ref_axis',(1.,1.08272661726521E-13,0.));
#33647=DIRECTION('center_axis',(0.,0.,1.));
#33648=DIRECTION('ref_axis',(1.,1.08272661726521E-13,0.));
#33649=DIRECTION('',(0.,0.,1.));
#33650=DIRECTION('center_axis',(0.,0.,1.));
#33651=DIRECTION('ref_axis',(1.,1.08272661726521E-13,0.));
#33652=DIRECTION('',(0.,0.,1.));
#33653=DIRECTION('center_axis',(0.,0.,1.));
#33654=DIRECTION('ref_axis',(1.,1.08272661726521E-13,0.));
#33655=DIRECTION('',(0.,0.,1.));
#33656=DIRECTION('center_axis',(0.,0.,1.));
#33657=DIRECTION('ref_axis',(1.,1.08272661726521E-13,0.));
#33658=DIRECTION('',(0.,0.,1.));
#33659=DIRECTION('center_axis',(0.,0.,1.));
#33660=DIRECTION('ref_axis',(1.,1.08272661726521E-13,0.));
#33661=DIRECTION('',(0.,0.,1.));
#33662=DIRECTION('center_axis',(0.,0.,1.));
#33663=DIRECTION('ref_axis',(1.,1.08272661726521E-13,0.));
#33664=DIRECTION('',(0.,0.,1.));
#33665=DIRECTION('center_axis',(0.,0.,1.));
#33666=DIRECTION('ref_axis',(1.,1.08272661726521E-13,0.));
#33667=DIRECTION('',(0.,0.,1.));
#33668=DIRECTION('center_axis',(0.,0.,1.));
#33669=DIRECTION('ref_axis',(1.,1.08272661726521E-13,0.));
#33670=DIRECTION('',(0.,0.,1.));
#33671=DIRECTION('center_axis',(0.,0.,1.));
#33672=DIRECTION('ref_axis',(1.,1.08272661726521E-13,0.));
#33673=DIRECTION('',(0.,0.,1.));
#33674=DIRECTION('center_axis',(0.,0.,1.));
#33675=DIRECTION('ref_axis',(1.,1.08272661726521E-13,0.));
#33676=DIRECTION('',(0.,0.,1.));
#33677=DIRECTION('center_axis',(0.,0.,1.));
#33678=DIRECTION('ref_axis',(1.,1.08272661726521E-13,0.));
#33679=DIRECTION('',(0.,0.,1.));
#33680=DIRECTION('center_axis',(0.,0.,1.));
#33681=DIRECTION('ref_axis',(1.,1.08272661726521E-13,0.));
#33682=DIRECTION('',(0.,0.,1.));
#33683=DIRECTION('center_axis',(0.,0.,1.));
#33684=DIRECTION('ref_axis',(1.,1.08272661726521E-13,0.));
#33685=DIRECTION('',(0.,0.,1.));
#33686=DIRECTION('center_axis',(0.,0.,1.));
#33687=DIRECTION('ref_axis',(1.,1.08272661726521E-13,0.));
#33688=DIRECTION('',(0.,0.,1.));
#33689=DIRECTION('center_axis',(0.,0.,1.));
#33690=DIRECTION('ref_axis',(1.,1.08272661726521E-13,0.));
#33691=DIRECTION('',(0.,0.,1.));
#33692=DIRECTION('center_axis',(0.,0.,1.));
#33693=DIRECTION('ref_axis',(1.,1.08272661726521E-13,0.));
#33694=DIRECTION('',(0.,0.,1.));
#33695=DIRECTION('center_axis',(0.,0.,1.));
#33696=DIRECTION('ref_axis',(1.,1.08272661726521E-13,0.));
#33697=DIRECTION('',(0.,0.,1.));
#33698=DIRECTION('center_axis',(0.,0.,1.));
#33699=DIRECTION('ref_axis',(1.,1.08272661726521E-13,0.));
#33700=DIRECTION('',(0.,0.,1.));
#33701=DIRECTION('center_axis',(0.,0.,1.));
#33702=DIRECTION('ref_axis',(1.,0.,0.));
#33703=DIRECTION('center_axis',(0.,0.,1.));
#33704=DIRECTION('ref_axis',(1.,0.,0.));
#33705=DIRECTION('center_axis',(0.,0.,1.));
#33706=DIRECTION('ref_axis',(1.,0.,0.));
#33707=DIRECTION('center_axis',(0.,0.,-1.));
#33708=DIRECTION('ref_axis',(1.,1.08272661726521E-13,0.));
#33709=DIRECTION('center_axis',(0.,0.,1.));
#33710=DIRECTION('ref_axis',(0.888988591948248,0.457929343224335,0.));
#33711=DIRECTION('center_axis',(0.,0.,-1.));
#33712=DIRECTION('ref_axis',(1.,0.,0.));
#33713=DIRECTION('',(0.866025403784438,1.06057523872491E-16,0.5));
#33714=DIRECTION('center_axis',(0.,0.,1.));
#33715=DIRECTION('ref_axis',(1.,0.,0.));
#33716=DIRECTION('center_axis',(-0.5,0.866025403784439,0.));
#33717=DIRECTION('ref_axis',(-0.866025403784439,-0.5,0.));
#33718=DIRECTION('',(0.,0.,1.));
#33719=DIRECTION('',(-0.866025403784439,-0.5,0.));
#33720=DIRECTION('',(0.,0.,1.));
#33721=DIRECTION('center_axis',(0.5,0.866025403784439,0.));
#33722=DIRECTION('ref_axis',(-0.866025403784439,0.5,0.));
#33723=DIRECTION('',(0.,0.,1.));
#33724=DIRECTION('',(-0.866025403784439,0.5,0.));
#33725=DIRECTION('center_axis',(1.,-3.20493781063927E-16,0.));
#33726=DIRECTION('ref_axis',(3.20493781063927E-16,1.,0.));
#33727=DIRECTION('',(0.,0.,1.));
#33728=DIRECTION('',(3.20493781063927E-16,1.,0.));
#33729=DIRECTION('center_axis',(0.,0.,1.));
#33730=DIRECTION('ref_axis',(1.,0.,0.));
#33731=DIRECTION('',(0.866025403784439,0.5,0.));
#33732=DIRECTION('',(0.866025403784439,-0.5,0.));
#33733=DIRECTION('',(1.60246890531964E-16,-1.,0.));
#33734=DIRECTION('center_axis',(0.,0.,1.));
#33735=DIRECTION('ref_axis',(1.,0.,0.));
#33736=DIRECTION('center_axis',(0.5,-0.866025403784439,0.));
#33737=DIRECTION('ref_axis',(0.866025403784439,0.5,0.));
#33738=DIRECTION('',(0.,0.,1.));
#33739=DIRECTION('center_axis',(-0.5,-0.866025403784439,0.));
#33740=DIRECTION('ref_axis',(0.866025403784439,-0.5,0.));
#33741=DIRECTION('',(0.,0.,1.));
#33742=DIRECTION('center_axis',(-1.,-1.60246890531964E-16,0.));
#33743=DIRECTION('ref_axis',(1.60246890531964E-16,-1.,0.));
#33744=DIRECTION('center_axis',(0.,0.,1.));
#33745=DIRECTION('ref_axis',(1.,0.,0.));
#33746=DIRECTION('center_axis',(0.,0.,-1.));
#33747=DIRECTION('ref_axis',(-1.,0.,0.));
#33748=DIRECTION('center_axis',(0.,0.,1.));
#33749=DIRECTION('ref_axis',(1.,0.,0.));
#33750=DIRECTION('center_axis',(0.,0.,1.));
#33751=DIRECTION('ref_axis',(1.,0.,0.));
#33752=DIRECTION('',(0.707106781186548,8.65956056235493E-17,-0.707106781186548));
#33753=DIRECTION('center_axis',(0.,0.,1.));
#33754=DIRECTION('ref_axis',(1.,0.,0.));
#33755=DIRECTION('center_axis',(0.,0.,1.));
#33756=DIRECTION('ref_axis',(1.,0.,0.));
#33757=DIRECTION('center_axis',(0.,0.,-1.));
#33758=DIRECTION('ref_axis',(-1.,0.,0.));
#33759=DIRECTION('center_axis',(0.,0.,1.));
#33760=DIRECTION('ref_axis',(1.,0.,0.));
#33761=DIRECTION('center_axis',(0.,0.,1.));
#33762=DIRECTION('ref_axis',(1.,0.,0.));
#33763=DIRECTION('',(0.,0.,-1.));
#58310=CARTESIAN_POINT('',(0.,0.,0.));
#58311=CARTESIAN_POINT('Origin',(0.,0.,-1.97));
#58312=CARTESIAN_POINT('',(-0.791095370814336,2.02259992215237E-5,-3.8846668491763));
#58313=CARTESIAN_POINT('',(-0.791088063690405,1.27402156131747E-5,-3.91313315082371));
#58314=CARTESIAN_POINT('',(-0.7911,-9.68818082805471E-17,-1.97));
#58315=CARTESIAN_POINT('',(0.342080900406933,0.713328864346838,-3.9489));
#58316=CARTESIAN_POINT('Ctrl Pts',(-0.791095370814336,2.02259992215237E-5,
-3.8846668491763));
#58317=CARTESIAN_POINT('Ctrl Pts',(-0.791127180071213,0.0317239595158518,
-3.88594249553439));
#58318=CARTESIAN_POINT('Ctrl Pts',(-0.789257131989506,0.0634239528721169,
-3.88721814189247));
#58319=CARTESIAN_POINT('Ctrl Pts',(-0.785455659529297,0.0948905938491621,
-3.88849378825056));
#58320=CARTESIAN_POINT('Ctrl Pts',(-0.769753962153839,0.224861198454451,
-3.89376275002326));
#58321=CARTESIAN_POINT('Ctrl Pts',(-0.72110136963018,0.35085071538898,-3.89903171179596));
#58322=CARTESIAN_POINT('Ctrl Pts',(-0.64537450685374,0.457642147479495,
-3.90430067356865));
#58323=CARTESIAN_POINT('Ctrl Pts',(-0.5696476440773,0.564433579570009,-3.90956963534135));
#58324=CARTESIAN_POINT('Ctrl Pts',(-0.466846511048079,0.65202692681651,
-3.91483859711405));
#58325=CARTESIAN_POINT('Ctrl Pts',(-0.349388046343934,0.709840384691014,
-3.92010755888674));
#58326=CARTESIAN_POINT('Ctrl Pts',(-0.231929581639788,0.767653842565517,
-3.92537652065944));
#58327=CARTESIAN_POINT('Ctrl Pts',(-0.0998137852607172,0.795687411068025,
-3.93064548243214));
#58328=CARTESIAN_POINT('Ctrl Pts',(0.0310013642589058,0.79055831756017,
-3.93591444420484));
#58329=CARTESIAN_POINT('Ctrl Pts',(0.138467660670603,0.786344702506695,
-3.94024296280323));
#58330=CARTESIAN_POINT('Ctrl Pts',(0.245056172644429,0.759750171050252,
-3.94457148140161));
#58331=CARTESIAN_POINT('Ctrl Pts',(0.342093838304098,0.713335417936179,
-3.9489));
#58332=CARTESIAN_POINT('',(-0.342067962509736,0.713322310757513,-3.9489));
#58333=CARTESIAN_POINT('Origin',(0.,0.,-3.9489));
#58334=CARTESIAN_POINT('Ctrl Pts',(-0.342067962509735,0.713322310757513,
-3.9489));
#58335=CARTESIAN_POINT('Ctrl Pts',(-0.46014371667664,0.65670003490751,-3.9436310382273));
#58336=CARTESIAN_POINT('Ctrl Pts',(-0.563833106070677,0.570227774954663,
-3.93836207645461));
#58337=CARTESIAN_POINT('Ctrl Pts',(-0.640649635030828,0.464237010222487,
-3.93309311468191));
#58338=CARTESIAN_POINT('Ctrl Pts',(-0.717466163990983,0.358246245490307,
-3.92782415290921));
#58339=CARTESIAN_POINT('Ctrl Pts',(-0.76740983251725,0.232736975978797,
-3.92255519113652));
#58340=CARTESIAN_POINT('Ctrl Pts',(-0.784443001930775,0.102927663684584,
-3.91728622936382));
#58341=CARTESIAN_POINT('Ctrl Pts',(-0.788918272607942,0.068821749815602,
-3.91590186985045));
#58342=CARTESIAN_POINT('Ctrl Pts',(-0.791121680212704,0.0344189972881027,
-3.91451751033708));
#58343=CARTESIAN_POINT('Ctrl Pts',(-0.791088063690405,1.27402156131747E-5,
-3.91313315082371));
#58344=CARTESIAN_POINT('Origin',(0.,0.,-1.97));
#58345=CARTESIAN_POINT('',(-0.791148086150792,-1.30343001421562E-5,-3.6846668491763));
#58346=CARTESIAN_POINT('',(-0.791154135421776,-1.08354013588121E-5,-3.71313315082371));
#58347=CARTESIAN_POINT('',(-0.7911,-9.68818082805471E-17,-1.97));
#58348=CARTESIAN_POINT('Ctrl Pts',(-0.791148086150792,-1.30343001421562E-5,
-3.6846668491763));
#58349=CARTESIAN_POINT('Ctrl Pts',(-0.791056365338982,0.117140979863682,
-3.68938162092869));
#58350=CARTESIAN_POINT('Ctrl Pts',(-0.764692832251995,0.234334903162113,
-3.69409639268107));
#58351=CARTESIAN_POINT('Ctrl Pts',(-0.714334439804961,0.340104540826193,
-3.69881116443346));
#58352=CARTESIAN_POINT('Ctrl Pts',(-0.658056753699895,0.458306694998732,
-3.70408012620616));
#58353=CARTESIAN_POINT('Ctrl Pts',(-0.571811812939802,0.562241023229086,
-3.70934908797886));
#58354=CARTESIAN_POINT('Ctrl Pts',(-0.466016861463421,0.639353638687129,
-3.71461804975155));
#58355=CARTESIAN_POINT('Ctrl Pts',(-0.360221909987037,0.716466254145174,
-3.71988701152425));
#58356=CARTESIAN_POINT('Ctrl Pts',(-0.234876947794366,0.766757156830906,
-3.72515597329695));
#58357=CARTESIAN_POINT('Ctrl Pts',(-0.105121982318275,0.784151872785568,
-3.73042493506965));
#58358=CARTESIAN_POINT('Ctrl Pts',(0.0246329831578159,0.80154658874023,
-3.73569389684234));
#58359=CARTESIAN_POINT('Ctrl Pts',(0.158797951917326,0.786045117963822,
-3.74096285861504));
#58360=CARTESIAN_POINT('Ctrl Pts',(0.281167576752436,0.739519833388521,
-3.74623182038774));
#58361=CARTESIAN_POINT('Ctrl Pts',(0.403537201587544,0.692994548813219,
-3.75150078216043));
#58362=CARTESIAN_POINT('Ctrl Pts',(0.514111482498253,0.615445450439025,
-3.75676974393313));
#58363=CARTESIAN_POINT('Ctrl Pts',(0.599534514333022,0.516239437821845,
-3.76203870570583));
#58364=CARTESIAN_POINT('Ctrl Pts',(0.684957546167791,0.417033425204665,
-3.76730766747853));
#58365=CARTESIAN_POINT('Ctrl Pts',(0.745229328926622,0.2961704983445,-3.77257662925122));
#58366=CARTESIAN_POINT('Ctrl Pts',(0.773069831196375,0.16824929834069,-3.77784559102392));
#58367=CARTESIAN_POINT('Ctrl Pts',(0.800910333466129,0.0403280983368783,
-3.78311455279662));
#58368=CARTESIAN_POINT('Ctrl Pts',(0.796319555246806,-0.0946513748105791,
-3.78838351456931));
#58369=CARTESIAN_POINT('Ctrl Pts',(0.759852001945513,-0.220385400473636,
-3.79365247634201));
#58370=CARTESIAN_POINT('Ctrl Pts',(0.72338444864422,-0.346119426136694,
-3.79892143811471));
#58371=CARTESIAN_POINT('Ctrl Pts',(0.655040120260958,-0.462608004315351,
-3.80419039988741));
#58372=CARTESIAN_POINT('Ctrl Pts',(0.563074103712653,-0.555780845804767,
-3.8094593616601));
#58373=CARTESIAN_POINT('Ctrl Pts',(0.471108087164348,-0.648953687294184,
-3.8147283234328));
#58374=CARTESIAN_POINT('Ctrl Pts',(0.355520382451001,-0.718810792094359,
-3.8199972852055));
#58375=CARTESIAN_POINT('Ctrl Pts',(0.230272451163248,-0.756914379389003,
-3.82526624697819));
#58376=CARTESIAN_POINT('Ctrl Pts',(0.105024519875495,-0.795017966683648,
-3.83053520875089));
#58377=CARTESIAN_POINT('Ctrl Pts',(-0.0298836379866628,-0.801368036472762,
-3.83580417052359));
#58378=CARTESIAN_POINT('Ctrl Pts',(-0.158156910444709,-0.775197525753902,
-3.84107313229629));
#58379=CARTESIAN_POINT('Ctrl Pts',(-0.286430182902755,-0.749027015035042,
-3.84634209406899));
#58380=CARTESIAN_POINT('Ctrl Pts',(-0.408068569956688,-0.690335923808209,
-3.85161105584168));
#58381=CARTESIAN_POINT('Ctrl Pts',(-0.508379764208429,-0.606213471982601,
-3.85688001761438));
#58382=CARTESIAN_POINT('Ctrl Pts',(-0.60869095846017,-0.522091020156992,
-3.86214897938708));
#58383=CARTESIAN_POINT('Ctrl Pts',(-0.687674959909718,-0.412537207732608,
-3.86741794115977));
#58384=CARTESIAN_POINT('Ctrl Pts',(-0.735791559520864,-0.290784455382393,
-3.87268690293247));
#58385=CARTESIAN_POINT('Ctrl Pts',(-0.772258849893215,-0.198508754076189,
-3.87668021834708));
#58386=CARTESIAN_POINT('Ctrl Pts',(-0.790995794317285,-0.0992259380727511,
-3.88067353376169));
#58387=CARTESIAN_POINT('Ctrl Pts',(-0.791095370814336,2.02259992215237E-5,
-3.8846668491763));
#58388=CARTESIAN_POINT('Ctrl Pts',(-0.791088063690405,1.27402156131747E-5,
-3.91313315082371));
#58389=CARTESIAN_POINT('Ctrl Pts',(-0.790993733556351,-0.0965334406484677,
-3.90924854856438));
#58390=CARTESIAN_POINT('Ctrl Pts',(-0.773285078394182,-0.193107216295182,
-3.90536394630505));
#58391=CARTESIAN_POINT('Ctrl Pts',(-0.738731862930085,-0.283227384398608,
-3.90147934404572));
#58392=CARTESIAN_POINT('Ctrl Pts',(-0.691864884215088,-0.405463765110667,
-3.89621038227303));
#58393=CARTESIAN_POINT('Ctrl Pts',(-0.614008256484312,-0.515827171457867,
-3.89094142050033));
#58394=CARTESIAN_POINT('Ctrl Pts',(-0.514564415044768,-0.600974467117274,
-3.88567245872763));
#58395=CARTESIAN_POINT('Ctrl Pts',(-0.415120573605223,-0.686121762776682,
-3.88040349695494));
#58396=CARTESIAN_POINT('Ctrl Pts',(-0.29408951845691,-0.746052947748297,
-3.87513453518224));
#58397=CARTESIAN_POINT('Ctrl Pts',(-0.166091021675515,-0.773535586441187,
-3.86986557340954));
#58398=CARTESIAN_POINT('Ctrl Pts',(-0.0380925248941205,-0.801018225134078,
-3.86459661163685));
#58399=CARTESIAN_POINT('Ctrl Pts',(0.0968734135203562,-0.796052317548245,
-3.85932764986415));
#58400=CARTESIAN_POINT('Ctrl Pts',(0.222505123087384,-0.75923438303122,
-3.85405868809145));
#58401=CARTESIAN_POINT('Ctrl Pts',(0.348136832654412,-0.722416448514195,
-3.84878972631875));
#58402=CARTESIAN_POINT('Ctrl Pts',(0.46443431337399,-0.653746487065977,
-3.84352076454606));
#58403=CARTESIAN_POINT('Ctrl Pts',(0.557350157120219,-0.561520602927027,
-3.83825180277336));
#58404=CARTESIAN_POINT('Ctrl Pts',(0.650266000866448,-0.469294718788076,
-3.83298284100066));
#58405=CARTESIAN_POINT('Ctrl Pts',(0.719800207639327,-0.353512911958392,
-3.82771387922796));
#58406=CARTESIAN_POINT('Ctrl Pts',(0.757554078908919,-0.228159226736181,
-3.82244491745526));
#58407=CARTESIAN_POINT('Ctrl Pts',(0.79530795017851,-0.10280554151397,-3.81717595568257));
#58408=CARTESIAN_POINT('Ctrl Pts',(0.801281485944814,0.0321200221007681,
-3.81190699390987));
#58409=CARTESIAN_POINT('Ctrl Pts',(0.77475310587338,0.160319807147988,-3.80663803213718));
#58410=CARTESIAN_POINT('Ctrl Pts',(0.748224725801946,0.288519592195209,
-3.80136907036448));
#58411=CARTESIAN_POINT('Ctrl Pts',(0.689194429892775,0.409993598674911,
-3.79610010859178));
#58412=CARTESIAN_POINT('Ctrl Pts',(0.604792323138865,0.510069604101474,
-3.79083114681908));
#58413=CARTESIAN_POINT('Ctrl Pts',(0.520390216384955,0.610145609528036,
-3.78556218504638));
#58414=CARTESIAN_POINT('Ctrl Pts',(0.410616298786307,0.68882361390146,-3.78029322327369));
#58415=CARTESIAN_POINT('Ctrl Pts',(0.288729787557062,0.736600243804584,
-3.77502426150099));
#58416=CARTESIAN_POINT('Ctrl Pts',(0.166843276327817,0.784376873707709,
-3.7697552997283));
#58417=CARTESIAN_POINT('Ctrl Pts',(0.0328441714679761,0.801252129140533,
-3.7644863379556));
#58418=CARTESIAN_POINT('Ctrl Pts',(-0.0970822064716226,0.785187762022969,
-3.7592173761829));
#58419=CARTESIAN_POINT('Ctrl Pts',(-0.227008584411221,0.769123394905404,
-3.7539484144102));
#58420=CARTESIAN_POINT('Ctrl Pts',(-0.352862235430576,0.72011940523745,
-3.7486794526375));
#58421=CARTESIAN_POINT('Ctrl Pts',(-0.459441713072965,0.644094794404274,
-3.74341049086481));
#58422=CARTESIAN_POINT('Ctrl Pts',(-0.566021190715353,0.568070183571098,
-3.73814152909211));
#58423=CARTESIAN_POINT('Ctrl Pts',(-0.653326494980774,0.465024951572699,
-3.73287256731941));
#58424=CARTESIAN_POINT('Ctrl Pts',(-0.710812302136216,0.347405609839384,
-3.72760360554672));
#58425=CARTESIAN_POINT('Ctrl Pts',(-0.763437835435081,0.239730674211535,
-3.72278012063905));
#58426=CARTESIAN_POINT('Ctrl Pts',(-0.79107303432946,0.11984185467478,-3.71795663573138));
#58427=CARTESIAN_POINT('Ctrl Pts',(-0.791154135421776,-1.08354013588121E-5,
-3.71313315082371));
#58428=CARTESIAN_POINT('Origin',(0.,0.,-1.97));
#58429=CARTESIAN_POINT('',(-0.791035972316788,-5.6290844032969E-6,-3.4846668491763));
#58430=CARTESIAN_POINT('',(-0.791038502556067,-7.96146359545246E-6,-3.51313315082371));
#58431=CARTESIAN_POINT('',(-0.7911,-9.68818082805471E-17,-1.97));
#58432=CARTESIAN_POINT('Ctrl Pts',(-0.791035972316788,-5.6290844032969E-6,
-3.4846668491763));
#58433=CARTESIAN_POINT('Ctrl Pts',(-0.791017986661468,0.0717093183474517,
-3.48755178455029));
#58434=CARTESIAN_POINT('Ctrl Pts',(-0.781352061791521,0.143429019127269,
-3.49043671992428));
#58435=CARTESIAN_POINT('Ctrl Pts',(-0.762101399692471,0.2124764625646,-3.49332165529827));
#58436=CARTESIAN_POINT('Ctrl Pts',(-0.726942552248791,0.338582698168257,
-3.49859061707097));
#58437=CARTESIAN_POINT('Ctrl Pts',(-0.659812564339618,0.455775271058536,
-3.50385957884366));
#58438=CARTESIAN_POINT('Ctrl Pts',(-0.568819847341814,0.549898874182554,
-3.50912854061636));
#58439=CARTESIAN_POINT('Ctrl Pts',(-0.477827130344009,0.644022477306572,
-3.51439750238906));
#58440=CARTESIAN_POINT('Ctrl Pts',(-0.362971684257575,0.715077110664329,
-3.51966646416176));
#58441=CARTESIAN_POINT('Ctrl Pts',(-0.238126522243223,0.754480317809225,
-3.52493542593445));
#58442=CARTESIAN_POINT('Ctrl Pts',(-0.113281360228871,0.793883524954121,
-3.53020438770715));
#58443=CARTESIAN_POINT('Ctrl Pts',(0.0215535177133972,0.801635305886155,
-3.53547334947985));
#58444=CARTESIAN_POINT('Ctrl Pts',(0.150091848285218,0.776799348374844,
-3.54074231125254));
#58445=CARTESIAN_POINT('Ctrl Pts',(0.278630178857039,0.751963390863533,
-3.54601127302524));
#58446=CARTESIAN_POINT('Ctrl Pts',(0.400871962058412,0.694539694908876,
-3.55128023479794));
#58447=CARTESIAN_POINT('Ctrl Pts',(0.502052013260071,0.611464280672721,
-3.55654919657064));
#58448=CARTESIAN_POINT('Ctrl Pts',(0.60323206446173,0.528388866436566,-3.56181815834333));
#58449=CARTESIAN_POINT('Ctrl Pts',(0.683350383663675,0.419661733918913,
-3.56708712011603));
#58450=CARTESIAN_POINT('Ctrl Pts',(0.732729741491315,0.298415677355171,
-3.57235608188873));
#58451=CARTESIAN_POINT('Ctrl Pts',(0.782109099318956,0.177169620791428,
-3.57762504366142));
#58452=CARTESIAN_POINT('Ctrl Pts',(0.800749495772293,0.0434046401815959,
-3.58289400543412));
#58453=CARTESIAN_POINT('Ctrl Pts',(0.786399418414295,-0.0867222305693646,
-3.58816296720682));
#58454=CARTESIAN_POINT('Ctrl Pts',(0.772049341056297,-0.216849101320323,
-3.59343192897952));
#58455=CARTESIAN_POINT('Ctrl Pts',(0.724708789886964,-0.34333786221241,
-3.59870089075221));
#58456=CARTESIAN_POINT('Ctrl Pts',(0.650095875033401,-0.450910350093206,
-3.60396985252491));
#58457=CARTESIAN_POINT('Ctrl Pts',(0.575482960179837,-0.558482837974004,
-3.60923881429761));
#58458=CARTESIAN_POINT('Ctrl Pts',(0.473597681642042,-0.647139052843511,
-3.61450777607031));
#58459=CARTESIAN_POINT('Ctrl Pts',(0.356746428521924,-0.706170500867693,
-3.619776737843));
#58460=CARTESIAN_POINT('Ctrl Pts',(0.239895175401807,-0.765201948891874,
-3.6250456996157));
#58461=CARTESIAN_POINT('Ctrl Pts',(0.108077947699368,-0.79460863007073,
-3.6303146613884));
#58462=CARTESIAN_POINT('Ctrl Pts',(-0.0227834833757317,-0.79083860770631,
-3.63558362316109));
#58463=CARTESIAN_POINT('Ctrl Pts',(-0.153644914450832,-0.787068585341889,
-3.64085258493379));
#58464=CARTESIAN_POINT('Ctrl Pts',(-0.283550548898593,-0.750121859434192,
-3.64612154670649));
#58465=CARTESIAN_POINT('Ctrl Pts',(-0.396809510599002,-0.684461103979865,
-3.65139050847919));
#58466=CARTESIAN_POINT('Ctrl Pts',(-0.510068472299412,-0.618800348525538,
-3.65665947025188));
#58467=CARTESIAN_POINT('Ctrl Pts',(-0.606680761252469,-0.52442556352458,
-3.66192843202458));
#58468=CARTESIAN_POINT('Ctrl Pts',(-0.674976895496427,-0.412735970199464,
-3.66719739379728));
#58469=CARTESIAN_POINT('Ctrl Pts',(-0.743273029740385,-0.301046376874347,
-3.67246635556998));
#58470=CARTESIAN_POINT('Ctrl Pts',(-0.783253009275243,-0.172041975225071,
-3.67773531734267));
#58471=CARTESIAN_POINT('Ctrl Pts',(-0.790087783317653,-0.04130478434307,
-3.68300427911537));
#58472=CARTESIAN_POINT('Ctrl Pts',(-0.790806665657055,-0.027553831195994,
-3.68355846913568));
#58473=CARTESIAN_POINT('Ctrl Pts',(-0.791158867321383,-0.0137837084490869,
-3.68411265915599));
#58474=CARTESIAN_POINT('Ctrl Pts',(-0.791148086150792,-1.30343001421562E-5,
-3.6846668491763));
#58475=CARTESIAN_POINT('Ctrl Pts',(-0.791154135421776,-1.08354013588121E-5,
-3.71313315082371));
#58476=CARTESIAN_POINT('Ctrl Pts',(-0.791161625579006,-0.0110799279064996,
-3.71268767395868));
#58477=CARTESIAN_POINT('Ctrl Pts',(-0.790934090413866,-0.0221487122419377,
-3.71224219709365));
#58478=CARTESIAN_POINT('Ctrl Pts',(-0.790469510301835,-0.033207538364532,
-3.71179672022862));
#58479=CARTESIAN_POINT('Ctrl Pts',(-0.784974601266551,-0.164007893366901,
-3.70652775845593));
#58480=CARTESIAN_POINT('Ctrl Pts',(-0.746318473150519,-0.293415151903407,
-3.70125879668323));
#58481=CARTESIAN_POINT('Ctrl Pts',(-0.679170272548202,-0.405798631037627,
-3.69598983491053));
#58482=CARTESIAN_POINT('Ctrl Pts',(-0.612022071945885,-0.518182110171848,
-3.69072087313784));
#58483=CARTESIAN_POINT('Ctrl Pts',(-0.516381798857284,-0.613541809903783,
-3.68545191136514));
#58484=CARTESIAN_POINT('Ctrl Pts',(-0.40380152889302,-0.680359546472222,
-3.68018294959244));
#58485=CARTESIAN_POINT('Ctrl Pts',(-0.291221258928757,-0.747177283040659,
-3.67491398781975));
#58486=CARTESIAN_POINT('Ctrl Pts',(-0.161700992088831,-0.785453056445601,
-3.66964502604705));
#58487=CARTESIAN_POINT('Ctrl Pts',(-0.0308850570683372,-0.79056366032998,
-3.66437606427435));
#58488=CARTESIAN_POINT('Ctrl Pts',(0.099930877952157,-0.795674264214359,
-3.65910710250165));
#58489=CARTESIAN_POINT('Ctrl Pts',(0.232042481153218,-0.767619698578176,
-3.65383814072896));
#58490=CARTESIAN_POINT('Ctrl Pts',(0.349492424604498,-0.709788583056294,
-3.64856917895626));
#58491=CARTESIAN_POINT('Ctrl Pts',(0.466942368055779,-0.651957467534411,
-3.64330021718356));
#58492=CARTESIAN_POINT('Ctrl Pts',(0.569730651757277,-0.564349802126829,
-3.63803125541086));
#58493=CARTESIAN_POINT('Ctrl Pts',(0.645441815605794,-0.457547429533762,
-3.63276229363817));
#58494=CARTESIAN_POINT('Ctrl Pts',(0.72115297945431,-0.350745056940696,
-3.62749333186547));
#58495=CARTESIAN_POINT('Ctrl Pts',(0.769787023449843,-0.224747977162145,
-3.62222437009277));
#58496=CARTESIAN_POINT('Ctrl Pts',(0.785469600685382,-0.0947749649415118,
-3.61695540832007));
#58497=CARTESIAN_POINT('Ctrl Pts',(0.80115217792092,0.0351980472791211,
-3.61168644654738));
#58498=CARTESIAN_POINT('Ctrl Pts',(0.783883288396462,0.169146991941836,
-3.60641748477468));
#58499=CARTESIAN_POINT('Ctrl Pts',(0.735748784728155,0.290892614798992,
-3.60114852300198));
#58500=CARTESIAN_POINT('Ctrl Pts',(0.687614281059848,0.412638237656147,
-3.59587956122929));
#58501=CARTESIAN_POINT('Ctrl Pts',(0.608614163247692,0.522180538707743,
-3.59061059945659));
#58502=CARTESIAN_POINT('Ctrl Pts',(0.508290596778049,0.606288262143795,
-3.58534163768389));
#58503=CARTESIAN_POINT('Ctrl Pts',(0.407967030308406,0.690395985579847,
-3.58007267591119));
#58504=CARTESIAN_POINT('Ctrl Pts',(0.286320015181275,0.749069131400354,
-3.5748037141385));
#58505=CARTESIAN_POINT('Ctrl Pts',(0.158042895940592,0.77522076250535,-3.5695347523658));
#58506=CARTESIAN_POINT('Ctrl Pts',(0.0297657766999073,0.801372393610346,
-3.5642657905931));
#58507=CARTESIAN_POINT('Ctrl Pts',(-0.105141446654331,0.79500250999983,
-3.55899682882041));
#58508=CARTESIAN_POINT('Ctrl Pts',(-0.230383772459609,0.756880509043066,
-3.55372786704771));
#58509=CARTESIAN_POINT('Ctrl Pts',(-0.355626098264886,0.718758508086303,
-3.54845890527501));
#58510=CARTESIAN_POINT('Ctrl Pts',(-0.471203526521203,0.648884389783291,
-3.54318994350231));
#58511=CARTESIAN_POINT('Ctrl Pts',(-0.563155838205542,0.555698020038532,
-3.53792098172961));
#58512=CARTESIAN_POINT('Ctrl Pts',(-0.655108149889881,0.462511650293772,
-3.53265201995692));
#58513=CARTESIAN_POINT('Ctrl Pts',(-0.723435345002244,0.346013029107264,
-3.52738305818422));
#58514=CARTESIAN_POINT('Ctrl Pts',(-0.759884405429078,0.220273643375871,
-3.52211409641153));
#58515=CARTESIAN_POINT('Ctrl Pts',(-0.780593547162765,0.148832713757253,
-3.51912044788225));
#58516=CARTESIAN_POINT('Ctrl Pts',(-0.791012000528327,0.0744087417130748,
-3.51612679935298));
#58517=CARTESIAN_POINT('Ctrl Pts',(-0.791038502556067,-7.96146359545246E-6,
-3.51313315082371));
#58518=CARTESIAN_POINT('Origin',(0.,0.,-1.97));
#58519=CARTESIAN_POINT('',(-0.791112467551816,1.9457402925846E-5,-3.2846668491763));
#58520=CARTESIAN_POINT('',(-0.791104010802578,1.99443795460114E-5,-3.31313315082371));
#58521=CARTESIAN_POINT('',(-0.7911,-9.68818082805471E-17,-1.97));
#58522=CARTESIAN_POINT('Ctrl Pts',(-0.791112467551816,1.9457402925846E-5,
-3.2846668491763));
#58523=CARTESIAN_POINT('Ctrl Pts',(-0.791139111989659,0.0262402740262119,
-3.28572194817189));
#58524=CARTESIAN_POINT('Ctrl Pts',(-0.789860844776933,0.0524585044539771,
-3.28677704716749));
#58525=CARTESIAN_POINT('Ctrl Pts',(-0.787258239359726,0.078544605909112,
-3.28783214616308));
#58526=CARTESIAN_POINT('Ctrl Pts',(-0.774261327686072,0.208813587246341,
-3.29310110793578));
#58527=CARTESIAN_POINT('Ctrl Pts',(-0.728237913550483,0.335787520668241,
-3.29837006970847));
#58528=CARTESIAN_POINT('Ctrl Pts',(-0.654747014411506,0.444129640619056,
-3.30363903148117));
#58529=CARTESIAN_POINT('Ctrl Pts',(-0.581256115272529,0.552471760569871,
-3.30890799325386));
#58530=CARTESIAN_POINT('Ctrl Pts',(-0.480297731130164,0.642182067049603,
-3.31417695502656));
#58531=CARTESIAN_POINT('Ctrl Pts',(-0.364066294548254,0.702424745955819,
-3.31944591679926));
#58532=CARTESIAN_POINT('Ctrl Pts',(-0.247834857966343,0.762667424862035,
-3.32471487857196));
#58533=CARTESIAN_POINT('Ctrl Pts',(-0.116330368944885,0.793442476194735,
-3.32998384034465));
#58534=CARTESIAN_POINT('Ctrl Pts',(0.0145631759878715,0.791032682297223,
-3.33525280211735));
#58535=CARTESIAN_POINT('Ctrl Pts',(0.145456720920629,0.788622888399711,
-3.34052176389005));
#58536=CARTESIAN_POINT('Ctrl Pts',(0.275739321764686,0.753028249271988,
-3.34579072566275));
#58537=CARTESIAN_POINT('Ctrl Pts',(0.389674569862843,0.6885481247955,-3.35105968743544));
#58538=CARTESIAN_POINT('Ctrl Pts',(0.503609817961001,0.624068000319013,
-3.35632864920814));
#58539=CARTESIAN_POINT('Ctrl Pts',(0.601197713313261,0.53070239049376,-3.36159761098084));
#58540=CARTESIAN_POINT('Ctrl Pts',(0.670650933657783,0.41972862154151,-3.36686657275354));
#58541=CARTESIAN_POINT('Ctrl Pts',(0.740104154002306,0.308754852589261,
-3.37213553452623));
#58542=CARTESIAN_POINT('Ctrl Pts',(0.781422699339092,0.180172924510018,
-3.37740449629893));
#58543=CARTESIAN_POINT('Ctrl Pts',(0.789615837902518,0.0495138272677194,
-3.38267345807163));
#58544=CARTESIAN_POINT('Ctrl Pts',(0.797808976465944,-0.0811452699745802,
-3.38794241984432));
#58545=CARTESIAN_POINT('Ctrl Pts',(0.772876708256009,-0.213881536379933,
-3.39321138161702));
#58546=CARTESIAN_POINT('Ctrl Pts',(0.717830520292166,-0.332662193064182,
-3.39848034338972));
#58547=CARTESIAN_POINT('Ctrl Pts',(0.662784332328323,-0.45144284974843,
-3.40374930516242));
#58548=CARTESIAN_POINT('Ctrl Pts',(0.577624224610571,-0.556267896711576,
-3.40901826693511));
#58549=CARTESIAN_POINT('Ctrl Pts',(0.472636407635597,-0.634475859851665,
-3.41428722870781));
#58550=CARTESIAN_POINT('Ctrl Pts',(0.367648590660623,-0.712683822991754,
-3.41955619048051));
#58551=CARTESIAN_POINT('Ctrl Pts',(0.242833064428427,-0.764274702308787,
-3.4248251522532));
#58552=CARTESIAN_POINT('Ctrl Pts',(0.113265887559485,-0.783017004459389,
-3.4300941140259));
#58553=CARTESIAN_POINT('Ctrl Pts',(-0.0163012893094561,-0.801759306609992,
-3.4353630757986));
#58554=CARTESIAN_POINT('Ctrl Pts',(-0.150620116815143,-0.787653031594163,
-3.4406320375713));
#58555=CARTESIAN_POINT('Ctrl Pts',(-0.273466663701279,-0.742402030170502,
-3.44590099934399));
#58556=CARTESIAN_POINT('Ctrl Pts',(-0.396313210587416,-0.697151028746841,
-3.45116996111669));
#58557=CARTESIAN_POINT('Ctrl Pts',(-0.507687476854002,-0.620755300915348,
-3.45643892288939));
#58558=CARTESIAN_POINT('Ctrl Pts',(-0.594136929649284,-0.522442436431149,
-3.46170788466209));
#58559=CARTESIAN_POINT('Ctrl Pts',(-0.680586382444567,-0.42412957194695,
-3.46697684643478));
#58560=CARTESIAN_POINT('Ctrl Pts',(-0.742111021768545,-0.303899570810043,
-3.47224580820748));
#58561=CARTESIAN_POINT('Ctrl Pts',(-0.771279487941441,-0.176274621083071,
-3.47751476998018));
#58562=CARTESIAN_POINT('Ctrl Pts',(-0.784477229046018,-0.118528662313859,
-3.47989879637888));
#58563=CARTESIAN_POINT('Ctrl Pts',(-0.791050835137449,-0.0592687687029965,
-3.48228282277759));
#58564=CARTESIAN_POINT('Ctrl Pts',(-0.791035972316788,-5.6290844032969E-6,
-3.4846668491763));
#58565=CARTESIAN_POINT('Ctrl Pts',(-0.791038502556067,-7.96146359545246E-6,
-3.51313315082371));
#58566=CARTESIAN_POINT('Ctrl Pts',(-0.791058645339732,-0.0565681450035753,
-3.51085783758028));
#58567=CARTESIAN_POINT('Ctrl Pts',(-0.785075656402411,-0.113124129527635,
-3.50858252433686));
#58568=CARTESIAN_POINT('Ctrl Pts',(-0.773045075503138,-0.168362997183885,
-3.50630721109343));
#58569=CARTESIAN_POINT('Ctrl Pts',(-0.745185759409057,-0.296280101735969,
-3.50103824932074));
#58570=CARTESIAN_POINT('Ctrl Pts',(-0.684896201479589,-0.41713416056386,
-3.49576928754804));
#58571=CARTESIAN_POINT('Ctrl Pts',(-0.599458579958063,-0.516327607720986,
-3.49050032577534));
#58572=CARTESIAN_POINT('Ctrl Pts',(-0.514020958436537,-0.615521054878112,
-3.48523136400264));
#58573=CARTESIAN_POINT('Ctrl Pts',(-0.403435273322952,-0.693053890364472,
-3.47996240222995));
#58574=CARTESIAN_POINT('Ctrl Pts',(-0.281058807334294,-0.739561176915201,
-3.47469344045725));
#58575=CARTESIAN_POINT('Ctrl Pts',(-0.158682341345636,-0.78606846346593,
-3.46942447868455));
#58576=CARTESIAN_POINT('Ctrl Pts',(-0.0245150944819038,-0.801550201081026,
-3.46415551691186));
#58577=CARTESIAN_POINT('Ctrl Pts',(0.105237310929872,-0.784136401379585,
-3.45888655513916));
#58578=CARTESIAN_POINT('Ctrl Pts',(0.234989716341648,-0.766722601678145,
-3.45361759336646));
#58579=CARTESIAN_POINT('Ctrl Pts',(0.360327280301469,-0.716413264660167,
-3.44834863159376));
#58580=CARTESIAN_POINT('Ctrl Pts',(0.466110888961514,-0.639285090371915,
-3.44307966982107));
#58581=CARTESIAN_POINT('Ctrl Pts',(0.571894497621558,-0.562156916083665,
-3.43781070804837));
#58582=CARTESIAN_POINT('Ctrl Pts',(0.658124150981828,-0.458209904525141,
-3.43254174627567));
#58583=CARTESIAN_POINT('Ctrl Pts',(0.714384451630426,-0.339999474777539,
-3.42727278450297));
#58584=CARTESIAN_POINT('Ctrl Pts',(0.770644752279024,-0.221789045029936,
-3.42200382273028));
#58585=CARTESIAN_POINT('Ctrl Pts',(0.796935700215949,-0.0893151970932543,
-3.41673486095758));
#58586=CARTESIAN_POINT('Ctrl Pts',(0.790081697947446,0.0414209868157352,
-3.41146589918488));
#58587=CARTESIAN_POINT('Ctrl Pts',(0.783227695678943,0.172157170724725,
-3.40619693741219));
#58588=CARTESIAN_POINT('Ctrl Pts',(0.743228743205012,0.301155690606022,
-3.40092797563949));
#58589=CARTESIAN_POINT('Ctrl Pts',(0.674916182991274,0.412835237736315,
-3.39565901386679));
#58590=CARTESIAN_POINT('Ctrl Pts',(0.606603622777536,0.524514784866607,
-3.39039005209409));
#58591=CARTESIAN_POINT('Ctrl Pts',(0.509977454823992,0.618875359245894,
-3.3851210903214));
#58592=CARTESIAN_POINT('Ctrl Pts',(0.396708837489817,0.684519456142618,
-3.3798521285487));
#58593=CARTESIAN_POINT('Ctrl Pts',(0.283440220155643,0.750163553039342,
-3.374583166776));
#58594=CARTESIAN_POINT('Ctrl Pts',(0.153529153440839,0.787091172453503,
-3.3693142050033));
#58595=CARTESIAN_POINT('Ctrl Pts',(0.0226671696119708,0.790841948180603,
-3.36404524323061));
#58596=CARTESIAN_POINT('Ctrl Pts',(-0.108194814216899,0.794592723907703,
-3.35877628145791));
#58597=CARTESIAN_POINT('Ctrl Pts',(-0.240007715159833,0.765166655947741,
-3.35350731968522));
#58598=CARTESIAN_POINT('Ctrl Pts',(-0.356850284622694,0.70611802267398,
-3.34823835791252));
#58599=CARTESIAN_POINT('Ctrl Pts',(-0.473692854085554,0.64706938940022,
-3.34296939613982));
#58600=CARTESIAN_POINT('Ctrl Pts',(-0.575565092068342,0.558398190812661,
-3.33770043436712));
#58601=CARTESIAN_POINT('Ctrl Pts',(-0.650162184594864,0.450814730574705,
-3.33243147259442));
#58602=CARTESIAN_POINT('Ctrl Pts',(-0.724759277121385,0.343231270336749,
-3.32716251082173));
#58603=CARTESIAN_POINT('Ctrl Pts',(-0.772081224191642,0.216735548448396,
-3.32189354904903));
#58604=CARTESIAN_POINT('Ctrl Pts',(-0.786412162806834,0.0866065688604893,
-3.31662458727633));
#58605=CARTESIAN_POINT('Ctrl Pts',(-0.789577591066389,0.0578635841589875,
-3.31546077512546));
#58606=CARTESIAN_POINT('Ctrl Pts',(-0.791133444132945,0.0289433389935947,
-3.31429696297458));
#58607=CARTESIAN_POINT('Ctrl Pts',(-0.791104010802578,1.99443795460114E-5,
-3.31313315082371));
#58608=CARTESIAN_POINT('Origin',(0.,0.,-1.97));
#58609=CARTESIAN_POINT('',(-0.79113354225774,-1.66712748377318E-5,-3.0846668491763));
#58610=CARTESIAN_POINT('',(-0.791141030195672,-1.50259769734546E-5,-3.11313315082371));
#58611=CARTESIAN_POINT('',(-0.7911,-9.68818082805471E-17,-1.97));
#58612=CARTESIAN_POINT('Ctrl Pts',(-0.79113354225774,-1.66712748377318E-5,
-3.0846668491763));
#58613=CARTESIAN_POINT('Ctrl Pts',(-0.791029149168141,0.111663060150681,
-3.08916107356619));
#58614=CARTESIAN_POINT('Ctrl Pts',(-0.767145880831491,0.223386024459756,
-3.09365529795608));
#58615=CARTESIAN_POINT('Ctrl Pts',(-0.721249064670457,0.325183912992608,
-3.09814952234598));
#58616=CARTESIAN_POINT('Ctrl Pts',(-0.667440320633363,0.444530242122759,
-3.10341848411867));
#58617=CARTESIAN_POINT('Ctrl Pts',(-0.583374244479453,0.550234685063485,
-3.10868744589137));
#58618=CARTESIAN_POINT('Ctrl Pts',(-0.479204902215964,0.62952954835288,
-3.11395640766407));
#58619=CARTESIAN_POINT('Ctrl Pts',(-0.375035559952474,0.708824411642276,
-3.11922536943676));
#58620=CARTESIAN_POINT('Ctrl Pts',(-0.250762951579405,0.761709695280341,
-3.12449433120946));
#58621=CARTESIAN_POINT('Ctrl Pts',(-0.121397558447183,0.781797559065168,
-3.12976329298216));
#58622=CARTESIAN_POINT('Ctrl Pts',(0.00796783468503921,0.801885422849996,
-3.13503225475486));
#58623=CARTESIAN_POINT('Ctrl Pts',(0.142426012576414,0.789175866781586,
-3.14030121652755));
#58624=CARTESIAN_POINT('Ctrl Pts',(0.265736212293957,0.745204036511379,
-3.14557017830025));
#58625=CARTESIAN_POINT('Ctrl Pts',(0.3890464120115,0.701232206241173,-3.15083914007295));
#58626=CARTESIAN_POINT('Ctrl Pts',(0.501208633555211,0.625998101769169,
-3.15610810184565));
#58627=CARTESIAN_POINT('Ctrl Pts',(0.588675169536104,0.528589004169432,
-3.16137706361834));
#58628=CARTESIAN_POINT('Ctrl Pts',(0.676141705516998,0.431179906569694,
-3.16664602539104));
#58629=CARTESIAN_POINT('Ctrl Pts',(0.738912555935075,0.311595815842222,
-3.17191498716374));
#58630=CARTESIAN_POINT('Ctrl Pts',(0.769405835354065,0.184280902646762,
-3.17718394893643));
#58631=CARTESIAN_POINT('Ctrl Pts',(0.799899114773056,0.056965989451302,
-3.18245291070913));
#58632=CARTESIAN_POINT('Ctrl Pts',(0.798114823192961,-0.0780797462121464,
-3.18772187248183));
#58633=CARTESIAN_POINT('Ctrl Pts',(0.764268479349867,-0.204544572231665,
-3.19299083425453));
#58634=CARTESIAN_POINT('Ctrl Pts',(0.730422135506773,-0.331009398251184,
-3.19825979602722));
#58635=CARTESIAN_POINT('Ctrl Pts',(0.664513739400679,-0.448893314626773,
-3.20352875779992));
#58636=CARTESIAN_POINT('Ctrl Pts',(0.574504150335489,-0.543957509190278,
-3.20879771957262));
#58637=CARTESIAN_POINT('Ctrl Pts',(0.484494561270298,-0.639021703753782,
-3.21406668134531));
#58638=CARTESIAN_POINT('Ctrl Pts',(0.370383779246011,-0.711266176505201,
-3.21933564311801));
#58639=CARTESIAN_POINT('Ctrl Pts',(0.245954871890178,-0.751964754194423,
-3.22460460489071));
#58640=CARTESIAN_POINT('Ctrl Pts',(0.121525964534345,-0.792663331883645,
-3.22987356666341));
#58641=CARTESIAN_POINT('Ctrl Pts',(-0.0132210681530342,-0.801816014510671,
-3.2351425284361));
#58642=CARTESIAN_POINT('Ctrl Pts',(-0.142010573414216,-0.778317279517651,
-3.2404114902088));
#58643=CARTESIAN_POINT('Ctrl Pts',(-0.270800078675396,-0.754818544524631,
-3.2456804519815));
#58644=CARTESIAN_POINT('Ctrl Pts',(-0.393632056510379,-0.698668391911567,
-3.2509494137542));
#58645=CARTESIAN_POINT('Ctrl Pts',(-0.495670034613112,-0.616649014710823,
-3.2562183755269));
#58646=CARTESIAN_POINT('Ctrl Pts',(-0.597708012715845,-0.53462963751008,
-3.26148733729959));
#58647=CARTESIAN_POINT('Ctrl Pts',(-0.678951991086329,-0.426741035721658,
-3.26675629907229));
#58648=CARTESIAN_POINT('Ctrl Pts',(-0.729588775665712,-0.306014720201168,
-3.27202526084498));
#58649=CARTESIAN_POINT('Ctrl Pts',(-0.770085645997359,-0.209463606502664,
-3.27623912362209));
#58650=CARTESIAN_POINT('Ctrl Pts',(-0.791006054783621,-0.10470144899133,
-3.28045298639919));
#58651=CARTESIAN_POINT('Ctrl Pts',(-0.791112467551816,1.9457402925846E-5,
-3.2846668491763));
#58652=CARTESIAN_POINT('Ctrl Pts',(-0.791104010802578,1.99443795460114E-5,
-3.31313315082371));
#58653=CARTESIAN_POINT('Ctrl Pts',(-0.79100018973065,-0.102002415820376,
-3.30902800120189));
#58654=CARTESIAN_POINT('Ctrl Pts',(-0.7711721440249,-0.204063961641823,
-3.30492285158006));
#58655=CARTESIAN_POINT('Ctrl Pts',(-0.732685842008116,-0.298523440455128,
-3.30081770195824));
#58656=CARTESIAN_POINT('Ctrl Pts',(-0.68328865243408,-0.419762232895373,
-3.29554874018554));
#58657=CARTESIAN_POINT('Ctrl Pts',(-0.603154343125882,-0.528477580488403,
-3.29027977841284));
#58658=CARTESIAN_POINT('Ctrl Pts',(-0.501962074850703,-0.611538112460611,
-3.28501081664015));
#58659=CARTESIAN_POINT('Ctrl Pts',(-0.400769806575523,-0.694598644432819,
-3.27974185486745));
#58660=CARTESIAN_POINT('Ctrl Pts',(-0.278519579333359,-0.752004360784205,
-3.27447289309475));
#58661=CARTESIAN_POINT('Ctrl Pts',(-0.149977597681499,-0.776821413050642,
-3.26920393132206));
#58662=CARTESIAN_POINT('Ctrl Pts',(-0.0214356160296378,-0.801638465317079,
-3.26393496954936));
#58663=CARTESIAN_POINT('Ctrl Pts',(0.113398120031922,-0.793866853498568,
-3.25866600777666));
#58664=CARTESIAN_POINT('Ctrl Pts',(0.238237485128838,-0.754445285133253,
-3.25339704600397));
#58665=CARTESIAN_POINT('Ctrl Pts',(0.363076850225755,-0.715023716767938,
-3.24812808423127));
#58666=CARTESIAN_POINT('Ctrl Pts',(0.477921844358028,-0.643952191855818,
-3.24285912245857));
#58667=CARTESIAN_POINT('Ctrl Pts',(0.56890071682226,-0.549815207119108,
-3.23759016068587));
#58668=CARTESIAN_POINT('Ctrl Pts',(0.659879589286491,-0.4556782223824,-3.23232119891318));
#58669=CARTESIAN_POINT('Ctrl Pts',(0.726992340082681,-0.338475777821101,
-3.22705223714048));
#58670=CARTESIAN_POINT('Ctrl Pts',(0.762132639848386,-0.212364372854862,
-3.22178327536778));
#58671=CARTESIAN_POINT('Ctrl Pts',(0.797272939614092,-0.0862529678886238,
-3.21651431359509));
#58672=CARTESIAN_POINT('Ctrl Pts',(0.800440788349314,0.0487673974825542,
-3.21124535182239));
#58673=CARTESIAN_POINT('Ctrl Pts',(0.771253551980593,0.176388055541266,
-3.20597639004969));
#58674=CARTESIAN_POINT('Ctrl Pts',(0.742066315611872,0.304008713599979,
-3.20070742827699));
#58675=CARTESIAN_POINT('Ctrl Pts',(0.680523994139208,0.424229664346224,
-3.19543846650429));
#58676=CARTESIAN_POINT('Ctrl Pts',(0.594060083011206,0.52252981288442,-3.1901695047316));
#58677=CARTESIAN_POINT('Ctrl Pts',(0.507596171883205,0.620829961422615,
-3.1849005429589));
#58678=CARTESIAN_POINT('Ctrl Pts',(0.396210671099867,0.697209307752761,
-3.1796315811862));
#58679=CARTESIAN_POINT('Ctrl Pts',(0.273357470493429,0.742442240787621,
-3.17436261941351));
#58680=CARTESIAN_POINT('Ctrl Pts',(0.150504269886989,0.787675173822481,
-3.16909365764081));
#58681=CARTESIAN_POINT('Ctrl Pts',(0.0161833694574468,0.801761693562055,
-3.16382469586811));
#58682=CARTESIAN_POINT('Ctrl Pts',(-0.113381049157215,0.783000335422864,
-3.15855573409542));
#58683=CARTESIAN_POINT('Ctrl Pts',(-0.242945467771877,0.764238977283673,
-3.15328677232272));
#58684=CARTESIAN_POINT('Ctrl Pts',(-0.367753404571661,0.712629741265718,
-3.14801781055002));
#58685=CARTESIAN_POINT('Ctrl Pts',(-0.472729717638774,0.634406337958153,
-3.14274884877732));
#58686=CARTESIAN_POINT('Ctrl Pts',(-0.577706030705887,0.556182934650588,
-3.13747988700463));
#58687=CARTESIAN_POINT('Ctrl Pts',(-0.662850720040329,0.451345364053415,
-3.13221092523193));
#58688=CARTESIAN_POINT('Ctrl Pts',(-0.717879437481436,0.332556612957322,
-3.12694196345923));
#58689=CARTESIAN_POINT('Ctrl Pts',(-0.765952238253124,0.228783379073186,
-3.12233902591406));
#58690=CARTESIAN_POINT('Ctrl Pts',(-0.791041497371546,0.114363052701224,
-3.11773608836888));
#58691=CARTESIAN_POINT('Ctrl Pts',(-0.791141030195672,-1.50259769734546E-5,
-3.11313315082371));
#58692=CARTESIAN_POINT('Origin',(0.,0.,-1.97));
#58693=CARTESIAN_POINT('',(-0.791033587110486,-6.80849259582228E-7,-2.8846668491763));
#58694=CARTESIAN_POINT('',(-0.79103429425828,-3.14382039938683E-6,-2.91313315082371));
#58695=CARTESIAN_POINT('',(-0.7911,-9.68818082805471E-17,-1.97));
#58696=CARTESIAN_POINT('Ctrl Pts',(-0.791033587110486,-6.80849259582228E-7,
-2.8846668491763));
#58697=CARTESIAN_POINT('Ctrl Pts',(-0.791031585449306,0.0662323781931633,
-2.88733123718779));
#58698=CARTESIAN_POINT('Ctrl Pts',(-0.782802743498501,0.132465925751853,
-2.88999562519929));
#58699=CARTESIAN_POINT('Ctrl Pts',(-0.766353006923597,0.196590588117425,
-2.89266001321078));
#58700=CARTESIAN_POINT('Ctrl Pts',(-0.733822822577261,0.323400344516865,
-2.89792897498348));
#58701=CARTESIAN_POINT('Ctrl Pts',(-0.669143137337217,0.441962871204574,
-2.90319793675618));
#58702=CARTESIAN_POINT('Ctrl Pts',(-0.580126398546105,0.537957388895363,
-2.90846689852887));
#58703=CARTESIAN_POINT('Ctrl Pts',(-0.491109659754995,0.633951906586151,
-2.91373586030157));
#58704=CARTESIAN_POINT('Ctrl Pts',(-0.377755867412819,0.707378415280021,
-2.91900482207427));
#58705=CARTESIAN_POINT('Ctrl Pts',(-0.253756654842699,0.749367967476751,
-2.92427378384697));
#58706=CARTESIAN_POINT('Ctrl Pts',(-0.129757442272579,0.79135751967348,
-2.92954274561967));
#58707=CARTESIAN_POINT('Ctrl Pts',(0.00488719052548373,0.801910115373071,
-2.93481170739236));
#58708=CARTESIAN_POINT('Ctrl Pts',(0.133913959340999,0.779751141102602,
-2.94008066916506));
#58709=CARTESIAN_POINT('Ctrl Pts',(0.262940728156516,0.757592166832132,
-2.94534963093776));
#58710=CARTESIAN_POINT('Ctrl Pts',(0.386349632989485,0.702721622591603,
-2.95061859271045));
#58711=CARTESIAN_POINT('Ctrl Pts',(0.489234516411306,0.621767141709007,
-2.95588755448315));
#58712=CARTESIAN_POINT('Ctrl Pts',(0.592119399833126,0.540812660826412,
-2.96115651625585));
#58713=CARTESIAN_POINT('Ctrl Pts',(0.674480261843798,0.43377424330175,-2.96642547802854));
#58714=CARTESIAN_POINT('Ctrl Pts',(0.726369003667566,0.313580709017918,
-2.97169443980124));
#58715=CARTESIAN_POINT('Ctrl Pts',(0.778257745491333,0.193387174734087,
-2.97696340157394));
#58716=CARTESIAN_POINT('Ctrl Pts',(0.799674367128196,0.0600385236910853,
-2.98223236334664));
#58717=CARTESIAN_POINT('Ctrl Pts',(0.788032024993892,-0.0703584972922178,
-2.98750132511934));
#58718=CARTESIAN_POINT('Ctrl Pts',(0.776389682859588,-0.200755518275521,
-2.99277028689203));
#58719=CARTESIAN_POINT('Ctrl Pts',(0.731688376954118,-0.328200909199126,
-2.99803924866473));
#58720=CARTESIAN_POINT('Ctrl Pts',(0.659327431613055,-0.437300958699755,
-3.00330821043743));
#58721=CARTESIAN_POINT('Ctrl Pts',(0.586966486271991,-0.546401008200385,
-3.00857717221012));
#58722=CARTESIAN_POINT('Ctrl Pts',(0.486945901495334,-0.637155716278039,
-3.01384613398282));
#58723=CARTESIAN_POINT('Ctrl Pts',(0.371346836133002,-0.698603118981874,
-3.01911509575552));
#58724=CARTESIAN_POINT('Ctrl Pts',(0.255747770770669,-0.760050521685709,
-3.02438405752821));
#58725=CARTESIAN_POINT('Ctrl Pts',(0.12457022482266,-0.792190619015725,
-3.02965301930091));
#58726=CARTESIAN_POINT('Ctrl Pts',(-0.00634129556582329,-0.791141313879979,
-3.03492198107361));
#58727=CARTESIAN_POINT('Ctrl Pts',(-0.137252815954308,-0.790092008744234,
-3.04019094284631));
#58728=CARTESIAN_POINT('Ctrl Pts',(-0.267898310783268,-0.755853301142726,
-3.04545990461901));
#58729=CARTESIAN_POINT('Ctrl Pts',(-0.382497538619609,-0.692560772428769,
-3.0507288663917));
#58730=CARTESIAN_POINT('Ctrl Pts',(-0.497096766455945,-0.629268243714814,
-3.0559978281644));
#58731=CARTESIAN_POINT('Ctrl Pts',(-0.595649727299664,-0.536921893888413,
-3.0612667899371));
#58732=CARTESIAN_POINT('Ctrl Pts',(-0.666252531788976,-0.426675936094329,
-3.06653575170979));
#58733=CARTESIAN_POINT('Ctrl Pts',(-0.736855336278291,-0.316429978300241,
-3.07180471348249));
#58734=CARTESIAN_POINT('Ctrl Pts',(-0.779507984413199,-0.188284412538469,
-3.07707367525519));
#58735=CARTESIAN_POINT('Ctrl Pts',(-0.789058602520514,-0.0577175219977951,
-3.08234263702788));
#58736=CARTESIAN_POINT('Ctrl Pts',(-0.79046290591003,-0.0385192329567601,
-3.08311737441069));
#58737=CARTESIAN_POINT('Ctrl Pts',(-0.791151538072368,-0.019268594483546,
-3.08389211179349));
#58738=CARTESIAN_POINT('Ctrl Pts',(-0.79113354225774,-1.66712748377318E-5,
-3.0846668491763));
#58739=CARTESIAN_POINT('Ctrl Pts',(-0.791141030195672,-1.50259769734546E-5,
-3.11313315082371));
#58740=CARTESIAN_POINT('Ctrl Pts',(-0.791155432144787,-0.0165650162276427,
-3.11246712659618));
#58741=CARTESIAN_POINT('Ctrl Pts',(-0.79064662969104,-0.0331141219476401,
-3.11180110236866));
#58742=CARTESIAN_POINT('Ctrl Pts',(-0.789608545183721,-0.0496299602372971,
-3.11113507814114));
#58743=CARTESIAN_POINT('Ctrl Pts',(-0.781396189897128,-0.180287850740814,
-3.10586611636844));
#58744=CARTESIAN_POINT('Ctrl Pts',(-0.74005873377617,-0.30886370015284,
-3.10059715459575));
#58745=CARTESIAN_POINT('Ctrl Pts',(-0.670589192758155,-0.419827252731733,
-3.09532819282305));
#58746=CARTESIAN_POINT('Ctrl Pts',(-0.60111965174014,-0.530790805310627,
-3.09005923105035));
#58747=CARTESIAN_POINT('Ctrl Pts',(-0.50351802582507,-0.624142061056388,
-3.08479026927766));
#58748=CARTESIAN_POINT('Ctrl Pts',(-0.389573295744491,-0.688605427529499,
-3.07952130750496));
#58749=CARTESIAN_POINT('Ctrl Pts',(-0.275628565663913,-0.75306879400261,
-3.07425234573226));
#58750=CARTESIAN_POINT('Ctrl Pts',(-0.145340731417827,-0.788644271203071,
-3.06898338395956));
#58751=CARTESIAN_POINT('Ctrl Pts',(-0.0144468337889248,-0.79103481375587,
-3.06371442218686));
#58752=CARTESIAN_POINT('Ctrl Pts',(0.116447063839978,-0.79342535630867,
-3.05844546041417));
#58753=CARTESIAN_POINT('Ctrl Pts',(0.247947024851698,-0.762630964213808,
-3.05317649864147));
#58754=CARTESIAN_POINT('Ctrl Pts',(0.364169599641456,-0.702371191235297,
-3.04790753686877));
#58755=CARTESIAN_POINT('Ctrl Pts',(0.480392174431212,-0.642111418256788,
-3.04263857509608));
#58756=CARTESIAN_POINT('Ctrl Pts',(0.581337362999006,-0.552386264394629,
-3.03736961332338));
#58757=CARTESIAN_POINT('Ctrl Pts',(0.654812326631231,-0.444033337117951,
-3.03210065155068));
#58758=CARTESIAN_POINT('Ctrl Pts',(0.728287290263455,-0.335680409841273,
-3.02683168977798));
#58759=CARTESIAN_POINT('Ctrl Pts',(0.774292028960111,-0.208699709150073,
-3.02156272800529));
#58760=CARTESIAN_POINT('Ctrl Pts',(0.787269781007753,-0.0784288179964015,
-3.01629376623259));
#58761=CARTESIAN_POINT('Ctrl Pts',(0.800247533055396,0.0518420731572732,
-3.01102480445989));
#58762=CARTESIAN_POINT('Ctrl Pts',(0.780198298454025,0.185403154773419,
-3.0057558426872));
#58763=CARTESIAN_POINT('Ctrl Pts',(0.729543758586319,0.306122021239989,
-3.0004868809145));
#58764=CARTESIAN_POINT('Ctrl Pts',(0.678889218718613,0.426840887706558,
-2.9952179191418));
#58765=CARTESIAN_POINT('Ctrl Pts',(0.597629373584572,0.53471753902355,-2.9899489573691));
#58766=CARTESIAN_POINT('Ctrl Pts',(0.495579333737454,0.616721907793659,
-2.98467999559641));
#58767=CARTESIAN_POINT('Ctrl Pts',(0.393529293890335,0.698726276563767,
-2.97941103382371));
#58768=CARTESIAN_POINT('Ctrl Pts',(0.270689059330137,0.754858362786991,
-2.97414207205101));
#58769=CARTESIAN_POINT('Ctrl Pts',(0.141896099665709,0.778338155611023,
-2.96887311027832));
#58770=CARTESIAN_POINT('Ctrl Pts',(0.0131031400012812,0.801817948435054,
-2.96360414850562));
#58771=CARTESIAN_POINT('Ctrl Pts',(-0.121642544767378,0.792645447859891,
-2.95833518673292));
#58772=CARTESIAN_POINT('Ctrl Pts',(-0.24606546469321,0.751928570188435,
-2.95306622496022));
#58773=CARTESIAN_POINT('Ctrl Pts',(-0.370488384619043,0.711211692516977,
-2.94779726318752));
#58774=CARTESIAN_POINT('Ctrl Pts',(-0.484588539702047,0.638950437749227,
-2.94252830141483));
#58775=CARTESIAN_POINT('Ctrl Pts',(-0.57458414590811,0.54387300618008,-2.93725933964213));
#58776=CARTESIAN_POINT('Ctrl Pts',(-0.664579752114172,0.448795574610933,
-2.93199037786943));
#58777=CARTESIAN_POINT('Ctrl Pts',(-0.730470809443291,0.330901966240389,
-2.92672141609674));
#58778=CARTESIAN_POINT('Ctrl Pts',(-0.764298552885645,0.204432163900935,
-2.92145245432404));
#58779=CARTESIAN_POINT('Ctrl Pts',(-0.782102393349158,0.137869988740161,
-2.91867935315726));
#58780=CARTESIAN_POINT('Ctrl Pts',(-0.791024663908618,0.0689321993021295,
-2.91590625199048));
#58781=CARTESIAN_POINT('Ctrl Pts',(-0.79103429425828,-3.14382039938683E-6,
-2.91313315082371));
#58782=CARTESIAN_POINT('Origin',(0.,0.,-1.97));
#58783=CARTESIAN_POINT('',(-0.791129214786214,1.74461675192319E-5,-2.6846668491763));
#58784=CARTESIAN_POINT('',(-0.791121074183877,1.86068176132095E-5,-2.71313315082371));
#58785=CARTESIAN_POINT('',(-0.7911,-9.68818082805471E-17,-1.97));
#58786=CARTESIAN_POINT('Ctrl Pts',(-0.791129214786214,1.74461675192319E-5,
-2.6846668491763));
#58787=CARTESIAN_POINT('Ctrl Pts',(-0.791149167492266,0.0207560581004413,
-2.68550140080939));
#58788=CARTESIAN_POINT('Ctrl Pts',(-0.790349974374689,0.0414931362015937,
-2.68633595244249));
#58789=CARTESIAN_POINT('Ctrl Pts',(-0.788720691736706,0.0621647889368653,
-2.68717050407559));
#58790=CARTESIAN_POINT('Ctrl Pts',(-0.778434176683608,0.192675764796195,
-2.69243946584829));
#58791=CARTESIAN_POINT('Ctrl Pts',(-0.735059807397815,0.320578847270327,
-2.69770842762099));
#58792=CARTESIAN_POINT('Ctrl Pts',(-0.663836631886564,0.430425041932617,
-2.70297738939368));
#58793=CARTESIAN_POINT('Ctrl Pts',(-0.592613456375313,0.540271236594907,
-2.70824635116638));
#58794=CARTESIAN_POINT('Ctrl Pts',(-0.493541474638603,0.632060543445355,
-2.71351531293908));
#58795=CARTESIAN_POINT('Ctrl Pts',(-0.378587266872002,0.694706032735847,
-2.71878427471178));
#58796=CARTESIAN_POINT('Ctrl Pts',(-0.263633059105401,0.757351522026339,
-2.72405323648447));
#58797=CARTESIAN_POINT('Ctrl Pts',(-0.132796625308907,0.790853193756876,
-2.72932219825717));
#58798=CARTESIAN_POINT('Ctrl Pts',(-0.00188126980814461,0.791164490723075,
-2.73459116002987));
#58799=CARTESIAN_POINT('Ctrl Pts',(0.129034085692618,0.791475787689273,
-2.73986012180256));
#58800=CARTESIAN_POINT('Ctrl Pts',(0.260028362897649,0.758596709891134,
-2.74512908357526));
#58801=CARTESIAN_POINT('Ctrl Pts',(0.375279192092976,0.69649861345105,-2.75039804534796));
#58802=CARTESIAN_POINT('Ctrl Pts',(0.4905300212883,0.634400517010968,-2.75566700712066));
#58803=CARTESIAN_POINT('Ctrl Pts',(0.590037402473921,0.543083401928943,
-2.76093596889336));
#58804=CARTESIAN_POINT('Ctrl Pts',(0.661782164980846,0.433577163455892,
-2.76620493066605));
#58805=CARTESIAN_POINT('Ctrl Pts',(0.733526927487771,0.324070924982842,
-2.77147389243875));
#58806=CARTESIAN_POINT('Ctrl Pts',(0.777509071316001,0.196375563118767,
-2.77674285421144));
#58807=CARTESIAN_POINT('Ctrl Pts',(0.788416137361891,0.0659149823981434,
-2.78201181598414));
#58808=CARTESIAN_POINT('Ctrl Pts',(0.799323203407781,-0.0645455983224819,
-2.78728077775684));
#58809=CARTESIAN_POINT('Ctrl Pts',(0.77715519167133,-0.197771397899656,
-2.79254973952954));
#58810=CARTESIAN_POINT('Ctrl Pts',(0.72458970368599,-0.317670508340706,
-2.79781870130223));
#58811=CARTESIAN_POINT('Ctrl Pts',(0.67202421570065,-0.437569618781756,
-2.80308766307493));
#58812=CARTESIAN_POINT('Ctrl Pts',(0.589061251466421,-0.544142040086684,
-2.80835662484763));
#58813=CARTESIAN_POINT('Ctrl Pts',(0.485721635714653,-0.624515238529753,
-2.81362558662032));
#58814=CARTESIAN_POINT('Ctrl Pts',(0.382382019962884,-0.704888436972823,
-2.81889454839302));
#58815=CARTESIAN_POINT('Ctrl Pts',(0.258665752693575,-0.759062412554035,
-2.82416351016572));
#58816=CARTESIAN_POINT('Ctrl Pts',(0.129516116637345,-0.780493668192366,
-2.82943247193842));
#58817=CARTESIAN_POINT('Ctrl Pts',(0.000366480581115436,-0.801924923830697,
-2.83470143371112));
#58818=CARTESIAN_POINT('Ctrl Pts',(-0.134216524262036,-0.790613459526147,
-2.83997039548381));
#58819=CARTESIAN_POINT('Ctrl Pts',(-0.257977057520448,-0.747925550005001,
-2.84523935725651));
#58820=CARTESIAN_POINT('Ctrl Pts',(-0.381737590778861,-0.705237640483855,
-2.85050831902921));
#58821=CARTESIAN_POINT('Ctrl Pts',(-0.494675652452535,-0.631173285746112,
-2.8557772808019));
#58822=CARTESIAN_POINT('Ctrl Pts',(-0.583149823964202,-0.534678476626573,
-2.8610462425746));
#58823=CARTESIAN_POINT('Ctrl Pts',(-0.671623995475868,-0.438183667507034,
-2.8663152043473));
#58824=CARTESIAN_POINT('Ctrl Pts',(-0.735634276825528,-0.319258404005699,
-2.87158416611999));
#58825=CARTESIAN_POINT('Ctrl Pts',(-0.767449075774044,-0.192267279199444,
-2.87685312789269));
#58826=CARTESIAN_POINT('Ctrl Pts',(-0.783175891441716,-0.129492530426392,
-2.87945770165389));
#58827=CARTESIAN_POINT('Ctrl Pts',(-0.791035543835318,-0.0647468390521015,
-2.8820622754151));
#58828=CARTESIAN_POINT('Ctrl Pts',(-0.791033587110486,-6.80849259582228E-7,
-2.8846668491763));
#58829=CARTESIAN_POINT('Ctrl Pts',(-0.79103429425828,-3.14382039938683E-6,
-2.91313315082371));
#58830=CARTESIAN_POINT('Ctrl Pts',(-0.791042961814527,-0.0620466816892262,
-2.91063729021779));
#58831=CARTESIAN_POINT('Ctrl Pts',(-0.783831988405732,-0.124088237932048,
-2.90814142961187));
#58832=CARTESIAN_POINT('Ctrl Pts',(-0.769378721885218,-0.184394061429801,
-2.90564556900595));
#58833=CARTESIAN_POINT('Ctrl Pts',(-0.738866717886847,-0.311704488112714,
-2.90037660723325));
#58834=CARTESIAN_POINT('Ctrl Pts',(-0.676078280334516,-0.431279345170175,
-2.89510764546055));
#58835=CARTESIAN_POINT('Ctrl Pts',(-0.588597418956837,-0.528675577247199,
-2.88983868368786));
#58836=CARTESIAN_POINT('Ctrl Pts',(-0.501116557579159,-0.626071809324222,
-2.88456972191516));
#58837=CARTESIAN_POINT('Ctrl Pts',(-0.388943272376134,-0.701289416420807,
-2.87930076014246));
#58838=CARTESIAN_POINT('Ctrl Pts',(-0.265626607079919,-0.745243110126836,
-2.87403179836976));
#58839=CARTESIAN_POINT('Ctrl Pts',(-0.142309941783703,-0.789196803832866,
-2.86876283659707));
#58840=CARTESIAN_POINT('Ctrl Pts',(-0.00784989639429788,-0.801886584148338,
-2.86349387482437));
#58841=CARTESIAN_POINT('Ctrl Pts',(0.121512540586341,-0.781779694070242,
-2.85822491305167));
#58842=CARTESIAN_POINT('Ctrl Pts',(0.25087497756698,-0.761672803992146,
-2.85295595127898));
#58843=CARTESIAN_POINT('Ctrl Pts',(0.375139806138853,-0.708769243520481,
-2.84768698950628));
#58844=CARTESIAN_POINT('Ctrl Pts',(0.479297484648239,-0.629459060456024,
-2.84241802773358));
#58845=CARTESIAN_POINT('Ctrl Pts',(0.583455163157625,-0.550148877391566,
-2.83714906596088));
#58846=CARTESIAN_POINT('Ctrl Pts',(0.667505691604525,-0.444432071734316,
-2.83188010418819));
#58847=CARTESIAN_POINT('Ctrl Pts',(0.721296881938309,-0.325077830198219,
-2.82661114241549));
#58848=CARTESIAN_POINT('Ctrl Pts',(0.775088072272093,-0.205723588662121,
-2.82134218064279));
#58849=CARTESIAN_POINT('Ctrl Pts',(0.798619924492762,-0.0727319112471769,
-2.8160732188701));
#58850=CARTESIAN_POINT('Ctrl Pts',(0.789050103241593,0.0578335729031265,
-2.8108042570974));
#58851=CARTESIAN_POINT('Ctrl Pts',(0.779480281990424,0.18839905705343,-2.8055352953247));
#58852=CARTESIAN_POINT('Ctrl Pts',(0.736808787267417,0.316538347939092,
-2.800266333552));
#58853=CARTESIAN_POINT('Ctrl Pts',(0.666189769163409,0.426773920293066,
-2.79499737177931));
#58854=CARTESIAN_POINT('Ctrl Pts',(0.595570751059401,0.537009492647041,
-2.78972841000661));
#58855=CARTESIAN_POINT('Ctrl Pts',(0.497004209574392,0.629341346469327,
-2.78445944823391));
#58856=CARTESIAN_POINT('Ctrl Pts',(0.382395674431353,0.69261701954002,-2.77919048646121));
#58857=CARTESIAN_POINT('Ctrl Pts',(0.267787139288316,0.755892692610712,
-2.77392152468852));
#58858=CARTESIAN_POINT('Ctrl Pts',(0.137136610487249,0.790112184929811,
-2.76865256291582));
#58859=CARTESIAN_POINT('Ctrl Pts',(0.00622493749824819,0.791142236095035,
-2.76338360114312));
#58860=CARTESIAN_POINT('Ctrl Pts',(-0.124686735490752,0.792172287260259,
-2.75811463937043));
#58861=CARTESIAN_POINT('Ctrl Pts',(-0.255859552667686,0.760012897271608,
-2.75284567759773));
#58862=CARTESIAN_POINT('Ctrl Pts',(-0.371449579060123,0.698548493518071,
-2.74757671582503));
#58863=CARTESIAN_POINT('Ctrl Pts',(-0.487039605452563,0.637084089764534,
-2.74230775405233));
#58864=CARTESIAN_POINT('Ctrl Pts',(-0.587046841060505,0.546314672246109,
-2.73703879227964));
#58865=CARTESIAN_POINT('Ctrl Pts',(-0.6593917394364,0.437203981618818,-2.73176983050694));
#58866=CARTESIAN_POINT('Ctrl Pts',(-0.731736637812292,0.32809329099153,
-2.72650086873424));
#58867=CARTESIAN_POINT('Ctrl Pts',(-0.776419198956139,0.200641327255376,
-2.72123190696154));
#58868=CARTESIAN_POINT('Ctrl Pts',(-0.78804236265073,0.0702425956821335,
-2.71596294518885));
#58869=CARTESIAN_POINT('Ctrl Pts',(-0.790123175060398,0.0468982372964096,
-2.71501968040047));
#58870=CARTESIAN_POINT('Ctrl Pts',(-0.791144460334759,0.0234594373683183,
-2.71407641561209));
#58871=CARTESIAN_POINT('Ctrl Pts',(-0.791121074183877,1.86068176132095E-5,
-2.71313315082371));
#58872=CARTESIAN_POINT('Origin',(0.,0.,-1.97));
#58873=CARTESIAN_POINT('',(-0.791117092312022,-1.90463126063522E-5,-2.4846668491763));
#58874=CARTESIAN_POINT('',(-0.79112535605936,-1.80419918197743E-5,-2.51313315082371));
#58875=CARTESIAN_POINT('',(-0.7911,-9.68818082805471E-17,-1.97));
#58876=CARTESIAN_POINT('Ctrl Pts',(-0.791117092312022,-1.90463126063523E-5,
-2.4846668491763));
#58877=CARTESIAN_POINT('Ctrl Pts',(-0.791009985970769,0.106186545028923,
-2.4889405262037));
#58878=CARTESIAN_POINT('Ctrl Pts',(-0.76947514909813,0.212434259761034,
-2.49321420323109));
#58879=CARTESIAN_POINT('Ctrl Pts',(-0.727852076501281,0.310122790665191,
-2.49748788025849));
#58880=CARTESIAN_POINT('Ctrl Pts',(-0.676535522403009,0.430561731573734,
-2.50275684203119));
#58881=CARTESIAN_POINT('Ctrl Pts',(-0.594684631292216,0.537990619875222,
-2.50802580380389));
#58882=CARTESIAN_POINT('Ctrl Pts',(-0.492185904229906,0.61943347200049,
-2.51329476557658));
#58883=CARTESIAN_POINT('Ctrl Pts',(-0.389687177167596,0.700876324125758,
-2.51856372734928));
#58884=CARTESIAN_POINT('Ctrl Pts',(-0.26654061415377,0.756333140074806,
-2.52383268912198));
#58885=CARTESIAN_POINT('Ctrl Pts',(-0.13762068520791,0.77910547268011,-2.52910165089467));
#58886=CARTESIAN_POINT('Ctrl Pts',(-0.00870075626205005,0.801877805285414,
-2.53437061266737));
#58887=CARTESIAN_POINT('Ctrl Pts',(0.125992538615843,0.791965654546976,
-2.53963957444007));
#58888=CARTESIAN_POINT('Ctrl Pts',(0.250190037482034,0.750566276688429,
-2.54490853621277));
#58889=CARTESIAN_POINT('Ctrl Pts',(0.374387536348225,0.709166898829882,
-2.55017749798546));
#58890=CARTESIAN_POINT('Ctrl Pts',(0.488089239202712,0.636280293851226,
-2.55544645975816));
#58891=CARTESIAN_POINT('Ctrl Pts',(0.577561489751059,0.540710196051203,
-2.56071542153086));
#58892=CARTESIAN_POINT('Ctrl Pts',(0.667033740299406,0.445140098251179,
-2.56598438330356));
#58893=CARTESIAN_POINT('Ctrl Pts',(0.732276538541612,0.326886507629788,
-2.57125334507625));
#58894=CARTESIAN_POINT('Ctrl Pts',(0.765409420559802,0.200232888096587,
-2.57652230684895));
#58895=CARTESIAN_POINT('Ctrl Pts',(0.798542302577993,0.073579268563386,
-2.58179126862165));
#58896=CARTESIAN_POINT('Ctrl Pts',(0.799565268372166,-0.0614743798816252,
-2.58706023039434));
#58897=CARTESIAN_POINT('Ctrl Pts',(0.768354757254441,-0.18861536936756,
-2.59232919216704));
#58898=CARTESIAN_POINT('Ctrl Pts',(0.737144246136717,-0.315756358853493,
-2.59759815393974));
#58899=CARTESIAN_POINT('Ctrl Pts',(0.673700258107094,-0.434984689380349,
-2.60286711571244));
#58900=CARTESIAN_POINT('Ctrl Pts',(0.585685984689295,-0.531899161397838,
-2.60813607748513));
#58901=CARTESIAN_POINT('Ctrl Pts',(0.497671711271496,-0.628813633415326,
-2.61340503925783));
#58902=CARTESIAN_POINT('Ctrl Pts',(0.385087152465521,-0.703414246923448,
-2.61867400103053));
#58903=CARTESIAN_POINT('Ctrl Pts',(0.261531028395032,-0.74669023814687,
-2.62394296280322));
#58904=CARTESIAN_POINT('Ctrl Pts',(0.137974904324542,-0.789966229370293,
-2.62921192457592));
#58905=CARTESIAN_POINT('Ctrl Pts',(0.0034472149895384,-0.801917598309016,
-2.63448088634862));
#58906=CARTESIAN_POINT('Ctrl Pts',(-0.12580288061738,-0.781100778251796,
-2.63974984812132));
#58907=CARTESIAN_POINT('Ctrl Pts',(-0.255052976224298,-0.760283958194577,
-2.64501880989402));
#58908=CARTESIAN_POINT('Ctrl Pts',(-0.379025478103131,-0.706698949141413,
-2.65028777166671));
#58909=CARTESIAN_POINT('Ctrl Pts',(-0.482746153783988,-0.626818108835377,
-2.65555673343941));
#58910=CARTESIAN_POINT('Ctrl Pts',(-0.586466829464846,-0.54693726852934,
-2.6608256952121));
#58911=CARTESIAN_POINT('Ctrl Pts',(-0.669935678947729,-0.44076059697043,
-2.6660946569848));
#58912=CARTESIAN_POINT('Ctrl Pts',(-0.723070773278968,-0.321112826568711,
-2.6713636187575));
#58913=CARTESIAN_POINT('Ctrl Pts',(-0.767789792174107,-0.220416084185967,
-2.6757980288971));
#58914=CARTESIAN_POINT('Ctrl Pts',(-0.79102319560355,-0.110177666260909,
-2.6802324390367));
#58915=CARTESIAN_POINT('Ctrl Pts',(-0.791129214786214,1.74461675192319E-5,
-2.6846668491763));
#58916=CARTESIAN_POINT('Ctrl Pts',(-0.791121074183877,1.86068176132095E-5,
-2.71313315082371));
#58917=CARTESIAN_POINT('Ctrl Pts',(-0.791013828155412,-0.107478175922634,
-2.70880745383939));
#58918=CARTESIAN_POINT('Ctrl Pts',(-0.768936855257277,-0.215017663213923,
-2.70448175685507));
#58919=CARTESIAN_POINT('Ctrl Pts',(-0.726322873854477,-0.313687536405388,
-2.70015605987076));
#58920=CARTESIAN_POINT('Ctrl Pts',(-0.674416455118296,-0.43387343750933,
-2.69488709809806));
#58921=CARTESIAN_POINT('Ctrl Pts',(-0.592039851400596,-0.540899740306881,
-2.68961813632536));
#58922=CARTESIAN_POINT('Ctrl Pts',(-0.48914306286637,-0.621839088213354,
-2.68434917455266));
#58923=CARTESIAN_POINT('Ctrl Pts',(-0.386246274332143,-0.702778436119827,
-2.67908021277997));
#58924=CARTESIAN_POINT('Ctrl Pts',(-0.26282930098139,-0.757630829135223,
-2.67381125100727));
#58925=CARTESIAN_POINT('Ctrl Pts',(-0.133799274812547,-0.779770826358582,
-2.66854228923457));
#58926=CARTESIAN_POINT('Ctrl Pts',(-0.00476924864370518,-0.801910823581941,
-2.66327332746188));
#58927=CARTESIAN_POINT('Ctrl Pts',(0.129873830343226,-0.791338425013262,
-2.65800436568918));
#58928=CARTESIAN_POINT('Ctrl Pts',(0.253866865617512,-0.749330636049166,
-2.65273540391648));
#58929=CARTESIAN_POINT('Ctrl Pts',(0.377859900891799,-0.707322847085071,
-2.64746644214378));
#58930=CARTESIAN_POINT('Ctrl Pts',(0.491202892453441,-0.633879667725558,
-2.64219748037109));
#58931=CARTESIAN_POINT('Ctrl Pts',(0.58020551157022,-0.537872059065953,
-2.63692851859839));
#58932=CARTESIAN_POINT('Ctrl Pts',(0.669208130686999,-0.441864450406348,
-2.63165955682569));
#58933=CARTESIAN_POINT('Ctrl Pts',(0.733870377358915,-0.323292412446649,
-2.62639059505299));
#58934=CARTESIAN_POINT('Ctrl Pts',(0.766381910590859,-0.196477873307437,
-2.6211216332803));
#58935=CARTESIAN_POINT('Ctrl Pts',(0.798893443822801,-0.0696633341682291,
-2.6158526715076));
#58936=CARTESIAN_POINT('Ctrl Pts',(0.799254263614774,0.0653937061504918,
-2.6105837097349));
#58937=CARTESIAN_POINT('Ctrl Pts',(0.767420787725851,0.192380150084523,
-2.60531474796221));
#58938=CARTESIAN_POINT('Ctrl Pts',(0.735587311836928,0.319366594018558,
-2.60004578618951));
#58939=CARTESIAN_POINT('Ctrl Pts',(0.671559540267108,0.438282441567903,
-2.59477682441681));
#58940=CARTESIAN_POINT('Ctrl Pts',(0.583071177841939,0.534764236977682,
-2.58950786264412));
#58941=CARTESIAN_POINT('Ctrl Pts',(0.494582815416771,0.631246032387461,
-2.58423890087142));
#58942=CARTESIAN_POINT('Ctrl Pts',(0.381633862136254,0.705293775657674,
-2.57896993909872));
#58943=CARTESIAN_POINT('Ctrl Pts',(0.257867052139174,0.747963482398279,
-2.57370097732602));
#58944=CARTESIAN_POINT('Ctrl Pts',(0.134100242142095,0.790633189138884,
-2.56843201555332));
#58945=CARTESIAN_POINT('Ctrl Pts',(-0.000484424571547404,0.801924859349881,
-2.56316305378063));
#58946=CARTESIAN_POINT('Ctrl Pts',(-0.129630906898198,0.780474609168716,
-2.55789409200793));
#58947=CARTESIAN_POINT('Ctrl Pts',(-0.258777389224849,0.759024358987551,
-2.55262513023523));
#58948=CARTESIAN_POINT('Ctrl Pts',(-0.382485687164508,0.704832188414225,
-2.54735616846254));
#58949=CARTESIAN_POINT('Ctrl Pts',(-0.485813480575784,0.624443792243266,
-2.54208720668984));
#58950=CARTESIAN_POINT('Ctrl Pts',(-0.58914127398706,0.544055396072307,
-2.53681824491714));
#58951=CARTESIAN_POINT('Ctrl Pts',(-0.672088562869954,0.437470774303715,
-2.53154928314444));
#58952=CARTESIAN_POINT('Ctrl Pts',(-0.724636415867464,0.317563934317272,
-2.52628032137175));
#58953=CARTESIAN_POINT('Ctrl Pts',(-0.768342406730885,0.21783298521156,
-2.52189793118907));
#58954=CARTESIAN_POINT('Ctrl Pts',(-0.791018482792984,0.10888590738746,
-2.51751554100639));
#58955=CARTESIAN_POINT('Ctrl Pts',(-0.79112535605936,-1.80419918197743E-5,
-2.51313315082371));
#58956=CARTESIAN_POINT('Origin',(0.,0.,-1.97));
#58957=CARTESIAN_POINT('',(-0.791034957252612,4.30828170744357E-6,-2.2846668491763));
#58958=CARTESIAN_POINT('',(-0.791033810580254,1.8628665638589E-6,-2.31313315082371));
#58959=CARTESIAN_POINT('',(-0.7911,-9.68818082805471E-17,-1.97));
#58960=CARTESIAN_POINT('Ctrl Pts',(-0.791034957252612,4.30828170744357E-6,
-2.2846668491763));
#58961=CARTESIAN_POINT('Ctrl Pts',(-0.791046599626097,0.0607545590049239,
-2.2871106898253));
#58962=CARTESIAN_POINT('Ctrl Pts',(-0.784135866741558,0.12150220338301,
-2.2895545304743));
#58963=CARTESIAN_POINT('Ctrl Pts',(-0.770273514124328,0.180619777421388,
-2.2919983711233));
#58964=CARTESIAN_POINT('Ctrl Pts',(-0.740386047423214,0.30807826692241,
-2.297267332896));
#58965=CARTESIAN_POINT('Ctrl Pts',(-0.678184609475154,0.427959522898974,
-2.30253629466869));
#58966=CARTESIAN_POINT('Ctrl Pts',(-0.591182308249092,0.525783481074166,
-2.30780525644139));
#58967=CARTESIAN_POINT('Ctrl Pts',(-0.504180007023029,0.623607439249358,
-2.31307421821409));
#58968=CARTESIAN_POINT('Ctrl Pts',(-0.392376842518966,0.699374099623178,
-2.31834317998679));
#58969=CARTESIAN_POINT('Ctrl Pts',(-0.26927715280204,0.743931855438399,
-2.32361214175948));
#58970=CARTESIAN_POINT('Ctrl Pts',(-0.146177463085118,0.788489611253618,
-2.32888110353218));
#58971=CARTESIAN_POINT('Ctrl Pts',(-0.0117812481553361,0.80183846251024,
-2.33415006530488));
#58972=CARTESIAN_POINT('Ctrl Pts',(0.117678213357513,0.782366045184846,
-2.33941902707757));
#58973=CARTESIAN_POINT('Ctrl Pts',(0.247137674870368,0.76289362785945,-2.34468798885027));
#58974=CARTESIAN_POINT('Ctrl Pts',(0.371660382966294,0.710599941952033,
-2.34995695062297));
#58975=CARTESIAN_POINT('Ctrl Pts',(0.476205647568452,0.631801370512207,
-2.35522591239567));
#58976=CARTESIAN_POINT('Ctrl Pts',(0.580750912170611,0.553002799072381,
-2.36049487416836));
#58977=CARTESIAN_POINT('Ctrl Pts',(0.665318733279004,0.44769934210015,-2.36576383594106));
#58978=CARTESIAN_POINT('Ctrl Pts',(0.719694440756652,0.328610259275577,
-2.37103279771376));
#58979=CARTESIAN_POINT('Ctrl Pts',(0.774070148234299,0.209521176451008,
-2.37630175948645));
#58980=CARTESIAN_POINT('Ctrl Pts',(0.7982537420812,0.0766464677740978,-2.38157072125915));
#58981=CARTESIAN_POINT('Ctrl Pts',(0.789324165202169,-0.0539643658824301,
-2.38683968303185));
#58982=CARTESIAN_POINT('Ctrl Pts',(0.780394588323137,-0.18457519953896,
-2.39210864480455));
#58983=CARTESIAN_POINT('Ctrl Pts',(0.738351840718173,-0.312922158175111,
-2.39737760657724));
#58984=CARTESIAN_POINT('Ctrl Pts',(0.668274128172985,-0.423502633016406,
-2.40264656834994));
#58985=CARTESIAN_POINT('Ctrl Pts',(0.598196415627797,-0.534083107857701,
-2.40791553012264));
#58986=CARTESIAN_POINT('Ctrl Pts',(0.500083738142384,-0.626897098904138,
-2.41318449189533));
#58987=CARTESIAN_POINT('Ctrl Pts',(0.385786804693692,-0.690733908159592,
-2.41845345366803));
#58988=CARTESIAN_POINT('Ctrl Pts',(0.271489871244999,-0.754570717415047,
-2.42372241544073));
#58989=CARTESIAN_POINT('Ctrl Pts',(0.141008681833027,-0.789430344879519,
-2.42899137721343));
#58990=CARTESIAN_POINT('Ctrl Pts',(0.0101036319776801,-0.791102210323073,
-2.43426033898612));
#58991=CARTESIAN_POINT('Ctrl Pts',(-0.120801417877665,-0.792774075766627,
-2.43952930075882));
#58992=CARTESIAN_POINT('Ctrl Pts',(-0.252130328176385,-0.761258179189264,
-2.44479826253152));
#58993=CARTESIAN_POINT('Ctrl Pts',(-0.368020309969101,-0.70036122251838,
-2.45006722430422));
#58994=CARTESIAN_POINT('Ctrl Pts',(-0.483910291761818,-0.639464265847496,
-2.45533618607691));
#58995=CARTESIAN_POINT('Ctrl Pts',(-0.58436134504853,-0.549186249083092,
-2.46060514784961));
#58996=CARTESIAN_POINT('Ctrl Pts',(-0.657240316097855,-0.440431558193533,
-2.46587410962231));
#58997=CARTESIAN_POINT('Ctrl Pts',(-0.730119287147181,-0.331676867303971,
-2.471143071395));
#58998=CARTESIAN_POINT('Ctrl Pts',(-0.775426175959118,-0.204445502289255,
-2.4764120331677));
#58999=CARTESIAN_POINT('Ctrl Pts',(-0.78768851182221,-0.0741053230240971,
-2.4816809949404));
#59000=CARTESIAN_POINT('Ctrl Pts',(-0.790004815555806,-0.0494846106867235,
-2.4826762796857));
#59001=CARTESIAN_POINT('Ctrl Pts',(-0.791142036009661,-0.0247529708113624,
-2.483671564431));
#59002=CARTESIAN_POINT('Ctrl Pts',(-0.791117092312022,-1.90463126063523E-5,
-2.4846668491763));
#59003=CARTESIAN_POINT('Ctrl Pts',(-0.79112535605936,-1.80419918197743E-5,
-2.51313315082371));
#59004=CARTESIAN_POINT('Ctrl Pts',(-0.791146976863933,-0.0220496602493374,
-2.51224657923369));
#59005=CARTESIAN_POINT('Ctrl Pts',(-0.790244917210455,-0.0440795134067749,
-2.51136000764367));
#59006=CARTESIAN_POINT('Ctrl Pts',(-0.78840643244089,-0.0660309387040414,
-2.51047343605365));
#59007=CARTESIAN_POINT('Ctrl Pts',(-0.777480178904677,-0.196489913534617,
-2.50520447428096));
#59008=CARTESIAN_POINT('Ctrl Pts',(-0.733479254720125,-0.324178804991475,
-2.49993551250826));
#59009=CARTESIAN_POINT('Ctrl Pts',(-0.66171838740861,-0.433674490079434,
-2.49466655073556));
#59010=CARTESIAN_POINT('Ctrl Pts',(-0.589957520097096,-0.543170175167392,
-2.48939758896287));
#59011=CARTESIAN_POINT('Ctrl Pts',(-0.49043670965862,-0.634472653886452,
-2.48412862719017));
#59012=CARTESIAN_POINT('Ctrl Pts',(-0.375176748837641,-0.69655379886404,
-2.47885966541747));
#59013=CARTESIAN_POINT('Ctrl Pts',(-0.259916788016662,-0.758634943841629,
-2.47359070364477));
#59014=CARTESIAN_POINT('Ctrl Pts',(-0.128917676813181,-0.791494755077747,
-2.46832174187208));
#59015=CARTESIAN_POINT('Ctrl Pts',(0.00199763117598858,-0.791164203594926,
-2.46305278009938));
#59016=CARTESIAN_POINT('Ctrl Pts',(0.13291293916516,-0.790833652112105,
-2.45778381832668));
#59017=CARTESIAN_POINT('Ctrl Pts',(0.26374444394002,-0.757312737910344,
-2.45251485655398));
#59018=CARTESIAN_POINT('Ctrl Pts',(0.378689436535325,-0.694650342429101,
-2.44724589478129));
#59019=CARTESIAN_POINT('Ctrl Pts',(0.49363442913063,-0.631987946947858,
-2.44197693300859));
#59020=CARTESIAN_POINT('Ctrl Pts',(0.59269290954638,-0.540184070187133,
-2.43670797123589));
#59021=CARTESIAN_POINT('Ctrl Pts',(0.663899928367349,-0.430327401746784,
-2.4314390094632));
#59022=CARTESIAN_POINT('Ctrl Pts',(0.735106947188317,-0.320470733306435,
-2.4261700476905));
#59023=CARTESIAN_POINT('Ctrl Pts',(0.778462504414503,-0.192561273186463,
-2.4209010859178));
#59024=CARTESIAN_POINT('Ctrl Pts',(0.788729824285738,-0.0620487861484625,
-2.4156321241451));
#59025=CARTESIAN_POINT('Ctrl Pts',(0.798997144156974,0.0684637008895377,
-2.41036316237241));
#59026=CARTESIAN_POINT('Ctrl Pts',(0.776176226673258,0.201579214845565,
-2.40509420059971));
#59027=CARTESIAN_POINT('Ctrl Pts',(0.723023535714875,0.321219168765922,
-2.39982523882701));
#59028=CARTESIAN_POINT('Ctrl Pts',(0.669870844756492,0.440859122686279,
-2.39455627705432));
#59029=CARTESIAN_POINT('Ctrl Pts',(0.586386380323441,0.547023516570965,
-2.38928731528162));
#59030=CARTESIAN_POINT('Ctrl Pts',(0.48265395744808,0.626889100989973,-2.38401835350892));
#59031=CARTESIAN_POINT('Ctrl Pts',(0.378921534572719,0.706754685408981,
-2.37874939173623));
#59032=CARTESIAN_POINT('Ctrl Pts',(0.254941153255048,0.760321460362311,
-2.37348042996353));
#59033=CARTESIAN_POINT('Ctrl Pts',(0.125687997696566,0.781119270544093,
-2.36821146819083));
#59034=CARTESIAN_POINT('Ctrl Pts',(-0.00356515786191522,0.801917080725876,
-2.36294250641813));
#59035=CARTESIAN_POINT('Ctrl Pts',(-0.138091087661207,0.78994592613611,
-2.35767354464544));
#59036=CARTESIAN_POINT('Ctrl Pts',(-0.261640845237265,0.746651763330027,
-2.35240458287274));
#59037=CARTESIAN_POINT('Ctrl Pts',(-0.385190602813323,0.703357600523944,
-2.34713562110004));
#59038=CARTESIAN_POINT('Ctrl Pts',(-0.497764188166149,0.628740429501544,
-2.34186665932734));
#59039=CARTESIAN_POINT('Ctrl Pts',(-0.585764206619544,0.531813013966079,
-2.33659769755465));
#59040=CARTESIAN_POINT('Ctrl Pts',(-0.673764225072938,0.434885598430616,
-2.33132873578195));
#59041=CARTESIAN_POINT('Ctrl Pts',(-0.737190676626901,0.315647938382089,
-2.32605977400925));
#59042=CARTESIAN_POINT('Ctrl Pts',(-0.768382487931173,0.188502360253156,
-2.32079081223656));
#59043=CARTESIAN_POINT('Ctrl Pts',(-0.783493392136204,0.126906557673506,
-2.31823825843227));
#59044=CARTESIAN_POINT('Ctrl Pts',(-0.79103905925902,0.0634548238769548,
-2.31568570462799));
#59045=CARTESIAN_POINT('Ctrl Pts',(-0.791033810580254,1.8628665638589E-6,
-2.31313315082371));
#59046=CARTESIAN_POINT('Origin',(0.,0.,-1.97));
#59047=CARTESIAN_POINT('',(-0.791144406175107,1.41356307707188E-5,-2.0846668491763));
#59048=CARTESIAN_POINT('',(-0.791137191533222,1.59212896634344E-5,-2.11313315082371));
#59049=CARTESIAN_POINT('',(-0.7911,-9.68818082805471E-17,-1.97));
#59050=CARTESIAN_POINT('Ctrl Pts',(-0.791144406175107,1.41356307707188E-5,
-2.0846668491763));
#59051=CARTESIAN_POINT('Ctrl Pts',(-0.791157104778467,0.0152712971938506,
-2.0852808534469));
#59052=CARTESIAN_POINT('Ctrl Pts',(-0.790724724866188,0.0305277394974985,
-2.0858948577175));
#59053=CARTESIAN_POINT('Ctrl Pts',(-0.78984238020639,0.0457581138935725,
-2.08650886198811));
#59054=CARTESIAN_POINT('Ctrl Pts',(-0.782270706025277,0.176454697482384,
-2.0917778237608));
#59055=CARTESIAN_POINT('Ctrl Pts',(-0.741564121327834,0.305231668946985,
-2.0970467855335));
#59056=CARTESIAN_POINT('Ctrl Pts',(-0.672639441158341,0.416534479671716,
-2.1023157473062));
#59057=CARTESIAN_POINT('Ctrl Pts',(-0.60371476098885,0.527837290396444,
-2.1075847090789));
#59058=CARTESIAN_POINT('Ctrl Pts',(-0.50657198534731,0.621665940381303,
-2.11285367085159));
#59059=CARTESIAN_POINT('Ctrl Pts',(-0.392944671943546,0.686687174300185,
-2.11812263262429));
#59060=CARTESIAN_POINT('Ctrl Pts',(-0.279317358539779,0.751708408219068,
-2.12339159439699));
#59061=CARTESIAN_POINT('Ctrl Pts',(-0.149205507373787,0.787922226071974,
-2.12866055616968));
#59062=CARTESIAN_POINT('Ctrl Pts',(-0.0183249028083912,0.790954479407162,
-2.13392951794238));
#59063=CARTESIAN_POINT('Ctrl Pts',(0.112555701757004,0.793986732742351,
-2.13919847971508));
#59064=CARTESIAN_POINT('Ctrl Pts',(0.244205059721803,0.763837421559821,
-2.14446744148778));
#59065=CARTESIAN_POINT('Ctrl Pts',(0.360721676312565,0.70414818241294,-2.14973640326047));
#59066=CARTESIAN_POINT('Ctrl Pts',(0.47723829290333,0.644458943266057,-2.15500536503317));
#59067=CARTESIAN_POINT('Ctrl Pts',(0.578622168120057,0.555229776154819,
-2.16027432680587));
#59068=CARTESIAN_POINT('Ctrl Pts',(0.65262747572559,0.447238379933159,-2.16554328857856));
#59069=CARTESIAN_POINT('Ctrl Pts',(0.726632783331119,0.339246983711505,
-2.17081225035126));
#59070=CARTESIAN_POINT('Ctrl Pts',(0.773259523325458,0.212493358379431,
-2.17608121212396));
#59071=CARTESIAN_POINT('Ctrl Pts',(0.78687580449558,0.0822876592000658,
-2.18135017389666));
#59072=CARTESIAN_POINT('Ctrl Pts',(0.800492085665702,-0.0479180399793047,
-2.18661913566935));
#59073=CARTESIAN_POINT('Ctrl Pts',(0.781097908011607,-0.181575813005962,
-2.19188809744205));
#59074=CARTESIAN_POINT('Ctrl Pts',(0.73103583073274,-0.302541575229069,
-2.19715705921475));
#59075=CARTESIAN_POINT('Ctrl Pts',(0.680973753453872,-0.423507337452174,
-2.20242602098744));
#59076=CARTESIAN_POINT('Ctrl Pts',(0.600243776550234,-0.531781088871725,
-2.20769498276014));
#59077=CARTESIAN_POINT('Ctrl Pts',(0.498597009526942,-0.614284797669602,
-2.21296394453284));
#59078=CARTESIAN_POINT('Ctrl Pts',(0.39695024250365,-0.696788506467478,
-2.21823290630554));
#59079=CARTESIAN_POINT('Ctrl Pts',(0.274386685360704,-0.753522172643679,
-2.22350186807823));
#59080=CARTESIAN_POINT('Ctrl Pts',(0.145710388747892,-0.777633122473658,
-2.22877082985093));
#59081=CARTESIAN_POINT('Ctrl Pts',(0.0170340921350798,-0.801744072303636,
-2.23403979162363));
#59082=CARTESIAN_POINT('Ctrl Pts',(-0.117754943947599,-0.793232305787391,
-2.23930875339633));
#59083=CARTESIAN_POINT('Ctrl Pts',(-0.242375993289851,-0.753125931324868,
-2.24457771516902));
#59084=CARTESIAN_POINT('Ctrl Pts',(-0.3669970426321,-0.713019556862346,
-2.24984667694172));
#59085=CARTESIAN_POINT('Ctrl Pts',(-0.481450105233923,-0.641318574453546,
-2.25511563871442));
#59086=CARTESIAN_POINT('Ctrl Pts',(-0.571910770517838,-0.546683510930122,
-2.26038460048711));
#59087=CARTESIAN_POINT('Ctrl Pts',(-0.662371435801757,-0.452048447406696,
-2.26565356225981));
#59088=CARTESIAN_POINT('Ctrl Pts',(-0.728839703767767,-0.334479302768643,
-2.27092252403251));
#59089=CARTESIAN_POINT('Ctrl Pts',(-0.763287090023688,-0.208176868936877,
-2.27619148580521));
#59090=CARTESIAN_POINT('Ctrl Pts',(-0.781757149736784,-0.140455809421626,
-2.2790166069289));
#59091=CARTESIAN_POINT('Ctrl Pts',(-0.791021498471951,-0.0702240090425869,
-2.2818417280526));
#59092=CARTESIAN_POINT('Ctrl Pts',(-0.791034957252612,4.30828170744357E-6,
-2.2846668491763));
#59093=CARTESIAN_POINT('Ctrl Pts',(-0.791033810580254,1.8628665638589E-6,
-2.31313315082371));
#59094=CARTESIAN_POINT('Ctrl Pts',(-0.791028224977005,-0.0675242862860532,
-2.31041674285529));
#59095=CARTESIAN_POINT('Ctrl Pts',(-0.782471188428489,-0.13505182526465,
-2.30770033488688));
#59096=CARTESIAN_POINT('Ctrl Pts',(-0.765379960987778,-0.200345458892024,
-2.30498392691846));
#59097=CARTESIAN_POINT('Ctrl Pts',(-0.732228451685532,-0.326994203698933,
-2.29971496514576));
#59098=CARTESIAN_POINT('Ctrl Pts',(-0.66696826202646,-0.445238197103409,
-2.29444600337307));
#59099=CARTESIAN_POINT('Ctrl Pts',(-0.577481956580721,-0.540795134412294,
-2.28917704160037));
#59100=CARTESIAN_POINT('Ctrl Pts',(-0.487995651134981,-0.636352071721179,
-2.28390807982767));
#59101=CARTESIAN_POINT('Ctrl Pts',(-0.374283229902573,-0.709221952934474,
-2.27863911805498));
#59102=CARTESIAN_POINT('Ctrl Pts',(-0.2500796438157,-0.75060306376228,-2.27337015628228));
#59103=CARTESIAN_POINT('Ctrl Pts',(-0.125876057728828,-0.791984174590086,
-2.26810119450958));
#59104=CARTESIAN_POINT('Ctrl Pts',(0.00881869321251119,-0.801876515032405,
-2.26283223273689));
#59105=CARTESIAN_POINT('Ctrl Pts',(0.137735271191444,-0.779085221686388,
-2.25756327096419));
#59106=CARTESIAN_POINT('Ctrl Pts',(0.266651849170376,-0.756293928340371,
-2.25229430919149));
#59107=CARTESIAN_POINT('Ctrl Pts',(0.389790254186903,-0.700819001206018,
-2.24702534741879));
#59108=CARTESIAN_POINT('Ctrl Pts',(0.492277001599317,-0.619361075041607,
-2.2417563856461));
#59109=CARTESIAN_POINT('Ctrl Pts',(0.59476374901173,-0.537903148877196,
-2.2364874238734));
#59110=CARTESIAN_POINT('Ctrl Pts',(0.676598838820031,-0.430462223682727,
-2.2312184621007));
#59111=CARTESIAN_POINT('Ctrl Pts',(0.727897678550787,-0.310015736924248,
-2.225949500328));
#59112=CARTESIAN_POINT('Ctrl Pts',(0.779196518281544,-0.189569250165767,
-2.22068053855531));
#59113=CARTESIAN_POINT('Ctrl Pts',(0.799959107934757,-0.0561172018432798,
-2.21541157678261));
#59114=CARTESIAN_POINT('Ctrl Pts',(0.7876776023074,0.074221172205609,-2.21014261500991));
#59115=CARTESIAN_POINT('Ctrl Pts',(0.775396096680042,0.204559546254496,
-2.20487365323722));
#59116=CARTESIAN_POINT('Ctrl Pts',(0.730070495772115,0.331784246029781,
-2.19960469146452));
#59117=CARTESIAN_POINT('Ctrl Pts',(0.657175530467858,0.440528216729188,
-2.19433572969182));
#59118=CARTESIAN_POINT('Ctrl Pts',(0.584280565163601,0.549272187428595,
-2.18906676791912));
#59119=CARTESIAN_POINT('Ctrl Pts',(0.483816235463015,0.639535429052127,
-2.18379780614643));
#59120=CARTESIAN_POINT('Ctrl Pts',(0.367917298712036,0.70041534027229,-2.17852884437373));
#59121=CARTESIAN_POINT('Ctrl Pts',(0.25201836196106,0.761295251492451,-2.17325988260103));
#59122=CARTESIAN_POINT('Ctrl Pts',(0.120684818159691,0.792791832309247,
-2.16799092082833));
#59123=CARTESIAN_POINT('Ctrl Pts',(-0.0102199840770827,0.791100713882735,
-2.16272195905564));
#59124=CARTESIAN_POINT('Ctrl Pts',(-0.14112478631386,0.789409595456224,
-2.15745299728294));
#59125=CARTESIAN_POINT('Ctrl Pts',(-0.271600846986045,0.754530777786403,
-2.15218403551024));
#59126=CARTESIAN_POINT('Ctrl Pts',(-0.385888390057411,0.690677159025263,
-2.14691507373755));
#59127=CARTESIAN_POINT('Ctrl Pts',(-0.500175933128777,0.626823540264123,
-2.14164611196485));
#59128=CARTESIAN_POINT('Ctrl Pts',(-0.598274958599326,0.533995120411663,
-2.13637715019215));
#59129=CARTESIAN_POINT('Ctrl Pts',(-0.668336406474275,0.42340434027223,
-2.13110818841946));
#59130=CARTESIAN_POINT('Ctrl Pts',(-0.738397854349223,0.312813560132798,
-2.12583922664676));
#59131=CARTESIAN_POINT('Ctrl Pts',(-0.780421724628571,0.184460419706392,
-2.12057026487406));
#59132=CARTESIAN_POINT('Ctrl Pts',(-0.789332091656947,0.0538482744456927,
-2.11530130310136));
#59133=CARTESIAN_POINT('Ctrl Pts',(-0.790554282631232,0.0359328524926724,
-2.11457858567548));
#59134=CARTESIAN_POINT('Ctrl Pts',(-0.791153467809793,0.0179749290533651,
-2.11385586824959));
#59135=CARTESIAN_POINT('Ctrl Pts',(-0.791137191533222,1.59212896634344E-5,
-2.11313315082371));
#59136=CARTESIAN_POINT('Origin',(0.,0.,-1.97));
#59137=CARTESIAN_POINT('',(-0.791099975804956,-2.00585267497999E-5,-1.8846668491763));
#59138=CARTESIAN_POINT('',(-0.791108422200728,-1.97323857704162E-5,-1.91313315082371));
#59139=CARTESIAN_POINT('',(-0.7911,-9.68818082805471E-17,-1.97));
#59140=CARTESIAN_POINT('Ctrl Pts',(-0.791099975804956,-2.00585267497999E-5,
-1.8846668491763));
#59141=CARTESIAN_POINT('Ctrl Pts',(-0.79099794526589,0.100710966905559,
-1.8887199788412));
#59142=CARTESIAN_POINT('Ctrl Pts',(-0.77168153183872,0.201480004270866,
-1.8927731085061));
#59143=CARTESIAN_POINT('Ctrl Pts',(-0.734140622488718,0.294927680913593,
-1.89682623817101));
#59144=CARTESIAN_POINT('Ctrl Pts',(-0.685338429459896,0.416407198393984,
-1.9020951999437));
#59145=CARTESIAN_POINT('Ctrl Pts',(-0.60573808677214,0.525514117795622,
-1.9073641617164));
#59146=CARTESIAN_POINT('Ctrl Pts',(-0.504954259113385,0.609069771668604,
-1.9126331234891));
#59147=CARTESIAN_POINT('Ctrl Pts',(-0.404170431454624,0.692625425541591,
-1.91790208526179));
#59148=CARTESIAN_POINT('Ctrl Pts',(-0.282203118824861,0.750629813885918,
-1.92317104703449));
#59149=CARTESIAN_POINT('Ctrl Pts',(-0.153784353451944,0.776076776608192,
-1.92844000880719));
#59150=CARTESIAN_POINT('Ctrl Pts',(-0.0253655880790338,0.801523739330464,
-1.93370897057989));
#59151=CARTESIAN_POINT('Ctrl Pts',(0.10950463003703,0.794413276430685,-1.93897793235258));
#59152=CARTESIAN_POINT('Ctrl Pts',(0.234535768974027,0.755604237434488,
-1.94424689412528));
#59153=CARTESIAN_POINT('Ctrl Pts',(0.359566907911032,0.716795198438288,
-1.94951585589798));
#59154=CARTESIAN_POINT('Ctrl Pts',(0.47475896766897,0.646287583345665,-1.95478481767068));
#59155=CARTESIAN_POINT('Ctrl Pts',(0.56619827662422,0.552597776058642,-1.96005377944337));
#59156=CARTESIAN_POINT('Ctrl Pts',(0.657637585579464,0.458907968771624,
-1.96532274121607));
#59157=CARTESIAN_POINT('Ctrl Pts',(0.725324143732022,0.342035969290208,
-1.97059170298877));
#59158=CARTESIAN_POINT('Ctrl Pts',(0.761082313408198,0.216098363655112,
-1.97586066476146));
#59159=CARTESIAN_POINT('Ctrl Pts',(0.796840483084376,0.0901607580200119,
-1.98112962653416));
#59160=CARTESIAN_POINT('Ctrl Pts',(0.800670264284169,-0.0448424537687684,
-1.98639858830686));
#59161=CARTESIAN_POINT('Ctrl Pts',(0.772109070279671,-0.172604675918861,
-1.99166755007956));
#59162=CARTESIAN_POINT('Ctrl Pts',(0.743547876275173,-0.300366898068953,
-1.99693651185225));
#59163=CARTESIAN_POINT('Ctrl Pts',(0.682595707066384,-0.420888130580358,
-2.00220547362495));
#59164=CARTESIAN_POINT('Ctrl Pts',(0.596614775542808,-0.519611008506553,
-2.00747443539765));
#59165=CARTESIAN_POINT('Ctrl Pts',(0.510633844019231,-0.618333886432751,
-2.01274339717035));
#59166=CARTESIAN_POINT('Ctrl Pts',(0.399624150180865,-0.695258409773738,
-2.01801235894304));
#59167=CARTESIAN_POINT('Ctrl Pts',(0.276994191369901,-0.741093117296691,
-2.02328132071574));
#59168=CARTESIAN_POINT('Ctrl Pts',(0.154364232558945,-0.78692782481964,
-2.02855028248844));
#59169=CARTESIAN_POINT('Ctrl Pts',(0.0201140087753928,-0.80167271652456,
-2.03381924426113));
#59170=CARTESIAN_POINT('Ctrl Pts',(-0.109540835143368,-0.783546805234561,
-2.03908820603383));
#59171=CARTESIAN_POINT('Ctrl Pts',(-0.239195679062133,-0.765420893944561,
-2.04435716780653));
#59172=CARTESIAN_POINT('Ctrl Pts',(-0.364255143116106,-0.71442417965964,
-2.04962612957922));
#59173=CARTESIAN_POINT('Ctrl Pts',(-0.469613704234257,-0.636716388474941,
-2.05489509135192));
#59174=CARTESIAN_POINT('Ctrl Pts',(-0.574972265352409,-0.559008597290241,
-2.06016405312462));
#59175=CARTESIAN_POINT('Ctrl Pts',(-0.66062992353474,-0.454589729205763,
-2.06543301489732));
#59176=CARTESIAN_POINT('Ctrl Pts',(-0.716240370793513,-0.336072197307012,
-2.07070197667002));
#59177=CARTESIAN_POINT('Ctrl Pts',(-0.765370404342706,-0.231365786814431,
-2.07535693417211));
#59178=CARTESIAN_POINT('Ctrl Pts',(-0.791048134110227,-0.115655155413321,
-2.0800118916742));
#59179=CARTESIAN_POINT('Ctrl Pts',(-0.791144406175107,1.41356307707188E-5,
-2.0846668491763));
#59180=CARTESIAN_POINT('Ctrl Pts',(-0.791137191533222,1.59212896634344E-5,
-2.11313315082371));
#59181=CARTESIAN_POINT('Ctrl Pts',(-0.791034805832124,-0.112954977979898,
-2.10858690647689));
#59182=CARTESIAN_POINT('Ctrl Pts',(-0.766578473242961,-0.225968784207304,
-2.10404066213008));
#59183=CARTESIAN_POINT('Ctrl Pts',(-0.719646100543896,-0.328716104796029,
-2.09949441778327));
#59184=CARTESIAN_POINT('Ctrl Pts',(-0.665252878625066,-0.447797188682058,
-2.09422545601057));
#59185=CARTESIAN_POINT('Ctrl Pts',(-0.580669571010003,-0.553088206359121,
-2.08895649423788));
#59186=CARTESIAN_POINT('Ctrl Pts',(-0.476112718400113,-0.631871400648869,
-2.08368753246518));
#59187=CARTESIAN_POINT('Ctrl Pts',(-0.371555865790223,-0.710654594938617,
-2.07841857069248));
#59188=CARTESIAN_POINT('Ctrl Pts',(-0.247025468185505,-0.762929965841049,
-2.07314960891978));
#59189=CARTESIAN_POINT('Ctrl Pts',(-0.117563144453371,-0.782383342516024,
-2.06788064714709));
#59190=CARTESIAN_POINT('Ctrl Pts',(0.0118991792787638,-0.801836719190998,
-2.06261168537439));
#59191=CARTESIAN_POINT('Ctrl Pts',(0.146293429138315,-0.788468101638515,
-2.05734272360169));
#59192=CARTESIAN_POINT('Ctrl Pts',(0.269386563849886,-0.743892241388133,
-2.052073761829));
#59193=CARTESIAN_POINT('Ctrl Pts',(0.392479698561456,-0.699316381137751,
-2.0468048000563));
#59194=CARTESIAN_POINT('Ctrl Pts',(0.504271718125046,-0.623533278189469,
-2.0415358382836));
#59195=CARTESIAN_POINT('Ctrl Pts',(0.591259630636372,-0.525696525345232,
-2.0362668765109));
#59196=CARTESIAN_POINT('Ctrl Pts',(0.678247543147696,-0.427859772500998,
-2.03099791473821));
#59197=CARTESIAN_POINT('Ctrl Pts',(0.740431348606757,-0.307969369760809,
-2.02572895296551));
#59198=CARTESIAN_POINT('Ctrl Pts',(0.77030006881521,-0.180506486209202,
-2.02045999119281));
#59199=CARTESIAN_POINT('Ctrl Pts',(0.800168789023663,-0.0530436026575909,
-2.01519102942012));
#59200=CARTESIAN_POINT('Ctrl Pts',(0.797722423981506,0.0819917617054397,
-2.00992206764742));
#59201=CARTESIAN_POINT('Ctrl Pts',(0.7632564621099,0.208289127483382,-2.00465310587472));
#59202=CARTESIAN_POINT('Ctrl Pts',(0.728790500238293,0.334586493261325,
-1.99938414410202));
#59203=CARTESIAN_POINT('Ctrl Pts',(0.662304941537236,0.452145860454179,
-1.99411518232933));
#59204=CARTESIAN_POINT('Ctrl Pts',(0.571830358890167,0.546767618126615,
-1.98884622055663));
#59205=CARTESIAN_POINT('Ctrl Pts',(0.481355776243099,0.641389375799051,
-1.98357725878393));
#59206=CARTESIAN_POINT('Ctrl Pts',(0.366892169650018,0.713073523951068,
-1.97830829701123));
#59207=CARTESIAN_POINT('Ctrl Pts',(0.242265223262576,0.753161569105755,
-1.97303933523854));
#59208=CARTESIAN_POINT('Ctrl Pts',(0.117638276875135,0.793249614260442,
-1.96777037346584));
#59209=CARTESIAN_POINT('Ctrl Pts',(-0.0171520093066676,0.8017415564178,
-1.96250141169314));
#59210=CARTESIAN_POINT('Ctrl Pts',(-0.145824758077158,0.777611681697264,
-1.95723244992045));
#59211=CARTESIAN_POINT('Ctrl Pts',(-0.274497506847648,0.753481806976729,
-1.95196348814775));
#59212=CARTESIAN_POINT('Ctrl Pts',(-0.397052718206826,0.696730115378302,
-1.94669452637505));
#59213=CARTESIAN_POINT('Ctrl Pts',(-0.498687349564794,0.614211457858244,
-1.94142556460235));
#59214=CARTESIAN_POINT('Ctrl Pts',(-0.600321980922761,0.531692800338187,
-1.93615660282966));
#59215=CARTESIAN_POINT('Ctrl Pts',(-0.681036032279518,0.4234071768965,-1.93088764105696));
#59216=CARTESIAN_POINT('Ctrl Pts',(-0.731080317724594,0.302434053333974,
-1.92561867928426));
#59217=CARTESIAN_POINT('Ctrl Pts',(-0.770609253225731,0.206879910515361,
-1.92145683646408));
#59218=CARTESIAN_POINT('Ctrl Pts',(-0.791003045630741,0.103409922135896,
-1.91729499364389));
#59219=CARTESIAN_POINT('Ctrl Pts',(-0.791108422200728,-1.97323857704162E-5,
-1.91313315082371));
#59220=CARTESIAN_POINT('Origin',(0.,0.,-1.97));
#59221=CARTESIAN_POINT('',(-0.791040023293942,9.038082159879E-6,-1.6846668491763));
#59222=CARTESIAN_POINT('',(-0.791037072492376,6.75761974000038E-6,-1.7131331508237));
#59223=CARTESIAN_POINT('',(-0.7911,-9.68818082805471E-17,-1.97));
#59224=CARTESIAN_POINT('Ctrl Pts',(-0.791040023293942,9.038082159879E-6,
-1.6846668491763));
#59225=CARTESIAN_POINT('Ctrl Pts',(-0.791062421323145,0.0552757956668374,
-1.6868901424628));
#59226=CARTESIAN_POINT('Ctrl Pts',(-0.785351984343387,0.110537990535984,
-1.68911343574931));
#59227=CARTESIAN_POINT('Ctrl Pts',(-0.773861227453778,0.164570930607212,
-1.69133672903581));
#59228=CARTESIAN_POINT('Ctrl Pts',(-0.746629391169211,0.292623085232824,
-1.69660569080851));
#59229=CARTESIAN_POINT('Ctrl Pts',(-0.686933074418255,0.413771276237449,
-1.70187465258121));
#59230=CARTESIAN_POINT('Ctrl Pts',(-0.601982799785173,0.513382410411572,
-1.7071436143539));
#59231=CARTESIAN_POINT('Ctrl Pts',(-0.517032525152087,0.612993544585701,
-1.7124125761266));
#59232=CARTESIAN_POINT('Ctrl Pts',(-0.406828292636872,0.691067621929326,
-1.7176815378993));
#59233=CARTESIAN_POINT('Ctrl Pts',(-0.284681310546525,0.738174330346637,
-1.722950499672));
#59234=CARTESIAN_POINT('Ctrl Pts',(-0.162534328456181,0.785281038763947,
-1.72821946144469));
#59235=CARTESIAN_POINT('Ctrl Pts',(-0.0284445967907067,0.801420378254945,
-1.73348842321739));
#59236=CARTESIAN_POINT('Ctrl Pts',(0.101391624929814,0.784642930861729,
-1.73875738499009));
#59237=CARTESIAN_POINT('Ctrl Pts',(0.231227846650335,0.767865483468514,
-1.74402634676279));
#59238=CARTESIAN_POINT('Ctrl Pts',(0.356810558425899,0.718171249191085,
-1.74929530853548));
#59239=CARTESIAN_POINT('Ctrl Pts',(0.462971035806919,0.641562631830331,
-1.75456427030818));
#59240=CARTESIAN_POINT('Ctrl Pts',(0.569131513187935,0.56495401446958,-1.75983323208088));
#59241=CARTESIAN_POINT('Ctrl Pts',(0.655869756174406,0.461431014025508,
-1.76510219385357));
#59242=CARTESIAN_POINT('Ctrl Pts',(0.712708936479214,0.343497834665462,
-1.77037115562627));
#59243=CARTESIAN_POINT('Ctrl Pts',(0.769548116784024,0.225564655305408,
-1.77564011739897));
#59244=CARTESIAN_POINT('Ctrl Pts',(0.796488234407167,0.0932212970293808,
-1.78090907917167));
#59245=CARTESIAN_POINT('Ctrl Pts',(0.790275280774633,-0.0375469193645623,
-1.78617804094436));
#59246=CARTESIAN_POINT('Ctrl Pts',(0.784062327142098,-0.168315135758502,
-1.79144700271706));
#59247=CARTESIAN_POINT('Ctrl Pts',(0.744696302253884,-0.297508210270366,
-1.79671596448976));
#59248=CARTESIAN_POINT('Ctrl Pts',(0.676932099325491,-0.40952133456021,
-1.80198492626246));
#59249=CARTESIAN_POINT('Ctrl Pts',(0.609167896397101,-0.52153445885005,
-1.80725388803515));
#59250=CARTESIAN_POINT('Ctrl Pts',(0.513005515428532,-0.61636763291788,
-1.81252284980785));
#59251=CARTESIAN_POINT('Ctrl Pts',(0.400060095468028,-0.682566268263607,
-1.81779181158055));
#59252=CARTESIAN_POINT('Ctrl Pts',(0.287114675507523,-0.748764903609333,
-1.82306077335325));
#59253=CARTESIAN_POINT('Ctrl Pts',(0.157386216555084,-0.786329000232956,
-1.82832973512594));
#59254=CARTESIAN_POINT('Ctrl Pts',(0.0265441942837325,-0.790721313932425,
-1.83359869689864));
#59255=CARTESIAN_POINT('Ctrl Pts',(-0.104297827987626,-0.795113627631893,
-1.83886765867134));
#59256=CARTESIAN_POINT('Ctrl Pts',(-0.236253413577895,-0.766334158407205,
-1.84413662044403));
#59257=CARTESIAN_POINT('Ctrl Pts',(-0.353384079481705,-0.707859084088112,
-1.84940558221673));
#59258=CARTESIAN_POINT('Ctrl Pts',(-0.470514745385511,-0.649384009769022,
-1.85467454398943));
#59259=CARTESIAN_POINT('Ctrl Pts',(-0.572820491602857,-0.561213330355531,
-1.85994350576213));
#59260=CARTESIAN_POINT('Ctrl Pts',(-0.647944142117717,-0.453996893439293,
-1.86521246753482));
#59261=CARTESIAN_POINT('Ctrl Pts',(-0.723067792632574,-0.346780456523059,
-1.87048142930752));
#59262=CARTESIAN_POINT('Ctrl Pts',(-0.771009347444945,-0.22051826210408,
-1.87575039108022));
#59263=CARTESIAN_POINT('Ctrl Pts',(-0.785978103166188,-0.0904611071150179,
-1.88101935285291));
#59264=CARTESIAN_POINT('Ctrl Pts',(-0.789432198034349,-0.0604499452000733,
-1.88223518496071));
#59265=CARTESIAN_POINT('Ctrl Pts',(-0.79113058227838,-0.0302367120999488,
-1.8834510170685));
#59266=CARTESIAN_POINT('Ctrl Pts',(-0.791099975804956,-2.00585267497999E-5,
-1.8846668491763));
#59267=CARTESIAN_POINT('Ctrl Pts',(-0.791108422200728,-1.97323857704162E-5,
-1.91313315082371));
#59268=CARTESIAN_POINT('Ctrl Pts',(-0.791136454109385,-0.027533729362611,
-1.91202603187119));
#59269=CARTESIAN_POINT('Ctrl Pts',(-0.789728780531539,-0.0550448721224735,
-1.91091891291868));
#59270=CARTESIAN_POINT('Ctrl Pts',(-0.786863691565349,-0.0824033887437885,
-1.90981179396617));
#59271=CARTESIAN_POINT('Ctrl Pts',(-0.773228260427633,-0.21260708357566,
-1.90454283219347));
#59272=CARTESIAN_POINT('Ctrl Pts',(-0.726582878618806,-0.339353849556038,
-1.89927387042078));
#59273=CARTESIAN_POINT('Ctrl Pts',(-0.65256168903561,-0.447334359940417,
-1.89400490864808));
#59274=CARTESIAN_POINT('Ctrl Pts',(-0.578540499452414,-0.555314870324795,
-1.88873594687538));
#59275=CARTESIAN_POINT('Ctrl Pts',(-0.477143502094848,-0.644529125113175,
-1.88346698510268));
#59276=CARTESIAN_POINT('Ctrl Pts',(-0.360618108180484,-0.704201226662264,
-1.87819802332999));
#59277=CARTESIAN_POINT('Ctrl Pts',(-0.24409271426612,-0.763873328211353,
-1.87292906155729));
#59278=CARTESIAN_POINT('Ctrl Pts',(-0.112438923794957,-0.794003276521151,
-1.86766009978459));
#59279=CARTESIAN_POINT('Ctrl Pts',(0.0184412330716377,-0.790951773816272,
-1.86239113801189));
#59280=CARTESIAN_POINT('Ctrl Pts',(0.149321389938229,-0.787900271111393,
-1.8571221762392));
#59281=CARTESIAN_POINT('Ctrl Pts',(0.279427913200253,-0.751667317391838,
-1.8518532144665));
#59282=CARTESIAN_POINT('Ctrl Pts',(0.393045662034959,-0.686629372468008,
-1.8465842526938));
#59283=CARTESIAN_POINT('Ctrl Pts',(0.506663410869671,-0.621591427544173,
-1.84131529092111));
#59284=CARTESIAN_POINT('Ctrl Pts',(0.603792385277063,-0.52774849141606,
-1.83604632914841));
#59285=CARTESIAN_POINT('Ctrl Pts',(0.67270069455318,-0.416435544986229,
-1.83077736737571));
#59286=CARTESIAN_POINT('Ctrl Pts',(0.741609003829294,-0.305122598556405,
-1.82550840560301));
#59287=CARTESIAN_POINT('Ctrl Pts',(0.782296647974136,-0.176339641824865,
-1.82023944383032));
#59288=CARTESIAN_POINT('Ctrl Pts',(0.789849099710743,-0.04564194634806,
-1.81497048205762));
#59289=CARTESIAN_POINT('Ctrl Pts',(0.797401551447349,0.085055749128749,
-1.80970152028492));
#59290=CARTESIAN_POINT('Ctrl Pts',(0.771818810775718,0.217668183350823,
-1.80443255851223));
#59291=CARTESIAN_POINT('Ctrl Pts',(0.716190933153538,0.336177534717853,
-1.79916359673953));
#59292=CARTESIAN_POINT('Ctrl Pts',(0.660563055531358,0.454686886084884,
-1.79389463496683));
#59293=CARTESIAN_POINT('Ctrl Pts',(0.574890040958628,0.559093154596869,
-1.78862567319413));
#59294=CARTESIAN_POINT('Ctrl Pts',(0.469520052271186,0.636785449029398,
-1.78335671142144));
#59295=CARTESIAN_POINT('Ctrl Pts',(0.364150063583744,0.714477743461927,
-1.77808774964874));
#59296=CARTESIAN_POINT('Ctrl Pts',(0.239083100781589,0.765456063814999,
-1.77281878787604));
#59297=CARTESIAN_POINT('Ctrl Pts',(0.109425592684985,0.783562905736258,
-1.76754982610334));
#59298=CARTESIAN_POINT('Ctrl Pts',(-0.020231915411619,0.801669747657518,
-1.76228086433065));
#59299=CARTESIAN_POINT('Ctrl Pts',(-0.154479968802673,0.786905111146965,
-1.75701190255795));
#59300=CARTESIAN_POINT('Ctrl Pts',(-0.277103184805389,0.74105236829189,
-1.75174294078525));
#59301=CARTESIAN_POINT('Ctrl Pts',(-0.399726400808106,0.695199625436816,
-1.74647397901256));
#59302=CARTESIAN_POINT('Ctrl Pts',(-0.510724779422485,0.61825877623722,
-1.74120501723986));
#59303=CARTESIAN_POINT('Ctrl Pts',(-0.596691190035183,0.519523253872919,
-1.73593605546716));
#59304=CARTESIAN_POINT('Ctrl Pts',(-0.682657600647882,0.420787731508618,
-1.73066709369446));
#59305=CARTESIAN_POINT('Ctrl Pts',(-0.743592043258899,0.300257535979611,
-1.72539813192177));
#59306=CARTESIAN_POINT('Ctrl Pts',(-0.772134446116417,0.17249111484596,
-1.72012917014907));
#59307=CARTESIAN_POINT('Ctrl Pts',(-0.784767118395946,0.115942570752923,
-1.71779716370728));
#59308=CARTESIAN_POINT('Ctrl Pts',(-0.791054555941974,0.057976531794004,
-1.71546515726549));
#59309=CARTESIAN_POINT('Ctrl Pts',(-0.791037072492376,6.75761974000038E-6,
-1.7131331508237));
#59310=CARTESIAN_POINT('Origin',(0.,0.,-1.97));
#59311=CARTESIAN_POINT('',(-0.791156699774446,9.7028961639975E-6,-1.4846668491763));
#59312=CARTESIAN_POINT('',(-0.79115108988969,1.20126448708321E-5,-1.5131331508237));
#59313=CARTESIAN_POINT('',(-0.7911,-9.68818082805471E-17,-1.97));
#59314=CARTESIAN_POINT('Ctrl Pts',(-0.791156699774446,9.7028961639975E-6,
-1.4846668491763));
#59315=CARTESIAN_POINT('Ctrl Pts',(-0.791162742476985,0.00978612533273453,
-1.4850603060844));
#59316=CARTESIAN_POINT('Ctrl Pts',(-0.790985257298765,0.0195623280860764,
-1.48545376299251));
#59317=CARTESIAN_POINT('Ctrl Pts',(-0.790622820147353,0.0293316692235354,
-1.48584721990062));
#59318=CARTESIAN_POINT('Ctrl Pts',(-0.785769258152526,0.160157393558066,
-1.49111618167332));
#59319=CARTESIAN_POINT('Ctrl Pts',(-0.747748045175354,0.289752616390813,
-1.49638514344602));
#59320=CARTESIAN_POINT('Ctrl Pts',(-0.681151639005095,0.402463955203277,
-1.50165410521871));
#59321=CARTESIAN_POINT('Ctrl Pts',(-0.614555232834838,0.515175294015737,
-1.50692306699141));
#59322=CARTESIAN_POINT('Ctrl Pts',(-0.519383633471496,0.611002748807917,
-1.51219202876411));
#59323=CARTESIAN_POINT('Ctrl Pts',(-0.407132306698205,0.678371635167473,
-1.5174609905368));
#59324=CARTESIAN_POINT('Ctrl Pts',(-0.294880979924907,0.745740521527034,
-1.5227299523095));
#59325=CARTESIAN_POINT('Ctrl Pts',(-0.165549925741656,0.784650839453969,
-1.5279989140822));
#59326=CARTESIAN_POINT('Ctrl Pts',(-0.0347606186009809,0.790402739084114,
-1.5332678758549));
#59327=CARTESIAN_POINT('Ctrl Pts',(0.0960286885396864,0.796154638714258,
-1.53853683762759));
#59328=CARTESIAN_POINT('Ctrl Pts',(0.22827624863778,0.768748120047617,-1.54380579940029));
#59329=CARTESIAN_POINT('Ctrl Pts',(0.346008312043396,0.711493526712698,
-1.54907476117299));
#59330=CARTESIAN_POINT('Ctrl Pts',(0.463740375449019,0.654238933377775,
-1.55434372294569));
#59331=CARTESIAN_POINT('Ctrl Pts',(0.566956942162166,0.567136265374568,
-1.55961268471838));
#59332=CARTESIAN_POINT('Ctrl Pts',(0.643190821142216,0.460706368694415,
-1.56488164649108));
#59333=CARTESIAN_POINT('Ctrl Pts',(0.719424700122262,0.354276472014268,
-1.57015060826378));
#59334=CARTESIAN_POINT('Ctrl Pts',(0.768675891369217,0.228519346657175,
-1.57541957003647));
#59335=CARTESIAN_POINT('Ctrl Pts',(0.784995504798797,0.0986247839180053,
-1.58068853180917));
#59336=CARTESIAN_POINT('Ctrl Pts',(0.801315118228378,-0.0312697788211682,
-1.58595749358187));
#59337=CARTESIAN_POINT('Ctrl Pts',(0.784703153840584,-0.16530177894241,
-1.59122645535457));
#59338=CARTESIAN_POINT('Ctrl Pts',(0.737166116406668,-0.2872819301298,-1.59649541712726));
#59339=CARTESIAN_POINT('Ctrl Pts',(0.689629078972751,-0.409262081317194,
-1.60176437889996));
#59340=CARTESIAN_POINT('Ctrl Pts',(0.611166968492709,-0.519190383570726,
-1.60703334067266));
#59341=CARTESIAN_POINT('Ctrl Pts',(0.511256966314024,-0.603788957295985,
-1.61230230244535));
#59342=CARTESIAN_POINT('Ctrl Pts',(0.411346964135345,-0.68838753102124,
-1.61757126421805));
#59343=CARTESIAN_POINT('Ctrl Pts',(0.289989070258022,-0.747656376218227,
-1.62284022599075));
#59344=CARTESIAN_POINT('Ctrl Pts',(0.161841707214753,-0.77443660319164,
-1.62810918776345));
#59345=CARTESIAN_POINT('Ctrl Pts',(0.0336943441714761,-0.801216830165056,
-1.63337814953614));
#59346=CARTESIAN_POINT('Ctrl Pts',(-0.101242488037751,-0.795508438914895,
-1.63864711130884));
#59347=CARTESIAN_POINT('Ctrl Pts',(-0.226670211392565,-0.758000927324264,
-1.64391607308154));
#59348=CARTESIAN_POINT('Ctrl Pts',(-0.352097934747372,-0.720493415733635,
-1.64918503485424));
#59349=CARTESIAN_POINT('Ctrl Pts',(-0.468016549247768,-0.651186783802539,
-1.65445399662693));
#59350=CARTESIAN_POINT('Ctrl Pts',(-0.560424625102388,-0.558452352610354,
-1.65972295839963));
#59351=CARTESIAN_POINT('Ctrl Pts',(-0.65283270095701,-0.465717921418167,
-1.66499192017233));
#59352=CARTESIAN_POINT('Ctrl Pts',(-0.721730238165856,-0.349555690964889,
-1.67026088194502));
#59353=CARTESIAN_POINT('Ctrl Pts',(-0.75879532886119,-0.223996516614949,
-1.67552984371772));
#59354=CARTESIAN_POINT('Ctrl Pts',(-0.780220418573089,-0.151418343349124,
-1.67857551220391));
#59355=CARTESIAN_POINT('Ctrl Pts',(-0.791009340445165,-0.0757003714371634,
-1.6816211806901));
#59356=CARTESIAN_POINT('Ctrl Pts',(-0.791040023293942,9.038082159879E-6,
-1.6846668491763));
#59357=CARTESIAN_POINT('Ctrl Pts',(-0.791037072492376,6.75761974000038E-6,
-1.7131331508237));
#59358=CARTESIAN_POINT('Ctrl Pts',(-0.79101505363789,-0.0730010326855647,
-1.7101961954928));
#59359=CARTESIAN_POINT('Ctrl Pts',(-0.780992693074769,-0.146014747479032,
-1.70725924016189));
#59360=CARTESIAN_POINT('Ctrl Pts',(-0.7610505204609,-0.216210297827144,
-1.70432228483098));
#59361=CARTESIAN_POINT('Ctrl Pts',(-0.725273828843842,-0.342142642628313,
-1.69905332305828));
#59362=CARTESIAN_POINT('Ctrl Pts',(-0.657570082505703,-0.459004685492353,
-1.69378436128558));
#59363=CARTESIAN_POINT('Ctrl Pts',(-0.566116995224823,-0.552681043005752,
-1.68851539951289));
#59364=CARTESIAN_POINT('Ctrl Pts',(-0.474663907943943,-0.646357400519152,
-1.68324643774019));
#59365=CARTESIAN_POINT('Ctrl Pts',(-0.359461479720322,-0.71684807268191,
-1.67797747596749));
#59366=CARTESIAN_POINT('Ctrl Pts',(-0.234424634550591,-0.75563872207301,
-1.6727085141948));
#59367=CARTESIAN_POINT('Ctrl Pts',(-0.10938778938086,-0.79442937146411,
-1.6674395524221));
#59368=CARTESIAN_POINT('Ctrl Pts',(0.0254834727349791,-0.801519998083552,
-1.6621705906494));
#59369=CARTESIAN_POINT('Ctrl Pts',(0.153898493773395,-0.776054148365041,
-1.6569016288767));
#59370=CARTESIAN_POINT('Ctrl Pts',(0.282313514811811,-0.75058829864653,
-1.65163266710401));
#59371=CARTESIAN_POINT('Ctrl Pts',(0.404272294772801,-0.692565972590067,
-1.64636370533131));
#59372=CARTESIAN_POINT('Ctrl Pts',(0.505043832061636,-0.608995496926544,
-1.64109474355861));
#59373=CARTESIAN_POINT('Ctrl Pts',(0.605815369350467,-0.525425021263023,
-1.63582578178591));
#59374=CARTESIAN_POINT('Ctrl Pts',(0.685399663967143,-0.416306395992444,
-1.63055682001322));
#59375=CARTESIAN_POINT('Ctrl Pts',(0.734183989617675,-0.29481970247828,
-1.62528785824052));
#59376=CARTESIAN_POINT('Ctrl Pts',(0.78296831526821,-0.173333008964113,
-1.62001889646782));
#59377=CARTESIAN_POINT('Ctrl Pts',(0.800952671952598,-0.0394782472063504,
-1.61474993469513));
#59378=CARTESIAN_POINT('Ctrl Pts',(0.785964788128907,0.0905767045204875,
-1.60948097292243));
#59379=CARTESIAN_POINT('Ctrl Pts',(0.770976904305216,0.220631656247329,
-1.60421201114973));
#59380=CARTESIAN_POINT('Ctrl Pts',(0.723016779973445,0.346886797943254,
-1.59894304937703));
#59381=CARTESIAN_POINT('Ctrl Pts',(0.647877361473669,0.454092184550919,
-1.59367408760433));
#59382=CARTESIAN_POINT('Ctrl Pts',(0.572737942973897,0.561297571158579,
-1.58840512583164));
#59383=CARTESIAN_POINT('Ctrl Pts',(0.470419230306124,0.649453202677979,
-1.58313616405894));
#59384=CARTESIAN_POINT('Ctrl Pts',(0.353279965661455,0.707911049103311,
-1.57786720228624));
#59385=CARTESIAN_POINT('Ctrl Pts',(0.236140701016785,0.766368895528643,
-1.57259824051355));
#59386=CARTESIAN_POINT('Ctrl Pts',(0.104180884395221,0.795128956859905,
-1.56732927874085));
#59387=CARTESIAN_POINT('Ctrl Pts',(-0.0266604901454559,0.790717399483225,
-1.56206031696815));
#59388=CARTESIAN_POINT('Ctrl Pts',(-0.157501864686137,0.786305842106544,
-1.55679135519546));
#59389=CARTESIAN_POINT('Ctrl Pts',(-0.287224797145929,0.74872266602192,
-1.55152239342276));
#59390=CARTESIAN_POINT('Ctrl Pts',(-0.400160479378758,0.682507419977008,
-1.54625343165006));
#59391=CARTESIAN_POINT('Ctrl Pts',(-0.513096161611586,0.616292173932096,
-1.54098446987736));
#59392=CARTESIAN_POINT('Ctrl Pts',(-0.609244593617448,0.521444857926898,
-1.53571550810467));
#59393=CARTESIAN_POINT('Ctrl Pts',(-0.67699232119762,0.409421768619803,
-1.53044654633197));
#59394=CARTESIAN_POINT('Ctrl Pts',(-0.744740048777793,0.297398679312709,
-1.52517758455927));
#59395=CARTESIAN_POINT('Ctrl Pts',(-0.784087071932273,0.168199816703719,
-1.51990862278657));
#59396=CARTESIAN_POINT('Ctrl Pts',(-0.790280792602754,0.0374306882580553,
-1.51463966101388));
#59397=CARTESIAN_POINT('Ctrl Pts',(-0.790871098859641,0.0249674470439252,
-1.51413749095049));
#59398=CARTESIAN_POINT('Ctrl Pts',(-0.791160258257041,0.0124899423751816,
-1.5136353208871));
#59399=CARTESIAN_POINT('Ctrl Pts',(-0.79115108988969,1.20126448708321E-5,
-1.5131331508237));
#59400=CARTESIAN_POINT('Origin',(0.,0.,-1.97));
#59401=CARTESIAN_POINT('',(-0.79108328723417,-1.97011904900513E-5,-1.2846668491763));
#59402=CARTESIAN_POINT('',(-0.791091395193699,-2.00455443718572E-5,-1.3131331508237));
#59403=CARTESIAN_POINT('',(-0.7911,-9.68818082805471E-17,-1.97));
#59404=CARTESIAN_POINT('Ctrl Pts',(-0.79108328723417,-1.97011904900513E-5,
-1.2846668491763));
#59405=CARTESIAN_POINT('Ctrl Pts',(-0.790992127656328,0.0952359163469633,
-1.2884994314787));
#59406=CARTESIAN_POINT('Ctrl Pts',(-0.773765886393891,0.190523615754407,
-1.29233201378111));
#59407=CARTESIAN_POINT('Ctrl Pts',(-0.74011198568934,0.27960514872973,-1.29616459608352));
#59408=CARTESIAN_POINT('Ctrl Pts',(-0.693845238540031,0.402072757998116,
-1.30143355785622));
#59409=CARTESIAN_POINT('Ctrl Pts',(-0.61652983531396,0.512810569252064,
-1.30670251962891));
#59410=CARTESIAN_POINT('Ctrl Pts',(-0.51750445034507,0.59844292495629,-1.31197148140161));
#59411=CARTESIAN_POINT('Ctrl Pts',(-0.418479065376179,0.684075280660516,
-1.31724044317431));
#59412=CARTESIAN_POINT('Ctrl Pts',(-0.297743698664468,0.744602180815023,
-1.32250940494701));
#59413=CARTESIAN_POINT('Ctrl Pts',(-0.169881579725185,0.772712779386538,
-1.32777836671971));
#59414=CARTESIAN_POINT('Ctrl Pts',(-0.0420194607859029,0.800823377958053,
-1.3330473284924));
#59415=CARTESIAN_POINT('Ctrl Pts',(0.0929694103809409,0.796517674946579,
-1.3383162902651));
#59416=CARTESIAN_POINT('Ctrl Pts',(0.218780170139753,0.760315742116927,
-1.34358525203779));
#59417=CARTESIAN_POINT('Ctrl Pts',(0.344590929898565,0.724113809287274,
-1.34885421381049));
#59418=CARTESIAN_POINT('Ctrl Pts',(0.461223578249343,0.656015646639435,
-1.35412317558319));
#59419=CARTESIAN_POINT('Ctrl Pts',(0.554590439590504,0.564246608206026,
-1.35939213735589));
#59420=CARTESIAN_POINT('Ctrl Pts',(0.647957300931661,0.472477569772619,
-1.36466109912858));
#59421=CARTESIAN_POINT('Ctrl Pts',(0.718058375263214,0.357037655553636,
-1.36993006090128));
#59422=CARTESIAN_POINT('Ctrl Pts',(0.756426383410174,0.231870474701282,
-1.37519902267398));
#59423=CARTESIAN_POINT('Ctrl Pts',(0.794794391557134,0.106703293848925,
-1.38046798444668));
#59424=CARTESIAN_POINT('Ctrl Pts',(0.801429333519501,-0.0281911536367966,
-1.38573694621937));
#59425=CARTESIAN_POINT('Ctrl Pts',(0.775529796388259,-0.156519409247474,
-1.39100590799207));
#59426=CARTESIAN_POINT('Ctrl Pts',(0.749630259257016,-0.284847664858156,
-1.39627486976477));
#59427=CARTESIAN_POINT('Ctrl Pts',(0.691196243032161,-0.406609728593785,
-1.40154383153746));
#59428=CARTESIAN_POINT('Ctrl Pts',(0.60728580115167,-0.507098359568208,
-1.40681279331016));
#59429=CARTESIAN_POINT('Ctrl Pts',(0.523375359271181,-0.607586990542628,
-1.41208175508286));
#59430=CARTESIAN_POINT('Ctrl Pts',(0.413988491735055,-0.686802188755845,
-1.41735071685556));
#59431=CARTESIAN_POINT('Ctrl Pts',(0.292337680011484,-0.735175809859585,
-1.42261967862825));
#59432=CARTESIAN_POINT('Ctrl Pts',(0.170686868287912,-0.783549430963325,
-1.42788864040095));
#59433=CARTESIAN_POINT('Ctrl Pts',(0.0367721123768919,-0.801081474957589,
-1.43315760217365));
#59434=CARTESIAN_POINT('Ctrl Pts',(-0.0932314629497926,-0.78565430366888,
-1.43842656394635));
#59435=CARTESIAN_POINT('Ctrl Pts',(-0.223235038276477,-0.770227132380172,
-1.44369552571904));
#59436=CARTESIAN_POINT('Ctrl Pts',(-0.349327433018828,-0.721840745808492,
-1.44896448749174));
#59437=CARTESIAN_POINT('Ctrl Pts',(-0.456278359790997,-0.646339577113788,
-1.45423344926444));
#59438=CARTESIAN_POINT('Ctrl Pts',(-0.563229286563166,-0.570838408419083,
-1.45950241103713));
#59439=CARTESIAN_POINT('Ctrl Pts',(-0.651038745365154,-0.468222457601353,
-1.46477137280983));
#59440=CARTESIAN_POINT('Ctrl Pts',(-0.709100519259907,-0.350886369274331,
-1.47004033458253));
#59441=CARTESIAN_POINT('Ctrl Pts',(-0.762826561179094,-0.242312290715897,
-1.47491583944712));
#59442=CARTESIAN_POINT('Ctrl Pts',(-0.791081821877995,-0.121134427923465,
-1.47979134431171));
#59443=CARTESIAN_POINT('Ctrl Pts',(-0.791156699774446,9.7028961639975E-6,
-1.4846668491763));
#59444=CARTESIAN_POINT('Ctrl Pts',(-0.79115108988969,1.20126448708321E-5,
-1.5131331508237));
#59445=CARTESIAN_POINT('Ctrl Pts',(-0.791064060214553,-0.118433303641197,
-1.5083663591144));
#59446=CARTESIAN_POINT('Ctrl Pts',(-0.764096094533504,-0.23691692026043,
-1.50359956740509));
#59447=CARTESIAN_POINT('Ctrl Pts',(-0.712658406752002,-0.343602652588724,
-1.49883277569579));
#59448=CARTESIAN_POINT('Ctrl Pts',(-0.655801882044296,-0.461527470707488,
-1.49356381392309));
#59449=CARTESIAN_POINT('Ctrl Pts',(-0.569048414442406,-0.565037712662681,
-1.48829485215039));
#59450=CARTESIAN_POINT('Ctrl Pts',(-0.462876671164885,-0.641630715343042,
-1.48302589037769));
#59451=CARTESIAN_POINT('Ctrl Pts',(-0.356704927887362,-0.718223718023404,
-1.477756928605));
#59452=CARTESIAN_POINT('Ctrl Pts',(-0.231114908934207,-0.767899481428933,
-1.4724879668323));
#59453=CARTESIAN_POINT('Ctrl Pts',(-0.101276221365059,-0.784657832794859,
-1.4672190050596));
#59454=CARTESIAN_POINT('Ctrl Pts',(0.0285624662040879,-0.801416184160784,
-1.46195004328691));
#59455=CARTESIAN_POINT('Ctrl Pts',(0.162649822389227,-0.785257123487106,
-1.45668108151421));
#59456=CARTESIAN_POINT('Ctrl Pts',(0.284789874596762,-0.738132450788793,
-1.45141211974151));
#59457=CARTESIAN_POINT('Ctrl Pts',(0.406929926804297,-0.691007778090479,
-1.44614315796881));
#59458=CARTESIAN_POINT('Ctrl Pts',(0.517122675034227,-0.612917493367531,
-1.44087419619612));
#59459=CARTESIAN_POINT('Ctrl Pts',(0.602058298128763,-0.513293866352021,
-1.43560523442342));
#59460=CARTESIAN_POINT('Ctrl Pts',(0.686993921223296,-0.413670239336515,
-1.43033627265072));
#59461=CARTESIAN_POINT('Ctrl Pts',(0.746672419182438,-0.292513270028449,
-1.42506731087802));
#59462=CARTESIAN_POINT('Ctrl Pts',(0.773885421695427,-0.164457111939861,
-1.41979834910533));
#59463=CARTESIAN_POINT('Ctrl Pts',(0.801098424208418,-0.0364009538512651,
-1.41452938733263));
#59464=CARTESIAN_POINT('Ctrl Pts',(0.795845931275253,0.0985543930178537,
-1.40926042555993));
#59465=CARTESIAN_POINT('Ctrl Pts',(0.758762374314478,0.224108114322004,
-1.40399146378723));
#59466=CARTESIAN_POINT('Ctrl Pts',(0.721678817353705,0.349661835626148,
-1.39872250201454));
#59467=CARTESIAN_POINT('Ctrl Pts',(0.652764196365327,0.465813931365325,
-1.39345354024184));
#59468=CARTESIAN_POINT('Ctrl Pts',(0.560342482710852,0.558534770314031,
-1.38818457846914));
#59469=CARTESIAN_POINT('Ctrl Pts',(0.467920769056375,0.651255609262739,
-1.38291561669645));
#59470=CARTESIAN_POINT('Ctrl Pts',(0.351991962735802,0.720545191420975,
-1.37764665492375));
#59471=CARTESIAN_POINT('Ctrl Pts',(0.226558724577076,0.758034255095584,
-1.37237769315105));
#59472=CARTESIAN_POINT('Ctrl Pts',(0.101125486418351,0.795523318770194,
-1.36710873137835));
#59473=CARTESIAN_POINT('Ctrl Pts',(-0.0338121835785264,0.801211863961177,
-1.36183976960566));
#59474=CARTESIAN_POINT('Ctrl Pts',(-0.161955606199568,0.774412789925915,
-1.35657080783296));
#59475=CARTESIAN_POINT('Ctrl Pts',(-0.29009902882061,0.747613715890653,
-1.35130184606026));
#59476=CARTESIAN_POINT('Ctrl Pts',(-0.411448204065817,0.688327022629146,
-1.34603288428757));
#59477=CARTESIAN_POINT('Ctrl Pts',(-0.511345762497513,0.603713755645957,
-1.34076392251487));
#59478=CARTESIAN_POINT('Ctrl Pts',(-0.611243320929208,0.519100488662768,
-1.33549496074217));
#59479=CARTESIAN_POINT('Ctrl Pts',(-0.689689262547392,0.409160647957897,
-1.33022599896947));
#59480=CARTESIAN_POINT('Ctrl Pts',(-0.737208358988454,0.287173506817499,
-1.32495703719678));
#59481=CARTESIAN_POINT('Ctrl Pts',(-0.77275365368526,0.195924531020277,
-1.32101574173909));
#59482=CARTESIAN_POINT('Ctrl Pts',(-0.790994270862107,0.0979346591559362,
-1.3170744462814));
#59483=CARTESIAN_POINT('Ctrl Pts',(-0.791091395193699,-2.00455443718572E-5,
-1.3131331508237));
#59484=CARTESIAN_POINT('Origin',(0.,0.,-1.97));
#59485=CARTESIAN_POINT('',(-0.791048562900586,1.32194889376214E-5,-1.0846668491763));
#59486=CARTESIAN_POINT('',(-0.791043937878947,1.12442601377988E-5,-1.1131331508237));
#59487=CARTESIAN_POINT('',(-0.7911,-9.68818082805471E-17,-1.97));
#59488=CARTESIAN_POINT('Ctrl Pts',(-0.791048562900586,1.32194889376214E-5,
-1.0846668491763));
#59489=CARTESIAN_POINT('Ctrl Pts',(-0.791078489980937,0.0497960584196038,
-1.08666959510031));
#59490=CARTESIAN_POINT('Ctrl Pts',(-0.786451603860431,0.0995734034696943,
-1.08867234102432));
#59491=CARTESIAN_POINT('Ctrl Pts',(-0.777114596853452,0.1484509815208,-1.09067508694833));
#59492=CARTESIAN_POINT('Ctrl Pts',(-0.75255015640129,0.277041476803167,
-1.09594404872103));
#59493=CARTESIAN_POINT('Ctrl Pts',(-0.695384752424045,0.399404261200396,
-1.10121301049372));
#59494=CARTESIAN_POINT('Ctrl Pts',(-0.612523206841235,0.500759534745093,
-1.10648197226642));
#59495=CARTESIAN_POINT('Ctrl Pts',(-0.529661661258425,0.602114808289789,
-1.11175093403912));
#59496=CARTESIAN_POINT('Ctrl Pts',(-0.421103974070052,0.682462570981951,
-1.11701989581181));
#59497=CARTESIAN_POINT('Ctrl Pts',(-0.29996247276581,0.732097879719245,
-1.12228885758451));
#59498=CARTESIAN_POINT('Ctrl Pts',(-0.178820971461567,0.781733188456539,
-1.12755781935721));
#59499=CARTESIAN_POINT('Ctrl Pts',(-0.0450956560414579,0.800656043238965,
-1.13282678112991));
#59500=CARTESIAN_POINT('Ctrl Pts',(0.0850612306191843,0.786580814413079,
-1.1380957429026));
#59501=CARTESIAN_POINT('Ctrl Pts',(0.215218117279826,0.772505585587193,
-1.1433647046753));
#59502=CARTESIAN_POINT('Ctrl Pts',(0.341806575180999,0.725432273152994,
-1.148633666448));
#59503=CARTESIAN_POINT('Ctrl Pts',(0.449536399092598,0.651046708345916,
-1.1539026282207));
#59504=CARTESIAN_POINT('Ctrl Pts',(0.557266223004195,0.57666114353884,-1.15917158999339));
#59505=CARTESIAN_POINT('Ctrl Pts',(0.646137412926217,0.474963326358887,
-1.16444055176609));
#59506=CARTESIAN_POINT('Ctrl Pts',(0.705415508896985,0.358237003064731,
-1.16970951353879));
#59507=CARTESIAN_POINT('Ctrl Pts',(0.764693604867754,0.241510679770572,
-1.17497847531148));
#59508=CARTESIAN_POINT('Ctrl Pts',(0.794378606887267,0.109755850362201,
-1.18024743708418));
#59509=CARTESIAN_POINT('Ctrl Pts',(0.790884960785258,-0.021113250836693,
-1.18551639885688));
#59510=CARTESIAN_POINT('Ctrl Pts',(0.78739131468325,-0.151982352035583,
-1.19078536062958));
#59511=CARTESIAN_POINT('Ctrl Pts',(0.750719020459724,-0.281965725025003,
-1.19605432240227));
#59512=CARTESIAN_POINT('Ctrl Pts',(0.685297604425638,-0.395363103900293,
-1.20132328417497));
#59513=CARTESIAN_POINT('Ctrl Pts',(0.619876188391549,-0.508760482775588,
-1.20659224594767));
#59514=CARTESIAN_POINT('Ctrl Pts',(0.525705650546899,-0.605571867536749,
-1.21186120772036));
#59515=CARTESIAN_POINT('Ctrl Pts',(0.414160541732633,-0.674103728093032,
-1.21713016949306));
#59516=CARTESIAN_POINT('Ctrl Pts',(0.302615432918367,-0.742635588649315,
-1.22239913126576));
#59517=CARTESIAN_POINT('Ctrl Pts',(0.173695753134486,-0.782887925000717,
-1.22766809303846));
#59518=CARTESIAN_POINT('Ctrl Pts',(0.0429732882671409,-0.789998789272934,
-1.23293705481115));
#59519=CARTESIAN_POINT('Ctrl Pts',(-0.0877491766002046,-0.797109653545151,
-1.23820601658385));
#59520=CARTESIAN_POINT('Ctrl Pts',(-0.220274426551013,-0.771079045738183,
-1.24347497835655));
#59521=CARTESIAN_POINT('Ctrl Pts',(-0.338595170687559,-0.71505111771415,
-1.24874394012925));
#59522=CARTESIAN_POINT('Ctrl Pts',(-0.456915914824105,-0.659023189690117,
-1.25401290190194));
#59523=CARTESIAN_POINT('Ctrl Pts',(-0.561032153146387,-0.572997941449019,
-1.25928186367464));
#59524=CARTESIAN_POINT('Ctrl Pts',(-0.638368026226707,-0.467366080977867,
-1.26455082544734));
#59525=CARTESIAN_POINT('Ctrl Pts',(-0.715703899307027,-0.361734220506716,
-1.26981978722003));
#59526=CARTESIAN_POINT('Ctrl Pts',(-0.766259407145385,-0.236495747805511,
-1.27508874899273));
#59527=CARTESIAN_POINT('Ctrl Pts',(-0.783928115528291,-0.106777807813496,
-1.28035771076543));
#59528=CARTESIAN_POINT('Ctrl Pts',(-0.788744808281546,-0.0714152081267372,
-1.28179409023572));
#59529=CARTESIAN_POINT('Ctrl Pts',(-0.791117452122437,-0.0357197077825311,
-1.28323046970601));
#59530=CARTESIAN_POINT('Ctrl Pts',(-0.79108328723417,-1.97011904900513E-5,
-1.2846668491763));
#59531=CARTESIAN_POINT('Ctrl Pts',(-0.791091395193699,-2.00455443718572E-5,
-1.3131331508237));
#59532=CARTESIAN_POINT('Ctrl Pts',(-0.791124112533671,-0.0330171053241025,
-1.3118054845087));
#59533=CARTESIAN_POINT('Ctrl Pts',(-0.789097998462795,-0.0660101745126855,
-1.31047781819369));
#59534=CARTESIAN_POINT('Ctrl Pts',(-0.784980989092685,-0.0987402366990249,
-1.30915015187868));
#59535=CARTESIAN_POINT('Ctrl Pts',(-0.768642271491913,-0.228632397499223,
-1.30388119010599));
#59536=CARTESIAN_POINT('Ctrl Pts',(-0.719372585026431,-0.354382277523696,
-1.29861222833329));
#59537=CARTESIAN_POINT('Ctrl Pts',(-0.643123053757393,-0.460800960617569,
-1.29334326656059));
#59538=CARTESIAN_POINT('Ctrl Pts',(-0.566873522488357,-0.56721964371144,
-1.2880743047879));
#59539=CARTESIAN_POINT('Ctrl Pts',(-0.463644146415765,-0.654307129874715,
-1.2828053430152));
#59540=CARTESIAN_POINT('Ctrl Pts',(-0.34590366378081,-0.71154440688078,
-1.2775363812425));
#59541=CARTESIAN_POINT('Ctrl Pts',(-0.228163181145847,-0.768781683886849,
-1.2722674194698));
#59542=CARTESIAN_POINT('Ctrl Pts',(-0.0959115919485175,-0.796168751735706,
-1.26699845769711));
#59543=CARTESIAN_POINT('Ctrl Pts',(0.0348768674995742,-0.79039761619942,
-1.26172949592441));
#59544=CARTESIAN_POINT('Ctrl Pts',(0.165665326947662,-0.784626480663134,
-1.25646053415171));
#59545=CARTESIAN_POINT('Ctrl Pts',(0.294990656646514,-0.745697141741706,
-1.25119157237902));
#59546=CARTESIAN_POINT('Ctrl Pts',(0.407232073585324,-0.678311746782928,
-1.24592261060632));
#59547=CARTESIAN_POINT('Ctrl Pts',(0.519473490524134,-0.610926351824149,
-1.24065364883362));
#59548=CARTESIAN_POINT('Ctrl Pts',(0.614630994702904,-0.515084900828019,
-1.23538468706092));
#59549=CARTESIAN_POINT('Ctrl Pts',(0.681210822849676,-0.402363768762516,
-1.23011572528823));
#59550=CARTESIAN_POINT('Ctrl Pts',(0.747790650996447,-0.289642636697016,
-1.22484676351553));
#59551=CARTESIAN_POINT('Ctrl Pts',(0.785792803111224,-0.160041823562142,
-1.21957780174283));
#59552=CARTESIAN_POINT('Ctrl Pts',(0.790627123703887,-0.0292153871106796,
-1.21430883997013));
#59553=CARTESIAN_POINT('Ctrl Pts',(0.795461444296551,0.101611049340787,
-1.20903987819744));
#59554=CARTESIAN_POINT('Ctrl Pts',(0.767127933367104,0.233663109108835,
-1.20377091642474));
#59555=CARTESIAN_POINT('Ctrl Pts',(0.709048902903408,0.350990656388148,
-1.19850195465204));
#59556=CARTESIAN_POINT('Ctrl Pts',(0.65096987243971,0.468318203667464,-1.19323299287935));
#59557=CARTESIAN_POINT('Ctrl Pts',(0.563145322441762,0.570921238458036,
-1.18796403110665));
#59558=CARTESIAN_POINT('Ctrl Pts',(0.456183292662752,0.646406676230745,
-1.18269506933395));
#59559=CARTESIAN_POINT('Ctrl Pts',(0.349221262883743,0.721892114003455,
-1.17742610756125));
#59560=CARTESIAN_POINT('Ctrl Pts',(0.22312175332367,0.770259954758303,-1.17215714578856));
#59561=CARTESIAN_POINT('Ctrl Pts',(0.0931159107439142,0.785668005423818,
-1.16688818401586));
#59562=CARTESIAN_POINT('Ctrl Pts',(-0.0368899318358343,0.801076056089331,
-1.16161922224316));
#59563=CARTESIAN_POINT('Ctrl Pts',(-0.170802107435268,0.783524316665514,
-1.15635026047047));
#59564=CARTESIAN_POINT('Ctrl Pts',(-0.292445802949988,0.735132804272293,
-1.15108129869777));
#59565=CARTESIAN_POINT('Ctrl Pts',(-0.414089498464712,0.68674129187907,
-1.14581233692507));
#59566=CARTESIAN_POINT('Ctrl Pts',(-0.523464713894725,0.60751000651644,
-1.14054337515237));
#59567=CARTESIAN_POINT('Ctrl Pts',(-0.607360375191571,0.507009035646765,
-1.13527441337968));
#59568=CARTESIAN_POINT('Ctrl Pts',(-0.691256036488417,0.406508064777091,
-1.13000545160698));
#59569=CARTESIAN_POINT('Ctrl Pts',(-0.749672143652099,0.28473740840037,
-1.12473648983428));
#59570=CARTESIAN_POINT('Ctrl Pts',(-0.775552806421482,0.15640534527973,
-1.11946752806158));
#59571=CARTESIAN_POINT('Ctrl Pts',(-0.785924102084645,0.104978154965951,
-1.11735606898229));
#59572=CARTESIAN_POINT('Ctrl Pts',(-0.791070569896215,0.0524972762412874,
-1.115244609903));
#59573=CARTESIAN_POINT('Ctrl Pts',(-0.791043937878947,1.12442601377988E-5,
-1.1131331508237));
#59574=CARTESIAN_POINT('Origin',(0.,0.,-1.97));
#59575=CARTESIAN_POINT('',(-0.791164617967662,4.43993036714635E-6,-0.884666849176296));
#59576=CARTESIAN_POINT('',(-0.79116135777148,7.11475864817537E-6,-0.913133150823704));
#59577=CARTESIAN_POINT('',(-0.7911,-9.68818082805471E-17,-1.97));
#59578=CARTESIAN_POINT('Ctrl Pts',(-0.791164617967662,4.43993036714635E-6,
-0.884666849176296));
#59579=CARTESIAN_POINT('Ctrl Pts',(-0.791165954160854,0.00430068567149038,
-0.884839758721909));
#59580=CARTESIAN_POINT('Ctrl Pts',(-0.79113168381486,0.00859691002598646,
-0.885012668267522));
#59581=CARTESIAN_POINT('Ctrl Pts',(-0.791061674373356,0.012892551912441,
-0.885185577813136));
#59582=CARTESIAN_POINT('Ctrl Pts',(-0.788928321528631,0.143790894214137,
-0.890454539585833));
#59583=CARTESIAN_POINT('Ctrl Pts',(-0.753608907198563,0.274148377270177,
-0.895723501358531));
#59584=CARTESIAN_POINT('Ctrl Pts',(-0.6893695477627,0.388219547646229,-0.900992463131228));
#59585=CARTESIAN_POINT('Ctrl Pts',(-0.625130188326837,0.50229071802228,
-0.906261424903925));
#59586=CARTESIAN_POINT('Ctrl Pts',(-0.531970883785179,0.600075575718343,
-0.911530386676622));
#59587=CARTESIAN_POINT('Ctrl Pts',(-0.421144041419974,0.669763008036159,
-0.916799348449319));
#59588=CARTESIAN_POINT('Ctrl Pts',(-0.310317199054769,0.739450440353975,
-0.922068310222016));
#59589=CARTESIAN_POINT('Ctrl Pts',(-0.181822818866018,0.781040447293544,
-0.927337271994713));
#59590=CARTESIAN_POINT('Ctrl Pts',(-0.0511813161947067,0.789509508131327,
-0.932606233767411));
#59591=CARTESIAN_POINT('Ctrl Pts',(0.0794601864766005,0.797978568969109,
-0.937875195540108));
#59592=CARTESIAN_POINT('Ctrl Pts',(0.212248811630478,0.773326683705103,
-0.943144157312806));
#59593=CARTESIAN_POINT('Ctrl Pts',(0.331145456140999,0.718531472821032,
-0.948413119085503));
#59594=CARTESIAN_POINT('Ctrl Pts',(0.450042100651527,0.663736261936958,
-0.9536820808582));
#59595=CARTESIAN_POINT('Ctrl Pts',(0.555046764518701,0.57879772543282,-0.958951042630897));
#59596=CARTESIAN_POINT('Ctrl Pts',(0.633476278303023,0.473975310944086,
-0.964220004403595));
#59597=CARTESIAN_POINT('Ctrl Pts',(0.711905792087343,0.369152896455355,
-0.969488966176292));
#59598=CARTESIAN_POINT('Ctrl Pts',(0.763760155788802,0.244446603982033,
-0.97475792794899));
#59599=CARTESIAN_POINT('Ctrl Pts',(0.782776050648192,0.114919298156625,
-0.980026889721687));
#59600=CARTESIAN_POINT('Ctrl Pts',(0.801791945507582,-0.0146080076687826,
-0.985295851494384));
#59601=CARTESIAN_POINT('Ctrl Pts',(0.787969371524902,-0.148956326846277,
-0.99056481326708));
#59602=CARTESIAN_POINT('Ctrl Pts',(0.742977912140126,-0.271898165917117,
-0.995833775039778));
#59603=CARTESIAN_POINT('Ctrl Pts',(0.697986452755349,-0.394840004987956,
-1.00110273681248));
#59604=CARTESIAN_POINT('Ctrl Pts',(0.621826107968476,-0.50637536395214,
-1.00637169858517));
#59605=CARTESIAN_POINT('Ctrl Pts',(0.523696036387599,-0.593032252098578,
-1.01164066035787));
#59606=CARTESIAN_POINT('Ctrl Pts',(0.425565964806725,-0.679689140245013,
-1.01690962213057));
#59607=CARTESIAN_POINT('Ctrl Pts',(0.30546616643185,-0.741467557573703,
-1.02217858390326));
#59608=CARTESIAN_POINT('Ctrl Pts',(0.177903102560412,-0.770905491390852,
-1.02744754567596));
#59609=CARTESIAN_POINT('Ctrl Pts',(0.0503400386889753,-0.800343425208001,
-1.03271650744866));
#59610=CARTESIAN_POINT('Ctrl Pts',(-0.0846862906790231,-0.797440875513609,
-1.03798546922136));
#59611=CARTESIAN_POINT('Ctrl Pts',(-0.210866497454535,-0.762548431778893,
-1.04325443099405));
#59612=CARTESIAN_POINT('Ctrl Pts',(-0.337046704230054,-0.727655988044175,
-1.04852339276675));
#59613=CARTESIAN_POINT('Ctrl Pts',(-0.454380788413085,-0.660773650269129,
-1.05379235453945));
#59614=CARTESIAN_POINT('Ctrl Pts',(-0.548696350265211,-0.569979916982019,
-1.05906131631214));
#59615=CARTESIAN_POINT('Ctrl Pts',(-0.643011912117332,-0.479186183694914,
-1.06433027808484));
#59616=CARTESIAN_POINT('Ctrl Pts',(-0.714308951638551,-0.364481054895748,
-1.06959923985754));
#59617=CARTESIAN_POINT('Ctrl Pts',(-0.753975732935622,-0.239719387412416,
-1.07486820163024));
#59618=CARTESIAN_POINT('Ctrl Pts',(-0.778565068620354,-0.162379950684253,
-1.07813441747892));
#59619=CARTESIAN_POINT('Ctrl Pts',(-0.790999755758863,-0.0811760594697772,
-1.08140063332761));
#59620=CARTESIAN_POINT('Ctrl Pts',(-0.791048562900586,1.32194889376214E-5,
-1.0846668491763));
#59621=CARTESIAN_POINT('Ctrl Pts',(-0.791043937878947,1.12442601377988E-5,
-1.1131331508237));
#59622=CARTESIAN_POINT('Ctrl Pts',(-0.791004112022466,-0.0784770338087006,
-1.1099756481303));
#59623=CARTESIAN_POINT('Ctrl Pts',(-0.779395894589143,-0.15697683589426,
-1.1068181454369));
#59624=CARTESIAN_POINT('Ctrl Pts',(-0.756392270823624,-0.231981723889169,
-1.10366064274349));
#59625=CARTESIAN_POINT('Ctrl Pts',(-0.718005854081292,-0.35714326007288,
-1.0983916809708));
#59626=CARTESIAN_POINT('Ctrl Pts',(-0.647887802221541,-0.472572862575744,
-1.0931227191981));
#59627=CARTESIAN_POINT('Ctrl Pts',(-0.554507445079383,-0.564328167763975,
-1.0878537574254));
#59628=CARTESIAN_POINT('Ctrl Pts',(-0.461127087937224,-0.656083472952205,
-1.0825847956527));
#59629=CARTESIAN_POINT('Ctrl Pts',(-0.344484425512659,-0.724164480825803,
-1.07731583388001));
#59630=CARTESIAN_POINT('Ctrl Pts',(-0.218668342974427,-0.760347909421159,
-1.07204687210731));
#59631=CARTESIAN_POINT('Ctrl Pts',(-0.0928522604361946,-0.796531338016516,
-1.06677791033461));
#59632=CARTESIAN_POINT('Ctrl Pts',(0.0421372422157041,-0.80081718733363,
-1.06150894856192));
#59633=CARTESIAN_POINT('Ctrl Pts',(0.169995225070644,-0.77268778367041,
-1.05623998678922));
#59634=CARTESIAN_POINT('Ctrl Pts',(0.297853207925584,-0.74455838000719,
-1.05097102501652));
#59635=CARTESIAN_POINT('Ctrl Pts',(0.418579670983564,-0.684013723363635,
-1.04570206324382));
#59636=CARTESIAN_POINT('Ctrl Pts',(0.517592460172511,-0.598366804521171,
-1.04043310147113));
#59637=CARTESIAN_POINT('Ctrl Pts',(0.616605249361455,-0.512719885678709,
-1.03516413969843));
#59638=CARTESIAN_POINT('Ctrl Pts',(0.693904364681367,-0.40197070463734,
-1.02989517792573));
#59639=CARTESIAN_POINT('Ctrl Pts',(0.740153099161143,-0.279496292251729,
-1.02462621615304));
#59640=CARTESIAN_POINT('Ctrl Pts',(0.786401833640922,-0.157021879866112,
-1.01935725438034));
#59641=CARTESIAN_POINT('Ctrl Pts',(0.801600187280563,-0.0228222361362515,
-1.01408829260764));
#59642=CARTESIAN_POINT('Ctrl Pts',(0.783912400721252,0.10689310349949,-1.00881933083494));
#59643=CARTESIAN_POINT('Ctrl Pts',(0.766224614161942,0.236608443135223,
-1.00355036906225));
#59644=CARTESIAN_POINT('Ctrl Pts',(0.715650687403683,0.361839478676839,
-0.998281407289548));
#59645=CARTESIAN_POINT('Ctrl Pts',(0.638299279420976,0.46745996349524,-0.993012445516851));
#59646=CARTESIAN_POINT('Ctrl Pts',(0.560947871438269,0.573080448313642,
-0.987743483744154));
#59647=CARTESIAN_POINT('Ctrl Pts',(0.456818982231114,0.659090382408831,
-0.982474521971457));
#59648=CARTESIAN_POINT('Ctrl Pts',(0.338489999286157,0.715100907539325,
-0.97720556019876));
#59649=CARTESIAN_POINT('Ctrl Pts',(0.220161016341194,0.771111432669822,
-0.971936598426063));
#59650=CARTESIAN_POINT('Ctrl Pts',(0.0876319396584279,0.79712254883562,
-0.966667636653365));
#59651=CARTESIAN_POINT('Ctrl Pts',(-0.0430894776459918,0.789992458506096,
-0.961398674880668));
#59652=CARTESIAN_POINT('Ctrl Pts',(-0.173810894950408,0.782862368176572,
-0.95612971310797));
#59653=CARTESIAN_POINT('Ctrl Pts',(-0.302724652876478,0.742591071351728,
-0.950860751335273));
#59654=CARTESIAN_POINT('Ctrl Pts',(-0.414259680819861,0.674042806079358,
-0.945591789562576));
#59655=CARTESIAN_POINT('Ctrl Pts',(-0.525794708763244,0.605494540806989,
-0.940322827789879));
#59656=CARTESIAN_POINT('Ctrl Pts',(-0.619951006723941,0.508669307087093,
-0.935053866017182));
#59657=CARTESIAN_POINT('Ctrl Pts',(-0.685355743849948,0.395262307780788,
-0.929784904244485));
#59658=CARTESIAN_POINT('Ctrl Pts',(-0.750760480975956,0.281855308474479,
-0.924515942471787));
#59659=CARTESIAN_POINT('Ctrl Pts',(-0.787413657267272,0.151866543581759,
-0.919246980699089));
#59660=CARTESIAN_POINT('Ctrl Pts',(-0.790888055605358,0.020996930277632,
-0.913978018926392));
#59661=CARTESIAN_POINT('Ctrl Pts',(-0.79107376001662,0.0140020315568058,
-0.913696396225496));
#59662=CARTESIAN_POINT('Ctrl Pts',(-0.79116467811953,0.0070046163970303,
-0.9134147735246));
#59663=CARTESIAN_POINT('Ctrl Pts',(-0.79116135777148,7.11475864817537E-6,
-0.913133150823704));
#59664=CARTESIAN_POINT('Origin',(0.,0.,-1.97));
#59665=CARTESIAN_POINT('',(-0.79106797157506,-1.80494624554273E-5,-0.684666849176296));
#59666=CARTESIAN_POINT('',(-0.791075294242739,-1.90178071996814E-5,-0.713133150823704));
#59667=CARTESIAN_POINT('',(-0.7911,-9.68818082805471E-17,-1.97));
#59668=CARTESIAN_POINT('Ctrl Pts',(-0.79106797157506,-1.80494624554273E-5,
-0.684666849176296));
#59669=CARTESIAN_POINT('Ctrl Pts',(-0.790991667205036,0.0897610395828043,
-0.688278884116209));
#59670=CARTESIAN_POINT('Ctrl Pts',(-0.775729031502744,0.179565416210847,
-0.691890919056122));
#59671=CARTESIAN_POINT('Ctrl Pts',(-0.74576358619739,0.264161814157916,
-0.695502953996035));
#59672=CARTESIAN_POINT('Ctrl Pts',(-0.702052274307491,0.387564603528967,
-0.700771915768733));
#59673=CARTESIAN_POINT('Ctrl Pts',(-0.627055214381976,0.499885462766481,
-0.70604087754143));
#59674=CARTESIAN_POINT('Ctrl Pts',(-0.529831055660502,0.587557523154006,
-0.711309839314127));
#59675=CARTESIAN_POINT('Ctrl Pts',(-0.432606896939028,0.675229583541531,
-0.716578801086824));
#59676=CARTESIAN_POINT('Ctrl Pts',(-0.313155639421595,0.738252845079068,
-0.721847762859521));
#59677=CARTESIAN_POINT('Ctrl Pts',(-0.18590540927956,0.769014934417917,
-0.727116724632219));
#59678=CARTESIAN_POINT('Ctrl Pts',(-0.058655179137525,0.799777023756766,
-0.732385686404916));
#59679=CARTESIAN_POINT('Ctrl Pts',(0.0763940236291114,0.798277940896928,
-0.737654648177614));
#59680=CARTESIAN_POINT('Ctrl Pts',(0.202930048128393,0.76469875514728,-0.742923609950311));
#59681=CARTESIAN_POINT('Ctrl Pts',(0.329466072627671,0.731119569397634,
-0.748192571723008));
#59682=CARTESIAN_POINT('Ctrl Pts',(0.447488918859595,0.665460280758179,
-0.753461533495704));
#59683=CARTESIAN_POINT('Ctrl Pts',(0.542742993773683,0.575651659657794,
-0.758730495268401));
#59684=CARTESIAN_POINT('Ctrl Pts',(0.637997068687777,0.485843038557404,
-0.763999457041099));
#59685=CARTESIAN_POINT('Ctrl Pts',(0.710482372284031,0.37188508499608,-0.769268418813797));
#59686=CARTESIAN_POINT('Ctrl Pts',(0.751443642143352,0.247542406951874,
-0.774537380586494));
#59687=CARTESIAN_POINT('Ctrl Pts',(0.792404912002671,0.123199728907672,
-0.779806342359191));
#59688=CARTESIAN_POINT('Ctrl Pts',(0.801842148125059,-0.0115276736194127,
-0.785075304131888));
#59689=CARTESIAN_POINT('Ctrl Pts',(0.778615457667923,-0.140366518934405,
-0.790344265904585));
#59690=CARTESIAN_POINT('Ctrl Pts',(0.755388767210788,-0.269205364249398,
-0.795613227677282));
#59691=CARTESIAN_POINT('Ctrl Pts',(0.699498150174129,-0.392155652352298,
-0.80088218944998));
#59692=CARTESIAN_POINT('Ctrl Pts',(0.617694451138065,-0.49436662062728,
-0.806151151222677));
#59693=CARTESIAN_POINT('Ctrl Pts',(0.535890752102002,-0.596577588902262,
-0.811420112995375));
#59694=CARTESIAN_POINT('Ctrl Pts',(0.428173971066533,-0.678049237349324,
-0.816689074768072));
#59695=CARTESIAN_POINT('Ctrl Pts',(0.307554865221265,-0.728940872386727,
-0.82195803654077));
#59696=CARTESIAN_POINT('Ctrl Pts',(0.186935759375997,-0.779832507424129,
-0.827226998313467));
#59697=CARTESIAN_POINT('Ctrl Pts',(0.0534143287209287,-0.800144129051871,
-0.832495960086164));
#59698=CARTESIAN_POINT('Ctrl Pts',(-0.0768818104416133,-0.787422363017722,
-0.837764921858862));
#59699=CARTESIAN_POINT('Ctrl Pts',(-0.207177949604159,-0.774700596983572,
-0.843033883631559));
#59700=CARTESIAN_POINT('Ctrl Pts',(-0.334248797274178,-0.728945443287528,
-0.848302845404255));
#59701=CARTESIAN_POINT('Ctrl Pts',(-0.442745881941299,-0.655683517088247,
-0.853571807176953));
#59702=CARTESIAN_POINT('Ctrl Pts',(-0.551242966608413,-0.582421590888971,
-0.85884076894965));
#59703=CARTESIAN_POINT('Ctrl Pts',(-0.641166288272631,-0.48165289218646,
-0.864109730722348));
#59704=CARTESIAN_POINT('Ctrl Pts',(-0.701654303425048,-0.36554894206153,
-0.869378692495045));
#59705=CARTESIAN_POINT('Ctrl Pts',(-0.76015730603301,-0.253255131794522,
-0.874474744722129));
#59706=CARTESIAN_POINT('Ctrl Pts',(-0.791125237202045,-0.126616057506534,
-0.879570796949212));
#59707=CARTESIAN_POINT('Ctrl Pts',(-0.791164617967662,4.43993036714635E-6,
-0.884666849176296));
#59708=CARTESIAN_POINT('Ctrl Pts',(-0.79116135777148,7.11475864817537E-6,
-0.913133150823704));
#59709=CARTESIAN_POINT('Ctrl Pts',(-0.791102556753278,-0.123913695655651,
-0.908145811751903));
#59710=CARTESIAN_POINT('Ctrl Pts',(-0.761488779732474,-0.247861627410726,
-0.903158472680102));
#59711=CARTESIAN_POINT('Ctrl Pts',(-0.705362811486509,-0.358340748104591,
-0.898171133608301));
#59712=CARTESIAN_POINT('Ctrl Pts',(-0.646067548644711,-0.475058351467171,
-0.892902171835604));
#59713=CARTESIAN_POINT('Ctrl Pts',(-0.557181402576256,-0.576743096476801,
-0.887633210062906));
#59714=CARTESIAN_POINT('Ctrl Pts',(-0.449440639746771,-0.651112815819442,
-0.882364248290209));
#59715=CARTESIAN_POINT('Ctrl Pts',(-0.341699876917287,-0.725482535162083,
-0.877095286517512));
#59716=CARTESIAN_POINT('Ctrl Pts',(-0.215104497326772,-0.772537228837736,
-0.871826324744815));
#59717=CARTESIAN_POINT('Ctrl Pts',(-0.0849455422535194,-0.786593314509833,
-0.866557362972118));
#59718=CARTESIAN_POINT('Ctrl Pts',(0.0452134128197299,-0.800649400181929,
-0.861288401199421));
#59719=CARTESIAN_POINT('Ctrl Pts',(0.178935943375718,-0.781706877850472,
-0.856019439426723));
#59720=CARTESIAN_POINT('Ctrl Pts',(0.300070142913725,-0.732053752747738,
-0.850750477654026));
#59721=CARTESIAN_POINT('Ctrl Pts',(0.421204342451739,-0.682400627645001,
-0.845481515881328));
#59722=CARTESIAN_POINT('Ctrl Pts',(0.52975021097177,-0.602036899770983,
-0.840212554108631));
#59723=CARTESIAN_POINT('Ctrl Pts',(0.612596848522363,-0.500669440610047,
-0.834943592335933));
#59724=CARTESIAN_POINT('Ctrl Pts',(0.695443486072952,-0.399301981449116,
-0.829674630563237));
#59725=CARTESIAN_POINT('Ctrl Pts',(0.752590892654105,-0.276930791001269,
-0.82440566879054));
#59726=CARTESIAN_POINT('Ctrl Pts',(0.777136420192834,-0.148336684573226,
-0.819136707017843));
#59727=CARTESIAN_POINT('Ctrl Pts',(0.801681947731563,-0.0197425781451788,
-0.813867745245145));
#59728=CARTESIAN_POINT('Ctrl Pts',(0.793625596227868,0.115074444263065,
-0.808598783472448));
#59729=CARTESIAN_POINT('Ctrl Pts',(0.75394046599389,0.239830276064607,-0.80332982169975));
#59730=CARTESIAN_POINT('Ctrl Pts',(0.714255335759913,0.364586107866145,
-0.798060859927053));
#59731=CARTESIAN_POINT('Ctrl Pts',(0.642941426795649,0.479280749060992,
-0.792791898154356));
#59732=CARTESIAN_POINT('Ctrl Pts',(0.548612512599131,0.57006060958461,-0.787522936381659));
#59733=CARTESIAN_POINT('Ctrl Pts',(0.454283598402605,0.660840470108236,
-0.782253974608962));
#59734=CARTESIAN_POINT('Ctrl Pts',(0.336939678973828,0.727705549960633,
-0.776985012836264));
#59735=CARTESIAN_POINT('Ctrl Pts',(0.210754342018317,0.762579435141504,
-0.771716051063566));
#59736=CARTESIAN_POINT('Ctrl Pts',(0.0845690050628165,0.797453320322372,
-0.766447089290869));
#59737=CARTESIAN_POINT('Ctrl Pts',(-0.0504577494194056,0.800336010831712,
-0.761178127518172));
#59738=CARTESIAN_POINT('Ctrl Pts',(-0.178016481991146,0.770879315924228,
-0.755909165745476));
#59739=CARTESIAN_POINT('Ctrl Pts',(-0.30557521456289,0.741422621016742,
-0.750640203972778));
#59740=CARTESIAN_POINT('Ctrl Pts',(-0.425665925224152,0.679626540692429,
-0.745371242200081));
#59741=CARTESIAN_POINT('Ctrl Pts',(-0.523783250352655,0.592955221100478,
-0.740102280427384));
#59742=CARTESIAN_POINT('Ctrl Pts',(-0.621900575481158,0.506283901508527,
-0.734833318654687));
#59743=CARTESIAN_POINT('Ctrl Pts',(-0.698044515076902,0.394737342648938,
-0.729564356881989));
#59744=CARTESIAN_POINT('Ctrl Pts',(-0.743017892061099,0.271788888031485,
-0.724295395109292));
#59745=CARTESIAN_POINT('Ctrl Pts',(-0.774776446016752,0.184967186136503,
-0.720574647014096));
#59746=CARTESIAN_POINT('Ctrl Pts',(-0.79099127576657,0.0924597375550537,
-0.7168538989189));
#59747=CARTESIAN_POINT('Ctrl Pts',(-0.791075294242739,-1.90178071996815E-5,
-0.713133150823704));
#59748=CARTESIAN_POINT('Origin',(0.,0.,-1.97));
#59749=CARTESIAN_POINT('',(-0.79106019175573,1.65874934803245E-5,-0.484666849176295));
#59750=CARTESIAN_POINT('',(-0.791054102114328,1.50443135659429E-5,-0.513133150823704));
#59751=CARTESIAN_POINT('',(-0.7911,-9.68818082805471E-17,-1.97));
#59752=CARTESIAN_POINT('Ctrl Pts',(-0.79106019175573,1.65874934803245E-5,
-0.484666849176295));
#59753=CARTESIAN_POINT('Ctrl Pts',(-0.791094293741917,0.044315349832207,
-0.486449047737811));
#59754=CARTESIAN_POINT('Ctrl Pts',(-0.787435186917273,0.0886085381329495,
-0.488231246299327));
#59755=CARTESIAN_POINT('Ctrl Pts',(-0.780032216716909,0.13226689472754,
-0.490013444860843));
#59756=CARTESIAN_POINT('Ctrl Pts',(-0.758145785074321,0.261340173610695,
-0.49528240663354));
#59757=CARTESIAN_POINT('Ctrl Pts',(-0.70353599197578,0.384864685004406,
-0.500551368406237));
#59758=CARTESIAN_POINT('Ctrl Pts',(-0.622798975472762,0.48792030774224,
-0.505820330178935));
#59759=CARTESIAN_POINT('Ctrl Pts',(-0.542061958969747,0.59097593048007,
-0.511089291951632));
#59760=CARTESIAN_POINT('Ctrl Pts',(-0.435197719062254,0.673562664562026,
-0.51635825372433));
#59761=CARTESIAN_POINT('Ctrl Pts',(-0.315114037289311,0.725705128864625,
-0.521627215497027));
#59762=CARTESIAN_POINT('Ctrl Pts',(-0.195030355516371,0.777847593167222,
-0.526896177269724));
#59763=CARTESIAN_POINT('Ctrl Pts',(-0.0617272318779785,0.799545787690465,
-0.532165139042421));
#59764=CARTESIAN_POINT('Ctrl Pts',(0.0686940859131107,0.788178858583351,
-0.537434100815118));
#59765=CARTESIAN_POINT('Ctrl Pts',(0.199115403704207,0.776811929476236,
-0.542703062587815));
#59766=CARTESIAN_POINT('Ctrl Pts',(0.326654915647992,0.732379876738765,
-0.547972024360513));
#59767=CARTESIAN_POINT('Ctrl Pts',(0.435907541811431,0.660249502498192,
-0.55324098613321));
#59768=CARTESIAN_POINT('Ctrl Pts',(0.545160167974864,0.588119128257622,
-0.558509947905907));
#59769=CARTESIAN_POINT('Ctrl Pts',(0.63612590835795,0.488290432513946,-0.563778909678605));
#59770=CARTESIAN_POINT('Ctrl Pts',(0.697817309108831,0.372821396469276,
-0.569047871451302));
#59771=CARTESIAN_POINT('Ctrl Pts',(0.759508709859716,0.2573523604246,-0.574316833223999));
#59772=CARTESIAN_POINT('Ctrl Pts',(0.7919257709784,0.12624298407893,-0.579585794996696));
#59773=CARTESIAN_POINT('Ctrl Pts',(0.791152941824015,-0.00467046040555037,
-0.584854756769393));
#59774=CARTESIAN_POINT('Ctrl Pts',(0.790380112669631,-0.135583904890027,
-0.59012371854209));
#59775=CARTESIAN_POINT('Ctrl Pts',(0.756417393242176,-0.266301417513306,
-0.595392680314788));
#59776=CARTESIAN_POINT('Ctrl Pts',(0.693367029187332,-0.381034058048786,
-0.600661642087485));
#59777=CARTESIAN_POINT('Ctrl Pts',(0.63031666513249,-0.495766698584263,
-0.605930603860182));
#59778=CARTESIAN_POINT('Ctrl Pts',(0.538178656450259,-0.594514467031945,
-0.611199565632879));
#59779=CARTESIAN_POINT('Ctrl Pts',(0.428082051440955,-0.665349943857589,
-0.616468527405576));
#59780=CARTESIAN_POINT('Ctrl Pts',(0.317985446431644,-0.736185420683236,
-0.621737489178273));
#59781=CARTESIAN_POINT('Ctrl Pts',(0.189930245095256,-0.779108605886844,
-0.627006450950971));
#59782=CARTESIAN_POINT('Ctrl Pts',(0.0593838157975924,-0.788934948508754,
-0.632275412723668));
#59783=CARTESIAN_POINT('Ctrl Pts',(-0.0711626135000637,-0.798761291130663,
-0.637544374496366));
#59784=CARTESIAN_POINT('Ctrl Pts',(-0.204200270759008,-0.775490791170876,
-0.642813336269063));
#59785=CARTESIAN_POINT('Ctrl Pts',(-0.323659973080967,-0.721934216104501,
-0.64808229804176));
#59786=CARTESIAN_POINT('Ctrl Pts',(-0.443119675402932,-0.668377641038123,
-0.653351259814458));
#59787=CARTESIAN_POINT('Ctrl Pts',(-0.549001422787913,-0.58453499086516,
-0.658620221587155));
#59788=CARTESIAN_POINT('Ctrl Pts',(-0.628516105750902,-0.480533344700359,
-0.663889183359853));
#59789=CARTESIAN_POINT('Ctrl Pts',(-0.708030788713888,-0.376531698535561,
-0.66915814513255));
#59790=CARTESIAN_POINT('Ctrl Pts',(-0.761178407254874,-0.252371056378931,
-0.674427106905247));
#59791=CARTESIAN_POINT('Ctrl Pts',(-0.781539434598224,-0.123048375548322,
-0.679696068677944));
#59792=CARTESIAN_POINT('Ctrl Pts',(-0.787942353048508,-0.082380359874697,
-0.681352995510728));
#59793=CARTESIAN_POINT('Ctrl Pts',(-0.791102974214916,-0.0412018652717124,
-0.683009922343512));
#59794=CARTESIAN_POINT('Ctrl Pts',(-0.79106797157506,-1.80494624554273E-5,
-0.684666849176296));
#59795=CARTESIAN_POINT('Ctrl Pts',(-0.791075294242739,-1.90178071996815E-5,
-0.713133150823704));
#59796=CARTESIAN_POINT('Ctrl Pts',(-0.791110254565405,-0.0384996862821712,
-0.711584937146203));
#59797=CARTESIAN_POINT('Ctrl Pts',(-0.788352301462993,-0.0769753867691262,
-0.710036723468702));
#59798=CARTESIAN_POINT('Ctrl Pts',(-0.782759138437657,-0.115034424293976,
-0.708488509791201));
#59799=CARTESIAN_POINT('Ctrl Pts',(-0.763724193457369,-0.244558931626677,
-0.703219548018504));
#59800=CARTESIAN_POINT('Ctrl Pts',(-0.711851489124143,-0.369257595916767,
-0.697950586245807));
#59801=CARTESIAN_POINT('Ctrl Pts',(-0.633406559502031,-0.474068473915013,
-0.692681624473109));
#59802=CARTESIAN_POINT('Ctrl Pts',(-0.554961629879913,-0.578879351913266,
-0.687412662700412));
#59803=CARTESIAN_POINT('Ctrl Pts',(-0.449944474968907,-0.663802443619672,
-0.682143700927715));
#59804=CARTESIAN_POINT('Ctrl Pts',(-0.331039772960799,-0.718580166925286,
-0.676874739155018));
#59805=CARTESIAN_POINT('Ctrl Pts',(-0.212135070952697,-0.773357890230898,
-0.67160577738232));
#59806=CARTESIAN_POINT('Ctrl Pts',(-0.0793428218474851,-0.797990245135722,
-0.666336815609623));
#59807=CARTESIAN_POINT('Ctrl Pts',(0.0512974335036988,-0.789501970166157,
-0.661067853836925));
#59808=CARTESIAN_POINT('Ctrl Pts',(0.18193768885489,-0.781013695196591,
-0.655798892064228));
#59809=CARTESIAN_POINT('Ctrl Pts',(0.310425950452053,-0.739404790352641,
-0.650529930291531));
#59810=CARTESIAN_POINT('Ctrl Pts',(0.42124254199886,-0.669701058973814,
-0.645260968518834));
#59811=CARTESIAN_POINT('Ctrl Pts',(0.532059133545661,-0.599997327594991,
-0.639992006746136));
#59812=CARTESIAN_POINT('Ctrl Pts',(0.625204055042095,-0.502198769681299,
-0.634723044973439));
#59813=CARTESIAN_POINT('Ctrl Pts',(0.689426636486842,-0.388118152735411,
-0.629454083200742));
#59814=CARTESIAN_POINT('Ctrl Pts',(0.753649217931591,-0.27403753578952,
-0.624185121428045));
#59815=CARTESIAN_POINT('Ctrl Pts',(0.788949459324651,-0.143674859811422,
-0.618916159655348));
#59816=CARTESIAN_POINT('Ctrl Pts',(0.791063560122737,-0.0127762054715168,
-0.61364719788265));
#59817=CARTESIAN_POINT('Ctrl Pts',(0.793177660920822,0.118122448868388,
-0.608378236109953));
#59818=CARTESIAN_POINT('Ctrl Pts',(0.762105621123936,0.249557081570111,
-0.603109274337256));
#59819=CARTESIAN_POINT('Ctrl Pts',(0.701600530652673,0.365652133821474,
-0.597840312564558));
#59820=CARTESIAN_POINT('Ctrl Pts',(0.641095440181409,0.481747186072837,
-0.592571350791861));
#59821=CARTESIAN_POINT('Ctrl Pts',(0.551157299035769,0.582502657873839,
-0.587302389019164));
#59822=CARTESIAN_POINT('Ctrl Pts',(0.442649440721279,0.65574862577778,-0.582033427246467));
#59823=CARTESIAN_POINT('Ctrl Pts',(0.334141582406789,0.728994593681721,
-0.576764465473769));
#59824=CARTESIAN_POINT('Ctrl Pts',(0.207064006923452,0.7747310576886,-0.571495503701072));
#59825=CARTESIAN_POINT('Ctrl Pts',(0.0767659984121724,0.787433660106102,
-0.566226541928375));
#59826=CARTESIAN_POINT('Ctrl Pts',(-0.053532010099107,0.800136262523604,
-0.560957580155678));
#59827=CARTESIAN_POINT('Ctrl Pts',(-0.187050451638326,0.779805003351729,
-0.55568861838298));
#59828=CARTESIAN_POINT('Ctrl Pts',(-0.307662070948674,0.728895628797348,
-0.550419656610283));
#59829=CARTESIAN_POINT('Ctrl Pts',(-0.428273690259019,0.677986254242969,
-0.545150694837586));
#59830=CARTESIAN_POINT('Ctrl Pts',(-0.535978487340491,0.596498764306088,
-0.539881733064889));
#59831=CARTESIAN_POINT('Ctrl Pts',(-0.617767152506043,0.494275766010113,
-0.534612771292192));
#59832=CARTESIAN_POINT('Ctrl Pts',(-0.6995558176716,0.392052767714133,-0.529343809519495));
#59833=CARTESIAN_POINT('Ctrl Pts',(-0.755428350921232,0.269094261059059,
-0.524074847746797));
#59834=CARTESIAN_POINT('Ctrl Pts',(-0.778636091956227,0.140252001352719,
-0.5188058859741));
#59835=CARTESIAN_POINT('Ctrl Pts',(-0.786964827547154,0.0940134160283837,
-0.516914974257301));
#59836=CARTESIAN_POINT('Ctrl Pts',(-0.79108656509169,0.0470170442338496,
-0.515024062540503));
#59837=CARTESIAN_POINT('Ctrl Pts',(-0.791054102114328,1.50443135659429E-5,
-0.513133150823704));
#59838=CARTESIAN_POINT('Origin',(0.,0.,-1.97));
#59839=CARTESIAN_POINT('',(-0.79116655976261,-1.23482099584349E-6,-0.284666849176295));
#59840=CARTESIAN_POINT('',(-0.791166451109383,1.58231152821223E-6,-0.313133150823703));
#59841=CARTESIAN_POINT('',(-0.7911,-9.68818082805471E-17,-1.97));
#59842=CARTESIAN_POINT('Ctrl Pts',(-0.79116655976261,-1.23482099584349E-6,
-0.284666849176295));
#59843=CARTESIAN_POINT('Ctrl Pts',(-0.79115461052684,0.12973093383712,-0.289888173132111));
#59844=CARTESIAN_POINT('Ctrl Pts',(-0.758584934860785,0.25946888427355,
-0.295109497087927));
#59845=CARTESIAN_POINT('Ctrl Pts',(-0.697289616848199,0.373807411251276,
-0.300330821043743));
#59846=CARTESIAN_POINT('Ctrl Pts',(-0.635435058466726,0.48918912916231,
-0.30559978281644));
#59847=CARTESIAN_POINT('Ctrl Pts',(-0.544328298014483,0.58888914215781,
-0.310868744589137));
#59848=CARTESIAN_POINT('Ctrl Pts',(-0.434973822423203,0.660865012229132,
-0.316137706361834));
#59849=CARTESIAN_POINT('Ctrl Pts',(-0.325619346831915,0.73284088230046,
-0.321406668134531));
#59850=CARTESIAN_POINT('Ctrl Pts',(-0.19801715610159,0.777092609447604,
-0.326675629907229));
#59851=CARTESIAN_POINT('Ctrl Pts',(-0.0675799010697838,0.788275172467602,
-0.331944591679926));
#59852=CARTESIAN_POINT('Ctrl Pts',(0.0628573539620148,0.799457735487599,
-0.337213553452623));
#59853=CARTESIAN_POINT('Ctrl Pts',(0.196129673295302,0.77757113438045,-0.342482515225321));
#59854=CARTESIAN_POINT('Ctrl Pts',(0.316139530039515,0.725258980018091,
-0.347751476998018));
#59855=CARTESIAN_POINT('Ctrl Pts',(0.436149386783728,0.672946825655733,
-0.353020438770715));
#59856=CARTESIAN_POINT('Ctrl Pts',(0.542896780938876,0.590209118038164,
-0.358289400543412));
#59857=CARTESIAN_POINT('Ctrl Pts',(0.623488044345385,0.487039473884327,
-0.363558362316109));
#59858=CARTESIAN_POINT('Ctrl Pts',(0.704079307751897,0.383869829730486,
-0.368827324088806));
#59859=CARTESIAN_POINT('Ctrl Pts',(0.758514440409767,0.260268249040376,
-0.374096285861504));
#59860=CARTESIAN_POINT('Ctrl Pts',(0.780218400948583,0.131164161930088,
-0.379365247634201));
#59861=CARTESIAN_POINT('Ctrl Pts',(0.801922361487399,0.00206007481979883,
-0.384634209406898));
#59862=CARTESIAN_POINT('Ctrl Pts',(0.79089514990716,-0.132546518710666,
-0.389903171179595));
#59863=CARTESIAN_POINT('Ctrl Pts',(0.748468706969074,-0.256396929090264,
-0.395172132952293));
#59864=CARTESIAN_POINT('Ctrl Pts',(0.70604226403099,-0.380247339469859,
-0.40044109472499));
#59865=CARTESIAN_POINT('Ctrl Pts',(0.632216589735061,-0.493341566698584,
-0.405710056497687));
#59866=CARTESIAN_POINT('Ctrl Pts',(0.535908845492088,-0.582019329472792,
-0.410979018270384));
#59867=CARTESIAN_POINT('Ctrl Pts',(0.439601101249111,-0.670697092247003,
-0.416247980043081));
#59868=CARTESIAN_POINT('Ctrl Pts',(0.320811287059081,-0.734958390566697,
-0.421516941815779));
#59869=CARTESIAN_POINT('Ctrl Pts',(0.19388763551772,-0.767041312675278,
-0.426785903588476));
#59870=CARTESIAN_POINT('Ctrl Pts',(0.0669639839763566,-0.79912423478386,
-0.432054865361174));
#59871=CARTESIAN_POINT('Ctrl Pts',(-0.0680935049163425,-0.799028780681332,
-0.437323827133871));
#59872=CARTESIAN_POINT('Ctrl Pts',(-0.19497167941313,-0.766766479955989,
-0.442592788906568));
#59873=CARTESIAN_POINT('Ctrl Pts',(-0.321849853909913,-0.734504179230648,
-0.447861750679266));
#59874=CARTESIAN_POINT('Ctrl Pts',(-0.440548714010772,-0.670075031882501,
-0.453130712451962));
#59875=CARTESIAN_POINT('Ctrl Pts',(-0.536731013164729,-0.581261223602832,
-0.45839967422466));
#59876=CARTESIAN_POINT('Ctrl Pts',(-0.632913312318683,-0.492447415323166,
-0.463668635997357));
#59877=CARTESIAN_POINT('Ctrl Pts',(-0.706579050525731,-0.379248946111975,
-0.468937597770054));
#59878=CARTESIAN_POINT('Ctrl Pts',(-0.748830384535933,-0.255338688320087,
-0.474206559542751));
#59879=CARTESIAN_POINT('Ctrl Pts',(-0.776790427406901,-0.17334042243865,
-0.477693322753933));
#59880=CARTESIAN_POINT('Ctrl Pts',(-0.790993473291565,-0.0866512497267257,
-0.481180085965114));
#59881=CARTESIAN_POINT('Ctrl Pts',(-0.79106019175573,1.65874934803245E-5,
-0.484666849176295));
#59882=CARTESIAN_POINT('Ctrl Pts',(-0.791054102114328,1.50443135659429E-5,
-0.513133150823704));
#59883=CARTESIAN_POINT('Ctrl Pts',(-0.790996108099315,-0.0839524445160384,
-0.509755100767805));
#59884=CARTESIAN_POINT('Ctrl Pts',(-0.777680141657789,-0.167937895294183,
-0.506377050711907));
#59885=CARTESIAN_POINT('Ctrl Pts',(-0.75140722465577,-0.247652923090808,
-0.502999000656008));
#59886=CARTESIAN_POINT('Ctrl Pts',(-0.710427667499956,-0.37198957507041,
-0.497730038883311));
#59887=CARTESIAN_POINT('Ctrl Pts',(-0.637925604367967,-0.485936866272008,
-0.492461077110613));
#59888=CARTESIAN_POINT('Ctrl Pts',(-0.542658322008323,-0.575731476589062,
-0.487192115337916));
#59889=CARTESIAN_POINT('Ctrl Pts',(-0.447391039648685,-0.665526086906111,
-0.481923153565219));
#59890=CARTESIAN_POINT('Ctrl Pts',(-0.329358538061393,-0.731168016338618,
-0.476654191792522));
#59891=CARTESIAN_POINT('Ctrl Pts',(-0.202817576535695,-0.764728591219457,
-0.471385230019825));
#59892=CARTESIAN_POINT('Ctrl Pts',(-0.0762766150099927,-0.798289166100297,
-0.466116268247127));
#59893=CARTESIAN_POINT('Ctrl Pts',(0.0587728064541182,-0.799768386429468,
-0.46084730647443));
#59894=CARTESIAN_POINT('Ctrl Pts',(0.186018510548951,-0.768987582028121,
-0.455578344701733));
#59895=CARTESIAN_POINT('Ctrl Pts',(0.313264214643783,-0.738206777626774,
-0.450309382929035));
#59896=CARTESIAN_POINT('Ctrl Pts',(0.432706201369339,-0.675165948494908,
-0.445040421156339));
#59897=CARTESIAN_POINT('Ctrl Pts',(0.529917464342802,-0.5874795899134,-0.439771459383641));
#59898=CARTESIAN_POINT('Ctrl Pts',(0.627128727316267,-0.49979323133189,
-0.434502497610944));
#59899=CARTESIAN_POINT('Ctrl Pts',(0.70210926653764,-0.387461343300735,
-0.429233535838246));
#59900=CARTESIAN_POINT('Ctrl Pts',(0.745802428249095,-0.264052126668259,
-0.423964574065549));
#59901=CARTESIAN_POINT('Ctrl Pts',(0.789495589960546,-0.140642910035794,
-0.418695612292852));
#59902=CARTESIAN_POINT('Ctrl Pts',(0.801901374162086,-0.00615636480201949,
-0.413426650520155));
#59903=CARTESIAN_POINT('Ctrl Pts',(0.781521326810997,0.123163319701733,
-0.408157688747459));
#59904=CARTESIAN_POINT('Ctrl Pts',(0.761141279459906,0.252483004205497,
-0.402888726974761));
#59905=CARTESIAN_POINT('Ctrl Pts',(0.707975400556178,0.376635827979229,
-0.397619765202064));
#59906=CARTESIAN_POINT('Ctrl Pts',(0.628445422485195,0.480625778061912,
-0.392350803429367));
#59907=CARTESIAN_POINT('Ctrl Pts',(0.548915444414215,0.584615728144593,
-0.387081841656669));
#59908=CARTESIAN_POINT('Ctrl Pts',(0.443021367175978,0.668442804536227,
-0.381812879883972));
#59909=CARTESIAN_POINT('Ctrl Pts',(0.323553789537451,0.721981809228146,
-0.376543918111275));
#59910=CARTESIAN_POINT('Ctrl Pts',(0.204086211898923,0.775520813920066,
-0.371274956338577));
#59911=CARTESIAN_POINT('Ctrl Pts',(0.0710451338601018,0.798771746912272,
-0.36600599456588));
#59912=CARTESIAN_POINT('Ctrl Pts',(-0.0594998484946793,0.788926204159485,
-0.360737032793183));
#59913=CARTESIAN_POINT('Ctrl Pts',(-0.190044830849464,0.779080661406699,
-0.355468071020486));
#59914=CARTESIAN_POINT('Ctrl Pts',(-0.318093717520211,0.736138642908918,
-0.350199109247788));
#59915=CARTESIAN_POINT('Ctrl Pts',(-0.428179902871407,0.665286974437921,
-0.34493014747509));
#59916=CARTESIAN_POINT('Ctrl Pts',(-0.538266088222596,0.594435305966928,
-0.339661185702393));
#59917=CARTESIAN_POINT('Ctrl Pts',(-0.630389572254237,0.49567398752272,
-0.334392223929696));
#59918=CARTESIAN_POINT('Ctrl Pts',(-0.693423061046085,0.380932075298852,
-0.329123262156999));
#59919=CARTESIAN_POINT('Ctrl Pts',(-0.756456549837934,0.266190163074982,
-0.323854300384302));
#59920=CARTESIAN_POINT('Ctrl Pts',(-0.790400043389989,0.135467657071449,
-0.318585338611605));
#59921=CARTESIAN_POINT('Ctrl Pts',(-0.791153618296685,0.00455410064966138,
-0.313316376838907));
#59922=CARTESIAN_POINT('Ctrl Pts',(-0.791162353384246,0.00303661198591406,
-0.313255301500506));
#59923=CARTESIAN_POINT('Ctrl Pts',(-0.791166628954472,0.00151909765194257,
-0.313194226162105));
#59924=CARTESIAN_POINT('Ctrl Pts',(-0.791166451109383,1.58231152821223E-6,
-0.313133150823703));
#59925=CARTESIAN_POINT('Origin',(0.,0.,-1.97));
#59926=CARTESIAN_POINT('',(-0.791053952037979,-1.51658468628413E-5,-0.0846668491762948));
#59927=CARTESIAN_POINT('',(-0.791061003003137,-1.6759841323199E-5,-0.113133150823703));
#59928=CARTESIAN_POINT('',(-0.7911,-9.68818082805471E-17,-1.97));
#59929=CARTESIAN_POINT('Ctrl Pts',(-0.791053952037979,-1.51658468628413E-5,
-0.0846668491762948));
#59930=CARTESIAN_POINT('Ctrl Pts',(-0.790995158012751,0.0842860903451894,
-0.0880583367537131));
#59931=CARTESIAN_POINT('Ctrl Pts',(-0.777571904683029,0.168605678640689,
-0.0914498243311313));
#59932=CARTESIAN_POINT('Ctrl Pts',(-0.751093386412371,0.248604311213447,
-0.0948413119085496));
#59933=CARTESIAN_POINT('Ctrl Pts',(-0.709956776773963,0.372888928884019,
-0.100110273681247));
#59934=CARTESIAN_POINT('Ctrl Pts',(-0.637309665005789,0.486744383675089,
-0.105379235453944));
#59935=CARTESIAN_POINT('Ctrl Pts',(-0.541928542890219,0.576418288786221,
-0.110648197226642));
#59936=CARTESIAN_POINT('Ctrl Pts',(-0.446547420774654,0.666092193897349,
-0.115917158999339));
#59937=CARTESIAN_POINT('Ctrl Pts',(-0.328432288311695,0.731584549328544,
-0.121186120772036));
#59938=CARTESIAN_POINT('Ctrl Pts',(-0.201849024586547,0.764984829366641,
-0.126455082544733));
#59939=CARTESIAN_POINT('Ctrl Pts',(-0.0752657608613988,0.798385109404738,
-0.131724044317431));
#59940=CARTESIAN_POINT('Ctrl Pts',(0.059785634125941,0.799693314049738,
-0.136993006090128));
#59941=CARTESIAN_POINT('Ctrl Pts',(0.186992304834312,0.768751387957727,
-0.142261967862825));
#59942=CARTESIAN_POINT('Ctrl Pts',(0.314198975542698,0.737809461865712,
-0.147530929635522));
#59943=CARTESIAN_POINT('Ctrl Pts',(0.433560921972116,0.674617405036678,
-0.15279989140822));
#59944=CARTESIAN_POINT('Ctrl Pts',(0.530661030277562,0.586808000298712,
-0.158068853180918));
#59945=CARTESIAN_POINT('Ctrl Pts',(0.627761138582997,0.498998595560756,
-0.163337814953615));
#59946=CARTESIAN_POINT('Ctrl Pts',(0.702599408764469,0.386571842913873,
-0.168606776726312));
#59947=CARTESIAN_POINT('Ctrl Pts',(0.746136256454843,0.263107390736065,
-0.173875738499009));
#59948=CARTESIAN_POINT('Ctrl Pts',(0.789673104145218,0.139642938558253,
-0.179144700271706));
#59949=CARTESIAN_POINT('Ctrl Pts',(0.801908529344493,0.00514078684952503,
-0.184413662044403));
#59950=CARTESIAN_POINT('Ctrl Pts',(0.781364713780323,-0.124152984456936,
-0.1896826238171));
#59951=CARTESIAN_POINT('Ctrl Pts',(0.760820898216154,-0.253446755763393,
-0.194951585589797));
#59952=CARTESIAN_POINT('Ctrl Pts',(0.707497841888538,-0.377532146667576,
-0.200220547362495));
#59953=CARTESIAN_POINT('Ctrl Pts',(0.627836232155951,-0.48142129203795,
-0.205489509135192));
#59954=CARTESIAN_POINT('Ctrl Pts',(0.548174622423359,-0.585310437408331,
-0.210758470907889));
#59955=CARTESIAN_POINT('Ctrl Pts',(0.44217445928579,-0.669003337244903,
-0.216027432680586));
#59956=CARTESIAN_POINT('Ctrl Pts',(0.322639170592942,-0.722390998837629,
-0.221296394453284));
#59957=CARTESIAN_POINT('Ctrl Pts',(0.203103881900095,-0.775778660430356,
-0.226565356225981));
#59958=CARTESIAN_POINT('Ctrl Pts',(0.0700334676519663,-0.798861083779237,
-0.231834317998678));
#59959=CARTESIAN_POINT('Ctrl Pts',(-0.0604989404678671,-0.788850219306804,
-0.237103279771376));
#59960=CARTESIAN_POINT('Ctrl Pts',(-0.191031348587693,-0.778839354834371,
-0.242372241544073));
#59961=CARTESIAN_POINT('Ctrl Pts',(-0.319025750579227,-0.735735202540627,
-0.24764120331677));
#59962=CARTESIAN_POINT('Ctrl Pts',(-0.429022117832896,-0.664744171429373,
-0.252910165089467));
#59963=CARTESIAN_POINT('Ctrl Pts',(-0.539018485086566,-0.593753140318119,
-0.258179126862164));
#59964=CARTESIAN_POINT('Ctrl Pts',(-0.631016817602374,-0.494875230389354,
-0.263448088634861));
#59965=CARTESIAN_POINT('Ctrl Pts',(-0.693904940149093,-0.380053580733699,
-0.268717050407559));
#59966=CARTESIAN_POINT('Ctrl Pts',(-0.756793062695816,-0.265231931078037,
-0.273986012180256));
#59967=CARTESIAN_POINT('Ctrl Pts',(-0.790570975273448,-0.134466541695481,
-0.279254973952954));
#59968=CARTESIAN_POINT('Ctrl Pts',(-0.791158753406913,-0.00355213559091441,
-0.284523935725651));
#59969=CARTESIAN_POINT('Ctrl Pts',(-0.791164067635465,-0.00236851028214306,
-0.284571573542532));
#59970=CARTESIAN_POINT('Ctrl Pts',(-0.791166668783906,-0.0011848727922128,
-0.284619211359413));
#59971=CARTESIAN_POINT('Ctrl Pts',(-0.79116655976261,-1.23482099584349E-6,
-0.284666849176295));
#59972=CARTESIAN_POINT('Ctrl Pts',(-0.791166451109383,1.58231152821223E-6,
-0.313133150823703));
#59973=CARTESIAN_POINT('Ctrl Pts',(-0.791151286281004,-0.129396760162562,
-0.307925264389407));
#59974=CARTESIAN_POINT('Ctrl Pts',(-0.7587555547792,-0.258802420434021,
-0.302717377955112));
#59975=CARTESIAN_POINT('Ctrl Pts',(-0.697762466787314,-0.37292402380272,
-0.297509491520816));
#59976=CARTESIAN_POINT('Ctrl Pts',(-0.636054084109908,-0.488383984993266,
-0.292240529748119));
#59977=CARTESIAN_POINT('Ctrl Pts',(-0.545073662493758,-0.588199300534319,
-0.286971567975422));
#59978=CARTESIAN_POINT('Ctrl Pts',(-0.435810429125493,-0.660313605371724,
-0.281702606202725));
#59979=CARTESIAN_POINT('Ctrl Pts',(-0.326547195757222,-0.732427910209133,
-0.276433644430027));
#59980=CARTESIAN_POINT('Ctrl Pts',(-0.199001150636833,-0.776841204342892,
-0.27116468265733));
#59981=CARTESIAN_POINT('Ctrl Pts',(-0.0685781627465269,-0.78818895144174,
-0.265895720884632));
#59982=CARTESIAN_POINT('Ctrl Pts',(0.0618448251437718,-0.799536698540587,
-0.260626759111935));
#59983=CARTESIAN_POINT('Ctrl Pts',(0.195144755803988,-0.777818898604527,
-0.255357797339238));
#59984=CARTESIAN_POINT('Ctrl Pts',(0.315220767050154,-0.725658773547022,
-0.250088835566541));
#59985=CARTESIAN_POINT('Ctrl Pts',(0.435296778296324,-0.673498648489515,
-0.244819873793844));
#59986=CARTESIAN_POINT('Ctrl Pts',(0.542148870128444,-0.590896198310561,
-0.239550912021147));
#59987=CARTESIAN_POINT('Ctrl Pts',(0.622870728608792,-0.487828702451327,
-0.23428195024845));
#59988=CARTESIAN_POINT('Ctrl Pts',(0.703592587089139,-0.384761206592094,
-0.229012988475753));
#59989=CARTESIAN_POINT('Ctrl Pts',(0.758184212217714,-0.261228665052582,
-0.223744026703055));
#59990=CARTESIAN_POINT('Ctrl Pts',(0.780051659854463,-0.132152168891571,
-0.218475064930358));
#59991=CARTESIAN_POINT('Ctrl Pts',(0.801919107491212,-0.00307567273056075,
-0.21320610315766));
#59992=CARTESIAN_POINT('Ctrl Pts',(0.791062377636135,0.131544778051948,
-0.207937141384963));
#59993=CARTESIAN_POINT('Ctrl Pts',(0.748792820183465,0.255448820028436,
-0.202668179612266));
#59994=CARTESIAN_POINT('Ctrl Pts',(0.706523262730795,0.379352862004923,
-0.197399217839568));
#59995=CARTESIAN_POINT('Ctrl Pts',(0.632840877680532,0.492540495175389,
-0.192130256066871));
#59996=CARTESIAN_POINT('Ctrl Pts',(0.536645516940195,0.581340156202204,
-0.186861294294174));
#59997=CARTESIAN_POINT('Ctrl Pts',(0.440450156199858,0.670139817229018,
-0.181592332521477));
#59998=CARTESIAN_POINT('Ctrl Pts',(0.321741819769446,0.734551506112182,
-0.176323370748779));
#59999=CARTESIAN_POINT('Ctrl Pts',(0.194858902845346,0.766795145591679,
-0.171054408976082));
#60000=CARTESIAN_POINT('Ctrl Pts',(0.0679759859212461,0.799038785071176,
-0.165785447203385));
#60001=CARTESIAN_POINT('Ctrl Pts',(-0.0670815114965426,0.799114375147006,
-0.160516485430688));
#60002=CARTESIAN_POINT('Ctrl Pts',(-0.194000444516933,0.767012786166758,
-0.155247523657991));
#60003=CARTESIAN_POINT('Ctrl Pts',(-0.320919377537324,0.734911197186511,
-0.149978561885293));
#60004=CARTESIAN_POINT('Ctrl Pts',(-0.439699746160317,0.670632429150186,
-0.144709600112596));
#60005=CARTESIAN_POINT('Ctrl Pts',(-0.535994443260468,0.581940502701097,
-0.139440638339899));
#60006=CARTESIAN_POINT('Ctrl Pts',(-0.632289140360619,0.493248576252007,
-0.134171676567201));
#60007=CARTESIAN_POINT('Ctrl Pts',(-0.706098165937928,0.380143491390153,
-0.128902714794504));
#60008=CARTESIAN_POINT('Ctrl Pts',(-0.748506399712542,0.256286843270204,
-0.123633753021807));
#60009=CARTESIAN_POINT('Ctrl Pts',(-0.776678426258576,0.174008180185989,
-0.120133552289106));
#60010=CARTESIAN_POINT('Ctrl Pts',(-0.790993223398756,0.0869848316978164,
-0.116633351556404));
#60011=CARTESIAN_POINT('Ctrl Pts',(-0.791061003003137,-1.6759841323199E-5,
-0.113133150823703));
#60012=CARTESIAN_POINT('Origin',(0.,0.,-4.318617978381));
#60013=CARTESIAN_POINT('',(-0.676660610977248,-1.2972732373197E-5,-0.0186179783810009));
#60014=CARTESIAN_POINT('',(-0.6767,-7.33509820392354E-14,0.));
#60015=CARTESIAN_POINT('',(-0.6767,-7.33509820392354E-14,-4.318617978381));
#60016=CARTESIAN_POINT('',(-0.564209944071419,-0.373617490236908,0.));
#60017=CARTESIAN_POINT('Ctrl Pts',(-0.676660610977247,-1.2972732373228E-5,
-0.0186179783810009));
#60018=CARTESIAN_POINT('Ctrl Pts',(-0.676688451778648,-0.0399322421209059,
-0.0167405041857218));
#60019=CARTESIAN_POINT('Ctrl Pts',(-0.66520014873097,-0.171869541427616,
-0.0105345113920551));
#60020=CARTESIAN_POINT('Ctrl Pts',(-0.614942795555724,-0.296874006669216,
-0.00432851859838854));
#60021=CARTESIAN_POINT('Ctrl Pts',(-0.56421801023762,-0.373640954068593,
-1.08756319922021E-15));
#60022=CARTESIAN_POINT('Origin',(0.,0.,0.));
#60023=CARTESIAN_POINT('Origin',(0.,0.,-4.318617978381));
#60024=CARTESIAN_POINT('',(-0.676756934637034,-1.05625507715145E-6,-0.218617978381));
#60025=CARTESIAN_POINT('',(-0.676666642310989,-1.43362213473885E-5,-0.179182021618993));
#60026=CARTESIAN_POINT('',(-0.6767,-7.33509820392354E-14,-4.318617978381));
#60027=CARTESIAN_POINT('Ctrl Pts',(-0.676756934637034,-1.05625507717112E-6,
-0.218617978381));
#60028=CARTESIAN_POINT('Ctrl Pts',(-0.676757027892895,-0.00101352979207305,
-0.218570340564119));
#60029=CARTESIAN_POINT('Ctrl Pts',(-0.676508707702974,-0.114010189902111,
-0.21325374097454));
#60030=CARTESIAN_POINT('Ctrl Pts',(-0.618460816691914,-0.338732633997832,
-0.202668179612265));
#60031=CARTESIAN_POINT('Ctrl Pts',(-0.382377116982208,-0.592470524209418,
-0.186861294294173));
#60032=CARTESIAN_POINT('Ctrl Pts',(-0.0539212511207285,-0.703083265419793,
-0.171054408976082));
#60033=CARTESIAN_POINT('Ctrl Pts',(0.287560543804209,-0.643849758100151,
-0.155247523657989));
#60034=CARTESIAN_POINT('Ctrl Pts',(0.559575372758286,-0.429079241151316,
-0.139440638339898));
#60035=CARTESIAN_POINT('Ctrl Pts',(0.696411596561459,-0.110654576665681,
-0.123633753021806));
#60036=CARTESIAN_POINT('Ctrl Pts',(0.665013370424364,0.234501305250519,
-0.107826867703715));
#60037=CARTESIAN_POINT('Ctrl Pts',(0.472965371062188,0.523007879069813,
-0.0920199823856229));
#60038=CARTESIAN_POINT('Ctrl Pts',(0.166661885477124,0.685169672229466,
-0.076213097067531));
#60039=CARTESIAN_POINT('Ctrl Pts',(-0.179903450085766,0.681812591898513,
-0.0604062117494397));
#60040=CARTESIAN_POINT('Ctrl Pts',(-0.483007394483508,0.513747833004724,
-0.0445993264313473));
#60041=CARTESIAN_POINT('Ctrl Pts',(-0.647289724438253,0.256278004736498,
-0.0306699153085348));
#60042=CARTESIAN_POINT('Ctrl Pts',(-0.676610319083845,0.0720975822735199,
-0.0220094659584191));
#60043=CARTESIAN_POINT('Ctrl Pts',(-0.676660610977247,-1.2972732373228E-5,
-0.0186179783810009));
#60044=CARTESIAN_POINT('',(-0.537060862935905,0.411689834101525,0.));
#60045=CARTESIAN_POINT('Origin',(0.,0.,0.));
#60046=CARTESIAN_POINT('Ctrl Pts',(-0.676666642310989,-1.43362213474128E-5,
-0.179182021618993));
#60047=CARTESIAN_POINT('Ctrl Pts',(-0.676695940449894,-0.0376212939135734,
-0.177413260578998));
#60048=CARTESIAN_POINT('Ctrl Pts',(-0.664430133622077,-0.187236698051038,
-0.170375537766307));
#60049=CARTESIAN_POINT('Ctrl Pts',(-0.555635984344507,-0.434168324449232,
-0.158068853180918));
#60050=CARTESIAN_POINT('Ctrl Pts',(-0.281672681898704,-0.646447338792661,
-0.142261967862826));
#60051=CARTESIAN_POINT('Ctrl Pts',(0.0603360297254143,-0.702561900375898,
-0.126455082544735));
#60052=CARTESIAN_POINT('Ctrl Pts',(0.38776765641086,-0.588956040974949,
-0.110648197226643));
#60053=CARTESIAN_POINT('Ctrl Pts',(0.621527851581432,-0.333074272139639,
-0.0948413119085513));
#60054=CARTESIAN_POINT('Ctrl Pts',(0.705137669332003,0.00326985369309036,
-0.0790344265904595));
#60055=CARTESIAN_POINT('Ctrl Pts',(0.618416201049889,0.338823176482188,
-0.0632275412723679));
#60056=CARTESIAN_POINT('Ctrl Pts',(0.38227975109817,0.59252757256583,-0.0474206559542765));
#60057=CARTESIAN_POINT('Ctrl Pts',(0.0538381161213402,0.703089501623881,
-0.0316137706361843));
#60058=CARTESIAN_POINT('Ctrl Pts',(-0.287697821498663,0.643811669165333,
-0.015806885318092));
#60059=CARTESIAN_POINT('Ctrl Pts',(-0.468914126304642,0.500589151378386,
-0.00526896177269799));
#60060=CARTESIAN_POINT('Ctrl Pts',(-0.537060862935893,0.41168983410154,
-8.88178419700125E-16));
#60061=CARTESIAN_POINT('Origin',(0.,0.,-4.318617978381));
#60062=CARTESIAN_POINT('',(-0.676665948377073,1.41887963584822E-5,-0.418617978380999));
#60063=CARTESIAN_POINT('',(-0.676756841696018,1.35349531268708E-6,-0.379182021618994));
#60064=CARTESIAN_POINT('',(-0.6767,-7.33509820392354E-14,-4.318617978381));
#60065=CARTESIAN_POINT('Ctrl Pts',(-0.676665948377073,1.41887963584705E-5,
-0.418617978380999));
#60066=CARTESIAN_POINT('Ctrl Pts',(-0.676608877988115,-0.0741207188599466,
-0.415131215169819));
#60067=CARTESIAN_POINT('Ctrl Pts',(-0.646100723357651,-0.260329135516356,
-0.406375490185941));
#60068=CARTESIAN_POINT('Ctrl Pts',(-0.478375468842551,-0.518064176544559,
-0.392350803429365));
#60069=CARTESIAN_POINT('Ctrl Pts',(-0.173773577942818,-0.683400558836909,
-0.376543918111274));
#60070=CARTESIAN_POINT('Ctrl Pts',(0.172807395639615,-0.68364551064267,
-0.360737032793182));
#60071=CARTESIAN_POINT('Ctrl Pts',(0.477642690529216,-0.518739858109735,
-0.34493014747509));
#60072=CARTESIAN_POINT('Ctrl Pts',(0.667092192979181,-0.228520428584966,
-0.329123262156999));
#60073=CARTESIAN_POINT('Ctrl Pts',(0.695389933124598,0.11690346918548,-0.313316376838907));
#60074=CARTESIAN_POINT('Ctrl Pts',(0.555699928310104,0.434086592632565,
-0.297509491520815));
#60075=CARTESIAN_POINT('Ctrl Pts',(0.281767574784161,0.646405920447539,
-0.281702606202724));
#60076=CARTESIAN_POINT('Ctrl Pts',(-0.0602323436566084,0.702570740201827,
-0.265895720884633));
#60077=CARTESIAN_POINT('Ctrl Pts',(-0.387681727301688,0.589013122604281,
-0.25008883556654));
#60078=CARTESIAN_POINT('Ctrl Pts',(-0.62077289895915,0.333936630716867,
-0.23432958806533));
#60079=CARTESIAN_POINT('Ctrl Pts',(-0.676746713365588,0.110970702727291,
-0.223839302336816));
#60080=CARTESIAN_POINT('Ctrl Pts',(-0.676756934637034,-1.05625507717112E-6,
-0.218617978381));
#60081=CARTESIAN_POINT('Ctrl Pts',(-0.676756841696018,1.35349531267905E-6,
-0.379182021618994));
#60082=CARTESIAN_POINT('Ctrl Pts',(-0.676743869834842,-0.11068485349773,
-0.373974135184699));
#60083=CARTESIAN_POINT('Ctrl Pts',(-0.620996840527473,-0.333367929361865,
-0.363497286977708));
#60084=CARTESIAN_POINT('Ctrl Pts',(-0.388427374670541,-0.588521666917222,
-0.347751476998018));
#60085=CARTESIAN_POINT('Ctrl Pts',(-0.0611220704120482,-0.702493893463718,
-0.331944591679926));
#60086=CARTESIAN_POINT('Ctrl Pts',(0.280948703489239,-0.646762246832194,
-0.316137706361835));
#60087=CARTESIAN_POINT('Ctrl Pts',(0.555149729438401,-0.434790013096512,
-0.300330821043743));
#60088=CARTESIAN_POINT('Ctrl Pts',(0.695241321112673,-0.117784056100728,
-0.284523935725652));
#60089=CARTESIAN_POINT('Ctrl Pts',(0.667381066683655,0.227675401785218,
-0.268717050407559));
#60090=CARTESIAN_POINT('Ctrl Pts',(0.47829926932486,0.518134527179428,-0.252910165089469));
#60091=CARTESIAN_POINT('Ctrl Pts',(0.173673060517654,0.683426108018395,
-0.237103279771376));
#60092=CARTESIAN_POINT('Ctrl Pts',(-0.172907934941646,0.683620085281621,
-0.221296394453285));
#60093=CARTESIAN_POINT('Ctrl Pts',(-0.477718990865722,0.518669602421621,
-0.205489509135192));
#60094=CARTESIAN_POINT('Ctrl Pts',(-0.645931503859681,0.260900441967383,
-0.191451384857095));
#60095=CARTESIAN_POINT('Ctrl Pts',(-0.676608664232016,0.0744060619515273,
-0.182682222351695));
#60096=CARTESIAN_POINT('Ctrl Pts',(-0.676666642310989,-1.43362213474128E-5,
-0.179182021618993));
#60097=CARTESIAN_POINT('Origin',(0.,0.,-4.318617978381));
#60098=CARTESIAN_POINT('',(-0.676672603166279,-1.54393518830496E-5,-0.618617978381001));
#60099=CARTESIAN_POINT('',(-0.676660739351239,1.28687737398769E-5,-0.579182021618993));
#60100=CARTESIAN_POINT('',(-0.6767,-7.33509820392354E-14,-4.318617978381));
#60101=CARTESIAN_POINT('Ctrl Pts',(-0.676672603166279,-1.54393518830773E-5,
-0.618617978381001));
#60102=CARTESIAN_POINT('Ctrl Pts',(-0.676702544117346,-0.0352437141061704,
-0.616961051548217));
#60103=CARTESIAN_POINT('Ctrl Pts',(-0.665401738435777,-0.182477482807531,
-0.610035162942737));
#60104=CARTESIAN_POINT('Ctrl Pts',(-0.560181318740991,-0.428287835856923,
-0.597840312564558));
#60105=CARTESIAN_POINT('Ctrl Pts',(-0.288470365174735,-0.643442638177916,
-0.582033427246467));
#60106=CARTESIAN_POINT('Ctrl Pts',(0.0529273696266406,-0.703158782746691,
-0.566226541928374));
#60107=CARTESIAN_POINT('Ctrl Pts',(0.381539257166764,-0.593010434520368,
-0.550419656610283));
#60108=CARTESIAN_POINT('Ctrl Pts',(0.617981390178772,-0.339606509952495,
-0.534612771292191));
#60109=CARTESIAN_POINT('Ctrl Pts',(0.70513562694994,-0.00416266925407728,
-0.518805885974099));
#60110=CARTESIAN_POINT('Ctrl Pts',(0.621947817852421,0.33228676181577,-0.502999000656008));
#60111=CARTESIAN_POINT('Ctrl Pts',(0.388513928898186,0.588464533562985,
-0.487192115337916));
#60112=CARTESIAN_POINT('Ctrl Pts',(0.0612253899055303,0.702484897944656,
-0.471385230019824));
#60113=CARTESIAN_POINT('Ctrl Pts',(-0.280853577732319,0.646803562207529,
-0.455578344701733));
#60114=CARTESIAN_POINT('Ctrl Pts',(-0.555085777752791,0.434871658706356,
-0.439771459383642));
#60115=CARTESIAN_POINT('Ctrl Pts',(-0.664311591163683,0.187808550285201,
-0.42745133727673));
#60116=CARTESIAN_POINT('Ctrl Pts',(-0.676695118916897,0.037906961485815,
-0.420400176942516));
#60117=CARTESIAN_POINT('Ctrl Pts',(-0.676665948377073,1.41887963584705E-5,
-0.418617978380999));
#60118=CARTESIAN_POINT('Ctrl Pts',(-0.676660739351239,1.28687737398527E-5,
-0.579182021618993));
#60119=CARTESIAN_POINT('Ctrl Pts',(-0.676611131779544,-0.0718121845582891,
-0.575803971563096));
#60120=CARTESIAN_POINT('Ctrl Pts',(-0.647454493003157,-0.255706719105382,
-0.567156959734502));
#60121=CARTESIAN_POINT('Ctrl Pts',(-0.483658336941455,-0.513135645762089,
-0.55324098613321));
#60122=CARTESIAN_POINT('Ctrl Pts',(-0.18076643772218,-0.681584237521583,
-0.537434100815119));
#60123=CARTESIAN_POINT('Ctrl Pts',(0.165793833437332,-0.685380173800492,
-0.521627215497027));
#60124=CARTESIAN_POINT('Ctrl Pts',(0.47230271632388,-0.523606457177304,
-0.505820330178935));
#60125=CARTESIAN_POINT('Ctrl Pts',(0.66471580275202,-0.235343322438281,
-0.490013444860844));
#60126=CARTESIAN_POINT('Ctrl Pts',(0.696551199677241,0.109772510552645,
-0.474206559542751));
#60127=CARTESIAN_POINT('Ctrl Pts',(0.560118320442681,0.428370219493409,
-0.458399674224661));
#60128=CARTESIAN_POINT('Ctrl Pts',(0.288375726331517,0.643485056786609,
-0.442592788906568));
#60129=CARTESIAN_POINT('Ctrl Pts',(-0.0530307867851691,0.703150989118139,
-0.426785903588478));
#60130=CARTESIAN_POINT('Ctrl Pts',(-0.381626469796513,0.59295431138796,
-0.410979018270385));
#60131=CARTESIAN_POINT('Ctrl Pts',(-0.618031330032434,0.339515615175607,
-0.395172132952294));
#60132=CARTESIAN_POINT('Ctrl Pts',(-0.67643782299757,0.114581693286516,
-0.384573134068496));
#60133=CARTESIAN_POINT('Ctrl Pts',(-0.676756993823146,0.00129942280498109,
-0.379243096957396));
#60134=CARTESIAN_POINT('Ctrl Pts',(-0.676756841696018,1.35349531267905E-6,
-0.379182021618994));
#60135=CARTESIAN_POINT('Origin',(0.,0.,-4.318617978381));
#60136=CARTESIAN_POINT('',(-0.676755273642671,3.79787743738244E-6,-0.818617978381));
#60137=CARTESIAN_POINT('',(-0.676678866911972,-1.62676655498795E-5,-0.779182021618994));
#60138=CARTESIAN_POINT('',(-0.6767,-7.33509820392354E-14,-4.318617978381));
#60139=CARTESIAN_POINT('Ctrl Pts',(-0.676755273642671,3.797877437383E-6,
-0.818617978381));
#60140=CARTESIAN_POINT('Ctrl Pts',(-0.676721587681226,-0.108306264839717,
-0.813521926153917));
#60141=CARTESIAN_POINT('Ctrl Pts',(-0.622843396402541,-0.328633681308047,
-0.803156912154136));
#60142=CARTESIAN_POINT('Ctrl Pts',(-0.394608777314782,-0.584394980364765,
-0.787522936381659));
#60143=CARTESIAN_POINT('Ctrl Pts',(-0.0685229122472805,-0.701810651605228,
-0.771716051063567));
#60144=CARTESIAN_POINT('Ctrl Pts',(0.274116269111402,-0.649687502741008,
-0.755909165745476));
#60145=CARTESIAN_POINT('Ctrl Pts',(0.550536237737494,-0.440617102649509,
-0.740102280427383));
#60146=CARTESIAN_POINT('Ctrl Pts',(0.6939612682597,-0.125105309099136,-0.724295395109291));
#60147=CARTESIAN_POINT('Ctrl Pts',(0.669743681289579,0.220628605539007,
-0.7084885097912));
#60148=CARTESIAN_POINT('Ctrl Pts',(0.483733802853534,0.513064506847101,
-0.692681624473108));
#60149=CARTESIAN_POINT('Ctrl Pts',(0.180866680953096,0.681557645346608,
-0.676874739155017));
#60150=CARTESIAN_POINT('Ctrl Pts',(-0.165693028990715,0.685404552328976,
-0.661067853836925));
#60151=CARTESIAN_POINT('Ctrl Pts',(-0.47222570233939,0.523675917204019,
-0.645260968518833));
#60152=CARTESIAN_POINT('Ctrl Pts',(-0.644507402220349,0.265654755031154,
-0.631111010033525));
#60153=CARTESIAN_POINT('Ctrl Pts',(-0.676607333077552,0.0767808058218464,
-0.622230013320914));
#60154=CARTESIAN_POINT('Ctrl Pts',(-0.676672603166279,-1.54393518830773E-5,
-0.618617978381001));
#60155=CARTESIAN_POINT('Ctrl Pts',(-0.676678866911972,-1.62676655498725E-5,
-0.779182021618994));
#60156=CARTESIAN_POINT('Ctrl Pts',(-0.676708771665283,-0.0329322939036839,
-0.777633807941494));
#60157=CARTESIAN_POINT('Ctrl Pts',(-0.666320931935935,-0.177851150494438,
-0.770816632491298));
#60158=CARTESIAN_POINT('Ctrl Pts',(-0.564540062783472,-0.422525851702685,
-0.758730495268403));
#60159=CARTESIAN_POINT('Ctrl Pts',(-0.295047803669792,-0.640453254651953,
-0.742923609950312));
#60160=CARTESIAN_POINT('Ctrl Pts',(0.045720171186077,-0.703664155539672,
-0.727116724632219));
#60161=CARTESIAN_POINT('Ctrl Pts',(0.375443366570243,-0.596888478983344,
-0.711309839314129));
#60162=CARTESIAN_POINT('Ctrl Pts',(0.614469412746345,-0.345920393506668,
-0.695502953996035));
#60163=CARTESIAN_POINT('Ctrl Pts',(0.705055963185025,-0.0113871252686242,
-0.679696068677945));
#60164=CARTESIAN_POINT('Ctrl Pts',(0.625319712405524,0.325896970102082,
-0.663889183359852));
#60165=CARTESIAN_POINT('Ctrl Pts',(0.394522821570273,0.584453010176933,
-0.648082298041761));
#60166=CARTESIAN_POINT('Ctrl Pts',(0.0684196917652833,0.701820720428935,
-0.632275412723669));
#60167=CARTESIAN_POINT('Ctrl Pts',(-0.274211819002972,0.649647178215781,
-0.616468527405578));
#60168=CARTESIAN_POINT('Ctrl Pts',(-0.550601034721718,0.440536126110014,
-0.600661642087486));
#60169=CARTESIAN_POINT('Ctrl Pts',(-0.663338570721139,0.192434988319684,
-0.588232806825291));
#60170=CARTESIAN_POINT('Ctrl Pts',(-0.676688507897296,0.0402179671760706,
-0.581072933335794));
#60171=CARTESIAN_POINT('Ctrl Pts',(-0.676660739351239,1.28687737398527E-5,
-0.579182021618993));
#60172=CARTESIAN_POINT('Origin',(0.,0.,-4.318617978381));
#60173=CARTESIAN_POINT('',(-0.676656001156398,1.13078348284983E-5,-1.018617978381));
#60174=CARTESIAN_POINT('',(-0.676752484899457,6.08590203556372E-6,-0.979182021618994));
#60175=CARTESIAN_POINT('',(-0.6767,-7.33509820392354E-14,-4.318617978381));
#60176=CARTESIAN_POINT('Ctrl Pts',(-0.676656001156398,1.13078348284897E-5,
-1.018617978381));
#60177=CARTESIAN_POINT('Ctrl Pts',(-0.67661425195553,-0.0694372891457709,
-1.01535176253231));
#60178=CARTESIAN_POINT('Ctrl Pts',(-0.648819209846495,-0.250950949327346,
-1.00681658491093));
#60179=CARTESIAN_POINT('Ctrl Pts',(-0.489039886595606,-0.508009418739415,
-0.99301244551685));
#60180=CARTESIAN_POINT('Ctrl Pts',(-0.187940247738363,-0.67964111374272,
-0.977205560198759));
#60181=CARTESIAN_POINT('Ctrl Pts',(0.158560765091847,-0.687089560379787,
-0.961398674880666));
#60182=CARTESIAN_POINT('Ctrl Pts',(0.466757706920742,-0.528555411702021,
-0.945591789562577));
#60183=CARTESIAN_POINT('Ctrl Pts',(0.662198379341202,-0.242336308891769,
-0.929784904244484));
#60184=CARTESIAN_POINT('Ctrl Pts',(0.697669504916014,0.102424812031291,
-0.913978018926392));
#60185=CARTESIAN_POINT('Ctrl Pts',(0.564602201477338,0.422442817782887,
-0.898171133608301));
#60186=CARTESIAN_POINT('Ctrl Pts',(0.295141996551584,0.640409854765639,
-0.882364248290208));
#60187=CARTESIAN_POINT('Ctrl Pts',(-0.0456166786157439,0.703670873947096,
-0.866557362972117));
#60188=CARTESIAN_POINT('Ctrl Pts',(-0.375355575368597,0.596943692695645,
-0.850750477654026));
#60189=CARTESIAN_POINT('Ctrl Pts',(-0.614418530936816,0.346010764356899,
-0.834943592335933));
#60190=CARTESIAN_POINT('Ctrl Pts',(-0.6758338184604,0.119338197594593,-0.824232759244925));
#60191=CARTESIAN_POINT('Ctrl Pts',(-0.676756416610606,0.00367876879518259,
-0.818790887926614));
#60192=CARTESIAN_POINT('Ctrl Pts',(-0.676755273642671,3.797877437383E-6,
-0.818617978381));
#60193=CARTESIAN_POINT('Ctrl Pts',(-0.676752484899457,6.08590203554811E-6,
-0.979182021618994));
#60194=CARTESIAN_POINT('Ctrl Pts',(-0.67670218702431,-0.10599468821923,
-0.974194682547194));
#60195=CARTESIAN_POINT('Ctrl Pts',(-0.624609057349418,-0.324029546701264,
-0.963938381702699));
#60196=CARTESIAN_POINT('Ctrl Pts',(-0.400575654252081,-0.580321224034726,
-0.948413119085501));
#60197=CARTESIAN_POINT('Ctrl Pts',(-0.07570992285693,-0.701071740569853,
-0.932606233767413));
#60198=CARTESIAN_POINT('Ctrl Pts',(0.267445315774999,-0.652461938288095,
-0.916799348449319));
#60199=CARTESIAN_POINT('Ctrl Pts',(0.545992866884217,-0.446234654813134,
-0.900992463131228));
#60200=CARTESIAN_POINT('Ctrl Pts',(0.69264303765959,-0.132208926424586,
-0.885185577813137));
#60201=CARTESIAN_POINT('Ctrl Pts',(0.671969040456129,0.213754968393986,
-0.869378692495044));
#60202=CARTESIAN_POINT('Ctrl Pts',(0.488965164096191,0.508081338119234,
-0.853571807176953));
#60203=CARTESIAN_POINT('Ctrl Pts',(0.187840286290136,0.679668746295639,
-0.837764921858861));
#60204=CARTESIAN_POINT('Ctrl Pts',(-0.158661817457009,0.687066230814675,
-0.821958036540769));
#60205=CARTESIAN_POINT('Ctrl Pts',(-0.466835438634391,0.528486755822397,
-0.806151151222678));
#60206=CARTESIAN_POINT('Ctrl Pts',(-0.64309559662951,0.270275607400248,
-0.791892479582085));
#60207=CARTESIAN_POINT('Ctrl Pts',(-0.67660699824453,0.0790892483926756,
-0.782902769714191));
#60208=CARTESIAN_POINT('Ctrl Pts',(-0.676678866911972,-1.62676655498725E-5,
-0.779182021618994));
#60209=CARTESIAN_POINT('Origin',(0.,0.,-4.318617978381));
#60210=CARTESIAN_POINT('',(-0.676685704046724,-1.6852225544519E-5,-1.218617978381));
#60211=CARTESIAN_POINT('',(-0.676652044953461,9.61824139306122E-6,-1.17918202161899));
#60212=CARTESIAN_POINT('',(-0.6767,-7.33509820392354E-14,-4.318617978381));
#60213=CARTESIAN_POINT('Ctrl Pts',(-0.676685704046724,-1.68522255445426E-5,
-1.218617978381));
#60214=CARTESIAN_POINT('Ctrl Pts',(-0.676714928392431,-0.0305543246826664,
-1.21718159891071));
#60215=CARTESIAN_POINT('Ctrl Pts',(-0.667240586817943,-0.173092095040201,
-1.21047625766773));
#60216=CARTESIAN_POINT('Ctrl Pts',(-0.568962098984759,-0.416552169755792,
-1.19850195465204));
#60217=CARTESIAN_POINT('Ctrl Pts',(-0.301781748310929,-0.637307897798075,
-1.18269506933395));
#60218=CARTESIAN_POINT('Ctrl Pts',(0.0383010603417563,-0.704106958484362,
-1.16688818401586));
#60219=CARTESIAN_POINT('Ctrl Pts',(0.369131349722688,-0.600812472291737,
-1.15108129869777));
#60220=CARTESIAN_POINT('Ctrl Pts',(0.610789305579622,-0.352377644578884,
-1.13527441337968));
#60221=CARTESIAN_POINT('Ctrl Pts',(0.704896781882463,-0.0188177336879362,
-1.11946752806159));
#60222=CARTESIAN_POINT('Ctrl Pts',(0.628719910943502,0.319288042044476,
-1.10366064274349));
#60223=CARTESIAN_POINT('Ctrl Pts',(0.4006610022585,0.580262304030356,-1.0878537574254));
#60224=CARTESIAN_POINT('Ctrl Pts',(0.0758130331203709,0.701060599533658,
-1.07204687210731));
#60225=CARTESIAN_POINT('Ctrl Pts',(-0.267349351956566,0.65250126759862,
-1.05623998678922));
#60226=CARTESIAN_POINT('Ctrl Pts',(-0.545927231821457,0.446314953553164,
-1.04043310147113));
#60227=CARTESIAN_POINT('Ctrl Pts',(-0.662311355964471,0.197194252937781,
-1.02789243200172));
#60228=CARTESIAN_POINT('Ctrl Pts',(-0.676681600518395,0.04259511153144,
-1.02062072430501));
#60229=CARTESIAN_POINT('Ctrl Pts',(-0.676656001156398,1.13078348284897E-5,
-1.018617978381));
#60230=CARTESIAN_POINT('Ctrl Pts',(-0.676652044953461,9.61824139304387E-6,
-1.17918202161899));
#60231=CARTESIAN_POINT('Ctrl Pts',(-0.676617978265195,-0.0671285662727804,
-1.17602451892559));
#60232=CARTESIAN_POINT('Ctrl Pts',(-0.650118825411559,-0.24632733355921,
-1.16759805445949));
#60233=CARTESIAN_POINT('Ctrl Pts',(-0.494219175919373,-0.502972150320693,
-1.15390262822069));
#60234=CARTESIAN_POINT('Ctrl Pts',(-0.194893845382005,-0.677679840984561,
-1.1380957429026));
#60235=CARTESIAN_POINT('Ctrl Pts',(0.15151266369854,-0.688678074708074,
-1.12228885758451));
#60236=CARTESIAN_POINT('Ctrl Pts',(0.461317735944786,-0.533309970230656,
-1.10648197226642));
#60237=CARTESIAN_POINT('Ctrl Pts',(0.659680691337217,-0.249108336515458,
-1.09067508694833));
#60238=CARTESIAN_POINT('Ctrl Pts',(0.698682306460244,0.0952712573866783,
-1.07486820163024));
#60239=CARTESIAN_POINT('Ctrl Pts',(0.568900826606944,0.41663584499006,-1.05906131631215));
#60240=CARTESIAN_POINT('Ctrl Pts',(0.301688011565286,0.637352274274148,
-1.04325443099405));
#60241=CARTESIAN_POINT('Ctrl Pts',(-0.0384046171462246,0.704101316023837,
-1.02744754567596));
#60242=CARTESIAN_POINT('Ctrl Pts',(-0.369219710011492,0.600758173963263,
-1.01164066035787));
#60243=CARTESIAN_POINT('Ctrl Pts',(-0.610841123852988,0.352287807416983,
-0.99583377503978));
#60244=CARTESIAN_POINT('Ctrl Pts',(-0.675222522545463,0.123962206612681,
-0.985014228793486));
#60245=CARTESIAN_POINT('Ctrl Pts',(-0.676755325096052,0.00599168741729094,
-0.979463644319891));
#60246=CARTESIAN_POINT('Ctrl Pts',(-0.676752484899457,6.08590203554811E-6,
-0.979182021618994));
#60247=CARTESIAN_POINT('Origin',(0.,0.,-4.318617978381));
#60248=CARTESIAN_POINT('',(-0.676748500489657,8.29977222931769E-6,-1.418617978381));
#60249=CARTESIAN_POINT('',(-0.676692639524177,-1.71467829109539E-5,-1.37918202161899));
#60250=CARTESIAN_POINT('',(-0.6767,-7.33509820392354E-14,-4.318617978381));
#60251=CARTESIAN_POINT('Ctrl Pts',(-0.676748500489657,8.29977222930288E-6,
-1.418617978381));
#60252=CARTESIAN_POINT('Ctrl Pts',(-0.676684450593901,-0.103617326982464,
-1.41374247351641));
#60253=CARTESIAN_POINT('Ctrl Pts',(-0.626395365481128,-0.319291283088945,
-1.40359800687913));
#60254=CARTESIAN_POINT('Ctrl Pts',(-0.406669950001241,-0.576066950948749,
-1.38818457846914));
#60255=CARTESIAN_POINT('Ctrl Pts',(-0.0830949650860008,-0.700234822746455,
-1.37237769315105));
#60256=CARTESIAN_POINT('Ctrl Pts',(0.260553557193054,-0.655244552852938,
-1.35657080783296));
#60257=CARTESIAN_POINT('Ctrl Pts',(0.541259257844153,-0.451964595966764,
-1.34076392251487));
#60258=CARTESIAN_POINT('Ctrl Pts',(0.69121109242647,-0.13950199251626,-1.32495703719678));
#60259=CARTESIAN_POINT('Ctrl Pts',(0.67418467897962,0.206660588498508,-1.30915015187868));
#60260=CARTESIAN_POINT('Ctrl Pts',(0.494293146935006,0.50289945824438,-1.29334326656059));
#60261=CARTESIAN_POINT('Ctrl Pts',(0.194993514250268,0.677651171038411,
-1.2775363812425));
#60262=CARTESIAN_POINT('Ctrl Pts',(-0.151411374329973,0.688700352789885,
-1.26172949592441));
#60263=CARTESIAN_POINT('Ctrl Pts',(-0.461239294898093,0.533377814547353,
-1.24592261060632));
#60264=CARTESIAN_POINT('Ctrl Pts',(-0.641614910060592,0.275028249089165,
-1.23155210475852));
#60265=CARTESIAN_POINT('Ctrl Pts',(-0.676607726943547,0.0814639673770342,
-1.22245056068341));
#60266=CARTESIAN_POINT('Ctrl Pts',(-0.676685704046724,-1.68522255445426E-5,
-1.218617978381));
#60267=CARTESIAN_POINT('Ctrl Pts',(-0.676692639524176,-1.71467829109401E-5,
-1.37918202161899));
#60268=CARTESIAN_POINT('Ctrl Pts',(-0.676720625649769,-0.0282425422486149,
-1.37785435530399));
#60269=CARTESIAN_POINT('Ctrl Pts',(-0.668109463888461,-0.168465967902817,
-1.37125772721629));
#60270=CARTESIAN_POINT('Ctrl Pts',(-0.573200140887612,-0.410700835561685,
-1.35939213735589));
#60271=CARTESIAN_POINT('Ctrl Pts',(-0.308295632778683,-0.634182450604112,
-1.3435852520378));
#60272=CARTESIAN_POINT('Ctrl Pts',(0.0310849148505515,-0.704462423350869,
-1.3277783667197));
#60273=CARTESIAN_POINT('Ctrl Pts',(0.362956172367475,-0.604562978344687,
-1.31197148140161));
#60274=CARTESIAN_POINT('Ctrl Pts',(0.607146855256262,-0.358617169133155,
-1.29616459608352));
#60275=CARTESIAN_POINT('Ctrl Pts',(0.704666977880717,-0.026038973272816,
-1.28035771076543));
#60276=CARTESIAN_POINT('Ctrl Pts',(0.631958267808816,0.312829547186207,
-1.26455082544734));
#60277=CARTESIAN_POINT('Ctrl Pts',(0.40658521895174,0.57612675478111,-1.24874394012925));
#60278=CARTESIAN_POINT('Ctrl Pts',(0.0829919761785184,0.700247034791744,
-1.23293705481115));
#60279=CARTESIAN_POINT('Ctrl Pts',(-0.26064992457286,0.655206223005252,
-1.21713016949306));
#60280=CARTESIAN_POINT('Ctrl Pts',(-0.541325723895911,0.45188498369963,
-1.20132328417497));
#60281=CARTESIAN_POINT('Ctrl Pts',(-0.661287168256255,0.201820668754294,
-1.18867390155028));
#60282=CARTESIAN_POINT('Ctrl Pts',(-0.676674825747406,0.0449057095593861,
-1.18129348069829));
#60283=CARTESIAN_POINT('Ctrl Pts',(-0.676652044953461,9.61824139304387E-6,
-1.17918202161899));
#60284=CARTESIAN_POINT('Origin',(0.,0.,-4.318617978381));
#60285=CARTESIAN_POINT('',(-0.67664869645179,7.73109616231909E-6,-1.618617978381));
#60286=CARTESIAN_POINT('',(-0.67674370184345,1.02755109431876E-5,-1.57918202161899));
#60287=CARTESIAN_POINT('',(-0.6767,-7.33509820392354E-14,-4.318617978381));
#60288=CARTESIAN_POINT('Ctrl Pts',(-0.67664869645179,7.73109616233197E-6,
-1.618617978381));
#60289=CARTESIAN_POINT('Ctrl Pts',(-0.676622450612112,-0.0647534336386639,
-1.61557230989481));
#60290=CARTESIAN_POINT('Ctrl Pts',(-0.651428100979576,-0.241570457659696,
-1.60725767963592));
#60291=CARTESIAN_POINT('Ctrl Pts',(-0.499493016443407,-0.497735177311859,
-1.59367408760434));
#60292=CARTESIAN_POINT('Ctrl Pts',(-0.202025718633698,-0.67558803217637,
-1.57786720228624));
#60293=CARTESIAN_POINT('Ctrl Pts',(0.144245628943018,-0.690236755570315,
-1.56206031696815));
#60294=CARTESIAN_POINT('Ctrl Pts',(0.455671062340006,-0.538142604850548,
-1.54625343165006));
#60295=CARTESIAN_POINT('Ctrl Pts',(0.657018465304896,-0.256047488677006,
-1.53044654633197));
#60296=CARTESIAN_POINT('Ctrl Pts',(0.69964765112674,0.0879019026087411,
-1.51463966101388));
#60297=CARTESIAN_POINT('Ctrl Pts',(0.573260540331073,0.410616528051086,
-1.49883277569578));
#60298=CARTESIAN_POINT('Ctrl Pts',(0.308388903263251,0.63413710233158,-1.48302589037769));
#60299=CARTESIAN_POINT('Ctrl Pts',(-0.0309813049975863,0.704466989255031,
-1.4672190050596));
#60300=CARTESIAN_POINT('Ctrl Pts',(-0.362867252535701,0.604616355424324,
-1.45141211974151));
#60301=CARTESIAN_POINT('Ctrl Pts',(-0.607094106116187,0.358706462903012,
-1.43560523442342));
#60302=CARTESIAN_POINT('Ctrl Pts',(-0.674568768752993,0.128719220117463,
-1.42467385396992));
#60303=CARTESIAN_POINT('Ctrl Pts',(-0.676753669364399,0.0083709657598824,
-1.41901143528911));
#60304=CARTESIAN_POINT('Ctrl Pts',(-0.676748500489657,8.29977222930288E-6,
-1.418617978381));
#60305=CARTESIAN_POINT('Ctrl Pts',(-0.67674370184345,1.02755109432015E-5,
-1.57918202161899));
#60306=CARTESIAN_POINT('Ctrl Pts',(-0.676669257422799,-0.101306808967324,
-1.57441522990969));
#60307=CARTESIAN_POINT('Ctrl Pts',(-0.62810275948207,-0.314683464463068,
-1.56437947642769));
#60308=CARTESIAN_POINT('Ctrl Pts',(-0.412550866549072,-0.571870055479614,
-1.54907476117299));
#60309=CARTESIAN_POINT('Ctrl Pts',(-0.0902650651626452,-0.699346692174796,
-1.5332678758549));
#60310=CARTESIAN_POINT('Ctrl Pts',(0.253826379397398,-0.65787973594469,
-1.5174609905368));
#60311=CARTESIAN_POINT('Ctrl Pts',(0.536600109875943,-0.457486502452008,
-1.50165410521871));
#60312=CARTESIAN_POINT('Ctrl Pts',(0.689745500732789,-0.146576676396754,
-1.48584721990062));
#60313=CARTESIAN_POINT('Ctrl Pts',(0.67626669160168,0.199742183012912,-1.47004033458253));
#60314=CARTESIAN_POINT('Ctrl Pts',(0.499419804901498,0.497808634232871,
-1.45423344926444));
#60315=CARTESIAN_POINT('Ctrl Pts',(0.201926353111081,0.675617736418978,
-1.43842656394635));
#60316=CARTESIAN_POINT('Ctrl Pts',(-0.144347144374269,0.690215531378164,
-1.42261967862825));
#60317=CARTESIAN_POINT('Ctrl Pts',(-0.455750204246968,0.538075579424947,
-1.40681279331016));
#60318=CARTESIAN_POINT('Ctrl Pts',(-0.640147845607731,0.279647330628739,
-1.39233357430708));
#60319=CARTESIAN_POINT('Ctrl Pts',(-0.676609560222979,0.0837724483008001,
-1.38312331707669));
#60320=CARTESIAN_POINT('Ctrl Pts',(-0.676692639524176,-1.71467829109401E-5,
-1.37918202161899));
#60321=CARTESIAN_POINT('Origin',(0.,0.,-4.318617978381));
#60322=CARTESIAN_POINT('',(-0.676699979303772,-1.71578878559266E-5,-1.818617978381));
#60323=CARTESIAN_POINT('',(-0.676646172362016,5.7804085369928E-6,-1.77918202161899));
#60324=CARTESIAN_POINT('',(-0.6767,-7.33509820392354E-14,-4.318617978381));
#60325=CARTESIAN_POINT('Ctrl Pts',(-0.676699979303772,-1.7157887855928E-5,
-1.818617978381));
#60326=CARTESIAN_POINT('Ctrl Pts',(-0.676726159812639,-0.025864218275893,
-1.81740214627321));
#60327=CARTESIAN_POINT('Ctrl Pts',(-0.668977558555818,-0.163707169183447,
-1.81091735239272));
#60328=CARTESIAN_POINT('Ctrl Pts',(-0.577497061222251,-0.404636533804186,
-1.79916359673953));
#60329=CARTESIAN_POINT('Ctrl Pts',(-0.314962747739959,-0.630897810858063,
-1.78335671142144));
#60330=CARTESIAN_POINT('Ctrl Pts',(0.0236582032229997,-0.704750927370557,
-1.76754982610334));
#60331=CARTESIAN_POINT('Ctrl Pts',(0.356563960421018,-0.608354931218841,
-1.75174294078526));
#60332=CARTESIAN_POINT('Ctrl Pts',(0.603333331681656,-0.364996535725085,
-1.73593605546716));
#60333=CARTESIAN_POINT('Ctrl Pts',(0.704353388723183,-0.033464667988367,
-1.72012917014907));
#60334=CARTESIAN_POINT('Ctrl Pts',(0.635220367882906,0.306151375035467,
-1.70432228483098));
#60335=CARTESIAN_POINT('Ctrl Pts',(0.412634971489475,0.571809374278948,
-1.68851539951289));
#60336=CARTESIAN_POINT('Ctrl Pts',(0.0903679215898715,0.69933341043949,
-1.67270851419479));
#60337=CARTESIAN_POINT('Ctrl Pts',(-0.253729618865292,0.657917062189359,
-1.65690162887671));
#60338=CARTESIAN_POINT('Ctrl Pts',(-0.53653282001449,0.457565419646962,
-1.64109474355861));
#60339=CARTESIAN_POINT('Ctrl Pts',(-0.660207093665119,0.206579842277233,
-1.62833352672671));
#60340=CARTESIAN_POINT('Ctrl Pts',(-0.676667855529483,0.0472824307012137,
-1.62084127166751));
#60341=CARTESIAN_POINT('Ctrl Pts',(-0.67664869645179,7.73109616233197E-6,
-1.618617978381));
#60342=CARTESIAN_POINT('Ctrl Pts',(-0.676646172362016,5.7804085369928E-6,
-1.77918202161899));
#60343=CARTESIAN_POINT('Ctrl Pts',(-0.676627337627041,-0.0624444429508034,
-1.77624506628809));
#60344=CARTESIAN_POINT('Ctrl Pts',(-0.652674079260861,-0.236945885371131,
-1.76803914918448));
#60345=CARTESIAN_POINT('Ctrl Pts',(-0.504566489299185,-0.492591347590416,
-1.75456427030818));
#60346=CARTESIAN_POINT('Ctrl Pts',(-0.208937049864503,-0.6734826553361,
-1.73875738499009));
#60347=CARTESIAN_POINT('Ctrl Pts',(0.137166033464237,-0.691678434757318,
-1.722950499672));
#60348=CARTESIAN_POINT('Ctrl Pts',(0.450133444915136,-0.542783068650339,
-1.70714361435391));
#60349=CARTESIAN_POINT('Ctrl Pts',(0.654360567278065,-0.262765724241526,
-1.69133672903581));
#60350=CARTESIAN_POINT('Ctrl Pts',(0.700511550093094,0.0807288426203301,
-1.67552984371772));
#60351=CARTESIAN_POINT('Ctrl Pts',(0.577437541237162,0.404721464484683,
-1.65972295839963));
#60352=CARTESIAN_POINT('Ctrl Pts',(0.314869953591033,0.630944126028784,
-1.64391607308154));
#60353=CARTESIAN_POINT('Ctrl Pts',(-0.0237618549331032,0.704747438515944,
-1.62810918776345));
#60354=CARTESIAN_POINT('Ctrl Pts',(-0.356653430191126,0.608302481153537,
-1.61230230244536));
#60355=CARTESIAN_POINT('Ctrl Pts',(-0.603387005990771,0.364907794992297,
-1.59649541712726));
#60356=CARTESIAN_POINT('Ctrl Pts',(-0.673908967110712,0.133343716310157,
-1.58545532351848));
#60357=CARTESIAN_POINT('Ctrl Pts',(-0.676751544384454,0.0106837871384544,
-1.57968419168239));
#60358=CARTESIAN_POINT('Ctrl Pts',(-0.67674370184345,1.02755109432015E-5,
-1.57918202161899));
#60359=CARTESIAN_POINT('Origin',(0.,0.,-4.318617978381));
#60360=CARTESIAN_POINT('',(-0.67673798465263,1.20914945348619E-5,-2.018617978381));
#60361=CARTESIAN_POINT('',(-0.676707204276618,-1.68789097811373E-5,-1.979182021619));
#60362=CARTESIAN_POINT('',(-0.6767,-7.33509820392354E-14,-4.318617978381));
#60363=CARTESIAN_POINT('Ctrl Pts',(-0.676737984652629,1.2091494534832E-5,
-2.018617978381));
#60364=CARTESIAN_POINT('Ctrl Pts',(-0.676655634372884,-0.0989304053447198,
-2.01396302087891));
#60365=CARTESIAN_POINT('Ctrl Pts',(-0.629829434074097,-0.309941629925032,
-2.00403910160412));
#60366=CARTESIAN_POINT('Ctrl Pts',(-0.418555422414341,-0.567490033900997,
-1.98884622055663));
#60367=CARTESIAN_POINT('Ctrl Pts',(-0.097631117047166,-0.698356459978373,
-1.97303933523854));
#60368=CARTESIAN_POINT('Ctrl Pts',(0.246878274057621,-0.660518506938096,
-1.95723244992044));
#60369=CARTESIAN_POINT('Ctrl Pts',(0.531748428856327,-0.463116819623548,
-1.94142556460235));
#60370=CARTESIAN_POINT('Ctrl Pts',(0.68816228135381,-0.153838404604709,
-1.92561867928426));
#60371=CARTESIAN_POINT('Ctrl Pts',(0.678334397630255,0.192603284502106,
-1.90981179396617));
#60372=CARTESIAN_POINT('Ctrl Pts',(0.504638933459461,0.49251713375912,-1.89400490864808));
#60373=CARTESIAN_POINT('Ctrl Pts',(0.209036101308555,0.67345192000552,-1.87819802332998));
#60374=CARTESIAN_POINT('Ctrl Pts',(-0.137064302935446,0.691698602767291,
-1.8623911380119));
#60375=CARTESIAN_POINT('Ctrl Pts',(-0.450053610696377,0.542849267945122,
-1.8465842526938));
#60376=CARTESIAN_POINT('Ctrl Pts',(-0.638610030267167,0.284397992760645,
-1.83199319948351));
#60377=CARTESIAN_POINT('Ctrl Pts',(-0.676612703275732,0.0861472775944482,
-1.8226711080459));
#60378=CARTESIAN_POINT('Ctrl Pts',(-0.676699979303772,-1.7157887855928E-5,
-1.818617978381));
#60379=CARTESIAN_POINT('Ctrl Pts',(-0.676707204276618,-1.68789097811095E-5,
-1.97918202161899));
#60380=CARTESIAN_POINT('Ctrl Pts',(-0.676731182525368,-0.0235521105545861,
-1.97807490266648));
#60381=CARTESIAN_POINT('Ctrl Pts',(-0.669796504969086,-0.159081332134532,
-1.97169882194128));
#60382=CARTESIAN_POINT('Ctrl Pts',(-0.581612569954882,-0.398698377617872,
-1.96005377944337));
#60383=CARTESIAN_POINT('Ctrl Pts',(-0.321410263880308,-0.627637650334202,
-1.94424689412528));
#60384=CARTESIAN_POINT('Ctrl Pts',(0.0164362283905885,-0.704956330733284,
-1.92844000880719));
#60385=CARTESIAN_POINT('Ctrl Pts',(0.350312164270045,-0.611976278469258,
-1.9126331234891));
#60386=CARTESIAN_POINT('Ctrl Pts',(0.599561982174783,-0.37115900551555,
-1.896826238171));
#60387=CARTESIAN_POINT('Ctrl Pts',(0.70397354377059,-0.0406795712332764,
-1.88101935285292));
#60388=CARTESIAN_POINT('Ctrl Pts',(0.638323787940124,0.29962696740183,-1.86521246753482));
#60389=CARTESIAN_POINT('Ctrl Pts',(0.41847195266759,0.567551585915519,-1.84940558221673));
#60390=CARTESIAN_POINT('Ctrl Pts',(0.0975284042101817,0.698370809969075,
-1.83359869689864));
#60391=CARTESIAN_POINT('Ctrl Pts',(-0.246975417290485,0.660482188328222,
-1.81779181158055));
#60392=CARTESIAN_POINT('Ctrl Pts',(-0.531816535259198,0.46303860602497,
-1.80198492626245));
#60393=CARTESIAN_POINT('Ctrl Pts',(-0.659131299877361,0.211206098569119,
-1.78911499627527));
#60394=CARTESIAN_POINT('Ctrl Pts',(-0.676661127551435,0.0495926166918764,
-1.78151402806078));
#60395=CARTESIAN_POINT('Ctrl Pts',(-0.676646172362016,5.7804085369928E-6,
-1.77918202161899));
#60396=CARTESIAN_POINT('Origin',(0.,0.,-4.318617978381));
#60397=CARTESIAN_POINT('',(-0.676644363004478,3.68526634802388E-6,-2.218617978381));
#60398=CARTESIAN_POINT('',(-0.676731813311252,1.36189314004012E-5,-2.17918202161899));
#60399=CARTESIAN_POINT('',(-0.6767,-7.33509820392354E-14,-4.318617978381));
#60400=CARTESIAN_POINT('Ctrl Pts',(-0.676644363004478,3.6852663480233E-6,
-2.218617978381));
#60401=CARTESIAN_POINT('Ctrl Pts',(-0.676632850481567,-0.0600690012882533,
-2.2157928572573));
#60402=CARTESIAN_POINT('Ctrl Pts',(-0.653928438313362,-0.232188141953543,
-2.20769877436091));
#60403=CARTESIAN_POINT('Ctrl Pts',(-0.509730342149469,-0.487245891210574,
-2.19433572969182));
#60404=CARTESIAN_POINT('Ctrl Pts',(-0.216023905051799,-0.671243065256971,
-2.17852884437373));
#60405=CARTESIAN_POINT('Ctrl Pts',(0.129868171994647,-0.693085736480105,
-2.16272195905564));
#60406=CARTESIAN_POINT('Ctrl Pts',(0.444387546733483,-0.547497295443183,
-2.14691507373755));
#60407=CARTESIAN_POINT('Ctrl Pts',(0.65155468882939,-0.269648044075677,
-2.13110818841945));
#60408=CARTESIAN_POINT('Ctrl Pts',(0.701323517113522,0.0733410154887558,
-2.11530130310137));
#60409=CARTESIAN_POINT('Ctrl Pts',(0.581671204052573,0.398612832941228,
-2.09949441778327));
#60410=CARTESIAN_POINT('Ctrl Pts',(0.321502571670479,0.627590373268003,
-2.08368753246518));
#60411=CARTESIAN_POINT('Ctrl Pts',(-0.0163325460192437,0.704958742161505,
-2.06788064714709));
#60412=CARTESIAN_POINT('Ctrl Pts',(-0.350222154225635,0.612027795854858,
-2.052073761829));
#60413=CARTESIAN_POINT('Ctrl Pts',(-0.599507388494239,0.371247183625977,
-2.03626687651091));
#60414=CARTESIAN_POINT('Ctrl Pts',(-0.673205160779302,0.138101219917673,
-2.02511494869491));
#60415=CARTESIAN_POINT('Ctrl Pts',(-0.676748846926544,0.0130629336506955,
-2.01923198265161));
#60416=CARTESIAN_POINT('Ctrl Pts',(-0.676737984652629,1.2091494534832E-5,
-2.018617978381));
#60417=CARTESIAN_POINT('Ctrl Pts',(-0.676731813311252,1.36189314004047E-5,
-2.17918202161899));
#60418=CARTESIAN_POINT('Ctrl Pts',(-0.676644233480705,-0.0966206972557906,
-2.17463577727218));
#60419=CARTESIAN_POINT('Ctrl Pts',(-0.631479154499264,-0.305330546356952,
-2.16482057115268));
#60420=CARTESIAN_POINT('Ctrl Pts',(-0.424347837744089,-0.563171812546191,
-2.14973640326047));
#60421=CARTESIAN_POINT('Ctrl Pts',(-0.104781208775136,-0.697319493584015,
-2.13392951794238));
#60422=CARTESIAN_POINT('Ctrl Pts',(0.240097778255422,-0.663013299053236,
-2.11812263262429));
#60423=CARTESIAN_POINT('Ctrl Pts',(0.526975516741124,-0.46854069471079,
-2.1023157473062));
#60424=CARTESIAN_POINT('Ctrl Pts',(0.68654996177012,-0.160881098448797,
-2.08650886198811));
#60425=CARTESIAN_POINT('Ctrl Pts',(0.680272164181842,0.185643099747873,
-2.07070197667002));
#60426=CARTESIAN_POINT('Ctrl Pts',(0.509658673195849,0.48732085393598,-2.05489509135192));
#60427=CARTESIAN_POINT('Ctrl Pts',(0.215925178385313,0.671274828355656,
-2.03908820603383));
#60428=CARTESIAN_POINT('Ctrl Pts',(-0.129970106632608,0.693066626830752,
-2.02328132071574));
#60429=CARTESIAN_POINT('Ctrl Pts',(-0.444468064640782,0.547431929429699,
-2.00747443539765));
#60430=CARTESIAN_POINT('Ctrl Pts',(-0.637087153110088,0.289014990482141,
-1.99277466903207));
#60431=CARTESIAN_POINT('Ctrl Pts',(-0.67661706608309,0.0884559402215986,
-1.98334386443918));
#60432=CARTESIAN_POINT('Ctrl Pts',(-0.676707204276618,-1.68789097811095E-5,
-1.97918202161899));
#60433=CARTESIAN_POINT('Origin',(0.,0.,-4.318617978381));
#60434=CARTESIAN_POINT('',(-0.676714620613759,-1.62920487620288E-5,-2.418617978381));
#60435=CARTESIAN_POINT('',(-0.676643382151003,1.59347960965173E-6,-2.379182021619));
#60436=CARTESIAN_POINT('',(-0.6767,-7.33509820392354E-14,-4.318617978381));
#60437=CARTESIAN_POINT('Ctrl Pts',(-0.676714620613759,-1.6292048762058E-5,
-2.418617978381));
#60438=CARTESIAN_POINT('Ctrl Pts',(-0.676735957233897,-0.021173474084283,
-2.4176226936357));
#60439=CARTESIAN_POINT('Ctrl Pts',(-0.670613426882276,-0.154322869409382,
-2.41135844711771));
#60440=CARTESIAN_POINT('Ctrl Pts',(-0.58578251795406,-0.392546076109294,
-2.39982523882701));
#60441=CARTESIAN_POINT('Ctrl Pts',(-0.328007668658949,-0.624215146812637,
-2.38401835350892));
#60442=CARTESIAN_POINT('Ctrl Pts',(0.00900512466355355,-0.70509041118086,
-2.36821146819083));
#60443=CARTESIAN_POINT('Ctrl Pts',(0.343842518956618,-0.61563455260972,
-2.35240458287274));
#60444=CARTESIAN_POINT('Ctrl Pts',(0.595616689811292,-0.377457731445045,
-2.33659769755465));
#60445=CARTESIAN_POINT('Ctrl Pts',(0.703505682243138,-0.0480971440006585,
-2.32079081223656));
#60446=CARTESIAN_POINT('Ctrl Pts',(0.641446380171849,0.292882436437956,
-2.30498392691846));
#60447=CARTESIAN_POINT('Ctrl Pts',(0.424430663281246,0.563109396366323,
-2.28917704160037));
#60448=CARTESIAN_POINT('Ctrl Pts',(0.104883766927401,0.697304076887924,
-2.27337015628228));
#60449=CARTESIAN_POINT('Ctrl Pts',(-0.240000262814678,0.663048606105381,
-2.25756327096419));
#60450=CARTESIAN_POINT('Ctrl Pts',(-0.526906601153319,0.468618196264782,
-2.2417563856461));
#60451=CARTESIAN_POINT('Ctrl Pts',(-0.657997905630098,0.215965030249459,
-2.2287746214517));
#60452=CARTESIAN_POINT('Ctrl Pts',(-0.676654321788626,0.0519689167976407,
-2.22106181903));
#60453=CARTESIAN_POINT('Ctrl Pts',(-0.676644363004478,3.6852663480233E-6,
-2.218617978381));
#60454=CARTESIAN_POINT('Ctrl Pts',(-0.676643382151003,1.59347960970724E-6,
-2.379182021619));
#60455=CARTESIAN_POINT('Ctrl Pts',(-0.676638604274974,-0.0577596821259404,
-2.37646561365058));
#60456=CARTESIAN_POINT('Ctrl Pts',(-0.655121282576093,-0.227562834361756,
-2.36848024390947));
#60457=CARTESIAN_POINT('Ctrl Pts',(-0.514695806561756,-0.481997722559338,
-2.35522591239567));
#60458=CARTESIAN_POINT('Ctrl Pts',(-0.222889983854245,-0.668994493954996,
-2.33941902707757));
#60459=CARTESIAN_POINT('Ctrl Pts',(0.122760141143874,-0.694379957653575,
-2.32361214175949));
#60460=CARTESIAN_POINT('Ctrl Pts',(0.438754675367169,-0.55202165961862,
-2.30780525644139));
#60461=CARTESIAN_POINT('Ctrl Pts',(0.648757729114897,-0.276309584991779,
-2.2919983711233));
#60462=CARTESIAN_POINT('Ctrl Pts',(0.702038140257588,0.0661515492510317,
-2.2761914858052));
#60463=CARTESIAN_POINT('Ctrl Pts',(0.585724776077096,0.392632225542023,
-2.26038460048712));
#60464=CARTESIAN_POINT('Ctrl Pts',(0.327915857198116,0.624263380667703,
-2.24457771516902));
#60465=CARTESIAN_POINT('Ctrl Pts',(-0.0091088264969462,0.705089077439507,
-2.22877082985093));
#60466=CARTESIAN_POINT('Ctrl Pts',(-0.343933059552939,0.615583973468446,
-2.21296394453284));
#60467=CARTESIAN_POINT('Ctrl Pts',(-0.595672196966363,0.377370125481488,
-2.19715705921475));
#60468=CARTESIAN_POINT('Ctrl Pts',(-0.672496548540618,0.14272617859532,
-2.18589641824347));
#60469=CARTESIAN_POINT('Ctrl Pts',(-0.676745735895447,0.015375596625399,
-2.17990473904488));
#60470=CARTESIAN_POINT('Ctrl Pts',(-0.676731813311252,1.36189314004047E-5,
-2.17918202161899));
#60471=CARTESIAN_POINT('Origin',(0.,0.,-4.318617978381));
#60472=CARTESIAN_POINT('',(-0.676724990071838,1.49232986133271E-5,-2.618617978381));
#60473=CARTESIAN_POINT('',(-0.676721689350739,-1.54329616245952E-5,-2.579182021619));
#60474=CARTESIAN_POINT('',(-0.6767,-7.33509820392354E-14,-4.318617978381));
#60475=CARTESIAN_POINT('Ctrl Pts',(-0.676724990071838,1.49232986133355E-5,
-2.618617978381));
#60476=CARTESIAN_POINT('Ctrl Pts',(-0.676634302193046,-0.0942450091755502,
-2.6141835682414));
#60477=CARTESIAN_POINT('Ctrl Pts',(-0.633146801927531,-0.300585558606619,
-2.60448019632911));
#60478=CARTESIAN_POINT('Ctrl Pts',(-0.430260059478938,-0.558667934847332,
-2.58950786264411));
#60479=CARTESIAN_POINT('Ctrl Pts',(-0.11212508783917,-0.696176374840788,
-2.57370097732603));
#60480=CARTESIAN_POINT('Ctrl Pts',(0.23309632806146,-0.665507086403793,
-2.55789409200792));
#60481=CARTESIAN_POINT('Ctrl Pts',(0.5220078598931,-0.474068955342181,-2.54208720668984));
#60482=CARTESIAN_POINT('Ctrl Pts',(0.684816152269453,-0.16810835136977,
-2.52628032137174));
#60483=CARTESIAN_POINT('Ctrl Pts',(0.682191044370633,0.178462766956884,
-2.51047343605366));
#60484=CARTESIAN_POINT('Ctrl Pts',(0.514766692567439,0.481922019036879,
-2.49466655073556));
#60485=CARTESIAN_POINT('Ctrl Pts',(0.222988375079262,0.668961706519075,
-2.47885966541747));
#60486=CARTESIAN_POINT('Ctrl Pts',(-0.122658013407166,0.694398006878195,
-2.46305278009938));
#60487=CARTESIAN_POINT('Ctrl Pts',(-0.43867348246843,0.552086185290324,
-2.44724589478129));
#60488=CARTESIAN_POINT('Ctrl Pts',(-0.635491633703408,0.29376333873624,
-2.4324342942085));
#60489=CARTESIAN_POINT('Ctrl Pts',(-0.676623002789058,0.0908310390861413,
-2.4228916554084));
#60490=CARTESIAN_POINT('Ctrl Pts',(-0.676714620613759,-1.6292048762058E-5,
-2.418617978381));
#60491=CARTESIAN_POINT('Ctrl Pts',(-0.676721689350739,-1.54329616246299E-5,
-2.579182021619));
#60492=CARTESIAN_POINT('Ctrl Pts',(-0.676740183597297,-0.0188610859446095,
-2.57829545002898));
#60493=CARTESIAN_POINT('Ctrl Pts',(-0.671382810041269,-0.14969739182925,
-2.57213991666627));
#60494=CARTESIAN_POINT('Ctrl Pts',(-0.589773715425885,-0.386523663489563,
-2.56071542153086));
#60495=CARTESIAN_POINT('Ctrl Pts',(-0.334386030845991,-0.620821681499372,
-2.54490853621277));
#60496=CARTESIAN_POINT('Ctrl Pts',(0.00178044071789455,-0.705145664296035,
-2.52910165089467));
#60497=CARTESIAN_POINT('Ctrl Pts',(0.337516805075675,-0.619125176467695,
-2.51329476557658));
#60498=CARTESIAN_POINT('Ctrl Pts',(0.591718070518745,-0.383540483999043,
-2.49748788025849));
#60499=CARTESIAN_POINT('Ctrl Pts',(0.702975960450328,-0.0553025937328847,
-2.4816809949404));
#60500=CARTESIAN_POINT('Ctrl Pts',(0.644413522599621,0.286294934875548,
-2.46587410962231));
#60501=CARTESIAN_POINT('Ctrl Pts',(0.430177887097737,0.558731208450694,
-2.45006722430421));
#60502=CARTESIAN_POINT('Ctrl Pts',(0.112022695449392,0.69619285657704,-2.43426033898612));
#60503=CARTESIAN_POINT('Ctrl Pts',(-0.233194205177004,0.665472794723054,
-2.41845345366803));
#60504=CARTESIAN_POINT('Ctrl Pts',(-0.522077577221963,0.473992174204058,
-2.40264656834994));
#60505=CARTESIAN_POINT('Ctrl Pts',(-0.656870050744532,0.220590971059179,
-2.38955609100026));
#60506=CARTESIAN_POINT('Ctrl Pts',(-0.676647871824783,0.054278699680794,
-2.38173457542328));
#60507=CARTESIAN_POINT('Ctrl Pts',(-0.676643382151003,1.59347960970724E-6,
-2.379182021619));
#60508=CARTESIAN_POINT('Origin',(0.,0.,-4.318617978381));
#60509=CARTESIAN_POINT('',(-0.676643190996923,-5.82392518506049E-7,-2.818617978381));
#60510=CARTESIAN_POINT('',(-0.676718026672013,1.59161084590936E-5,-2.779182021619));
#60511=CARTESIAN_POINT('',(-0.6767,-7.33509820392354E-14,-4.318617978381));
#60512=CARTESIAN_POINT('Ctrl Pts',(-0.676643190996923,-5.82392518481967E-7,
-2.818617978381));
#60513=CARTESIAN_POINT('Ctrl Pts',(-0.676644864762177,-0.0553838781273899,
-2.8160134046198));
#60514=CARTESIAN_POINT('Ctrl Pts',(-0.656321235606746,-0.222804440132633,
-2.8081398690859));
#60515=CARTESIAN_POINT('Ctrl Pts',(-0.519747440714448,-0.476546092293478,
-2.79499737177931));
#60516=CARTESIAN_POINT('Ctrl Pts',(-0.229928759127129,-0.666608090211678,
-2.77919048646121));
#60517=CARTESIAN_POINT('Ctrl Pts',(0.115434605974731,-0.695635272217317,
-2.76338360114313));
#60518=CARTESIAN_POINT('Ctrl Pts',(0.432912035103061,-0.556615441819869,
-2.74757671582503));
#60519=CARTESIAN_POINT('Ctrl Pts',(0.645809410519448,-0.28313209901727,
-2.73176983050694));
#60520=CARTESIAN_POINT('Ctrl Pts',(0.70269637882455,0.0587484416496746,
-2.71596294518884));
#60521=CARTESIAN_POINT('Ctrl Pts',(0.589830558845161,0.386436918606138,
-2.70015605987076));
#60522=CARTESIAN_POINT('Ctrl Pts',(0.334477336060517,0.620772496065396,
-2.68434917455266));
#60523=CARTESIAN_POINT('Ctrl Pts',(-0.00167673062376321,0.705145920206461,
-2.66854228923458));
#60524=CARTESIAN_POINT('Ctrl Pts',(-0.337425743707141,0.619174811901361,
-2.65273540391648));
#60525=CARTESIAN_POINT('Ctrl Pts',(-0.591661655884731,0.383627508353011,
-2.63692851859839));
#60526=CARTESIAN_POINT('Ctrl Pts',(-0.671742365813614,0.147484140385321,
-2.6255560434199));
#60527=CARTESIAN_POINT('Ctrl Pts',(-0.676742057441559,0.017754550014597,
-2.6194525300141));
#60528=CARTESIAN_POINT('Ctrl Pts',(-0.676724990071838,1.49232986133355E-5,
-2.618617978381));
#60529=CARTESIAN_POINT('Ctrl Pts',(-0.676718026672013,1.59161084591075E-5,
-2.77918202161899));
#60530=CARTESIAN_POINT('Ctrl Pts',(-0.676626289360077,-0.0919358888217675,
-2.77485632463468));
#60531=CARTESIAN_POINT('Ctrl Pts',(-0.634739434109742,-0.295971603258148,
-2.76526166587767));
#60532=CARTESIAN_POINT('Ctrl Pts',(-0.435961470998621,-0.554230253278693,
-2.75039804534796));
#60533=CARTESIAN_POINT('Ctrl Pts',(-0.11925208204733,-0.694991020641291,
-2.73459116002987));
#60534=CARTESIAN_POINT('Ctrl Pts',(0.226265443741279,-0.667860409676459,
-2.71878427471177));
#60535=CARTESIAN_POINT('Ctrl Pts',(0.517123245750236,-0.479392455665905,
-2.70297738939368));
#60536=CARTESIAN_POINT('Ctrl Pts',(0.683057801392575,-0.17511601240717,
-2.68717050407559));
#60537=CARTESIAN_POINT('Ctrl Pts',(0.683983727646747,0.17146381005654,-2.6713636187575));
#60538=CARTESIAN_POINT('Ctrl Pts',(0.519677345313422,0.47662252843591,-2.65555673343941));
#60539=CARTESIAN_POINT('Ctrl Pts',(0.229830713971266,0.666641898443312,
-2.63974984812131));
#60540=CARTESIAN_POINT('Ctrl Pts',(-0.115536915778911,0.695618285367013,
-2.62394296280322));
#60541=CARTESIAN_POINT('Ctrl Pts',(-0.432993894223229,0.556551763459652,
-2.60813607748513));
#60542=CARTESIAN_POINT('Ctrl Pts',(-0.633912379396568,0.298377915502387,
-2.59321576375706));
#60543=CARTESIAN_POINT('Ctrl Pts',(-0.67663027089625,0.0931400499671855,
-2.58356441180168));
#60544=CARTESIAN_POINT('Ctrl Pts',(-0.676721689350739,-1.54329616246299E-5,
-2.579182021619));
#60545=CARTESIAN_POINT('Origin',(0.,0.,-4.318617978381));
#60546=CARTESIAN_POINT('',(-0.676728691753018,-1.42604622804819E-5,-3.018617978381));
#60547=CARTESIAN_POINT('',(-0.676643795884942,-2.68919649207278E-6,-2.979182021619));
#60548=CARTESIAN_POINT('',(-0.6767,-7.33509820392354E-14,-4.318617978381));
#60549=CARTESIAN_POINT('Ctrl Pts',(-0.676728691753018,-1.42604622804399E-5,
-3.018617978381));
#60550=CARTESIAN_POINT('Ctrl Pts',(-0.67674408521498,-0.0164821866856739,
-3.0178432409982));
#60551=CARTESIAN_POINT('Ctrl Pts',(-0.672148927518839,-0.144939328790899,
-3.0117995418427));
#60552=CARTESIAN_POINT('Ctrl Pts',(-0.593814889478732,-0.380286020309405,
-3.0004868809145));
#60553=CARTESIAN_POINT('Ctrl Pts',(-0.340910875057239,-0.617262792882503,
-2.98467999559641));
#60554=CARTESIAN_POINT('Ctrl Pts',(-0.0056518445272595,-0.705125263242527,
-2.96887311027831));
#60555=CARTESIAN_POINT('Ctrl Pts',(0.330972521582021,-0.622648191330417,
-2.95306622496023));
#60556=CARTESIAN_POINT('Ctrl Pts',(0.587642713915593,-0.389755847924465,
-2.93725933964213));
#60557=CARTESIAN_POINT('Ctrl Pts',(0.70235402869083,-0.0627088398167523,
-2.92145245432404));
#60558=CARTESIAN_POINT('Ctrl Pts',(0.647395257884359,0.27948695904862,-2.90564556900594));
#60559=CARTESIAN_POINT('Ctrl Pts',(0.436042981348057,0.554166129086307,
-2.88983868368786));
#60560=CARTESIAN_POINT('Ctrl Pts',(0.11935429761476,0.694973475645141,-2.87403179836976));
#60561=CARTESIAN_POINT('Ctrl Pts',(-0.226167215523084,0.667893682281796,
-2.85822491305168));
#60562=CARTESIAN_POINT('Ctrl Pts',(-0.5170527342108,0.479468508094678,-2.84241802773358));
#60563=CARTESIAN_POINT('Ctrl Pts',(-0.655682860652459,0.225349490586159,
-2.82921571617669));
#60564=CARTESIAN_POINT('Ctrl Pts',(-0.676641478793513,0.0566545952765675,
-2.8212823663925));
#60565=CARTESIAN_POINT('Ctrl Pts',(-0.676643190996923,-5.82392518481967E-7,
-2.818617978381));
#60566=CARTESIAN_POINT('Ctrl Pts',(-0.676643795884942,-2.68919649208318E-6,
-2.979182021619));
#60567=CARTESIAN_POINT('Ctrl Pts',(-0.676651210036511,-0.0530741872066186,
-2.97668616101308));
#60568=CARTESIAN_POINT('Ctrl Pts',(-0.657461434917153,-0.218178597507427,
-2.96892133863446));
#60569=CARTESIAN_POINT('Ctrl Pts',(-0.524602751372391,-0.471195852164642,
-2.95588755448315));
#60570=CARTESIAN_POINT('Ctrl Pts',(-0.236746619036826,-0.664217295935056,
-2.94008066916506));
#60571=CARTESIAN_POINT('Ctrl Pts',(0.108301210750851,-0.696781476213702,
-2.92427378384697));
#60572=CARTESIAN_POINT('Ctrl Pts',(0.427186343456901,-0.56102175163586,
-2.90846689852887));
#60573=CARTESIAN_POINT('Ctrl Pts',(0.642874597533564,-0.289734067190421,
-2.89266001321078));
#60574=CARTESIAN_POINT('Ctrl Pts',(0.703261417396002,0.0515456753453884,
-2.87685312789269));
#60575=CARTESIAN_POINT('Ctrl Pts',(0.593758950657057,0.38037335127382,-2.8610462425746));
#60576=CARTESIAN_POINT('Ctrl Pts',(0.340820085951307,0.617312924582654,
-2.84523935725651));
#60577=CARTESIAN_POINT('Ctrl Pts',(0.00554813737457995,0.705126085190668,
-2.82943247193842));
#60578=CARTESIAN_POINT('Ctrl Pts',(-0.33106409388682,0.622599504965708,
-2.81362558662032));
#60579=CARTESIAN_POINT('Ctrl Pts',(-0.587700029934952,0.389669414579977,
-2.79781870130224));
#60580=CARTESIAN_POINT('Ctrl Pts',(-0.670984618310945,0.152109523970622,
-2.78633751296845));
#60581=CARTESIAN_POINT('Ctrl Pts',(-0.676738030980323,0.0200669969246454,
-2.78012528640738));
#60582=CARTESIAN_POINT('Ctrl Pts',(-0.676718026672013,1.59161084591075E-5,
-2.77918202161899));
#60583=CARTESIAN_POINT('Origin',(0.,0.,-4.318617978381));
#60584=CARTESIAN_POINT('',(-0.676710664634451,1.66436917362715E-5,-3.218617978381));
#60585=CARTESIAN_POINT('',(-0.676735096869437,-1.28530889785816E-5,-3.179182021619));
#60586=CARTESIAN_POINT('',(-0.6767,-7.33509820392354E-14,-4.318617978381));
#60587=CARTESIAN_POINT('Ctrl Pts',(-0.676710664634451,1.66436917362969E-5,
-3.218617978381));
#60588=CARTESIAN_POINT('Ctrl Pts',(-0.676619640086048,-0.0895607009637898,
-3.2144041156039));
#60589=CARTESIAN_POINT('Ctrl Pts',(-0.636348652061272,-0.291223853614914,
-3.20492129105409));
#60590=CARTESIAN_POINT('Ctrl Pts',(-0.441778804249146,-0.549604465343574,
-3.1901695047316));
#60591=CARTESIAN_POINT('Ctrl Pts',(-0.126570615394638,-0.693695509231553,
-3.17436261941351));
#60592=CARTESIAN_POINT('Ctrl Pts',(0.219213673644229,-0.67020813595241,
-3.15855573409542));
#60593=CARTESIAN_POINT('Ctrl Pts',(0.512041759331881,-0.484816271292242,
-3.14274884877732));
#60594=CARTESIAN_POINT('Ctrl Pts',(0.681174150856313,-0.182305667532811,
-3.12694196345923));
#60595=CARTESIAN_POINT('Ctrl Pts',(0.685752952950544,0.164245145222046,
-3.11113507814114));
#60596=CARTESIAN_POINT('Ctrl Pts',(0.52467204859744,0.471118691658448,-3.09532819282305));
#60597=CARTESIAN_POINT('Ctrl Pts',(0.236844307533238,0.664182470559487,
-3.07952130750496));
#60598=CARTESIAN_POINT('Ctrl Pts',(-0.108198729930143,0.696797398854864,
-3.06371442218686));
#60599=CARTESIAN_POINT('Ctrl Pts',(-0.427103826957276,0.561084575806403,
-3.04790753686878));
#60600=CARTESIAN_POINT('Ctrl Pts',(-0.632258570116134,0.30312359041971,
-3.03287538893349));
#60601=CARTESIAN_POINT('Ctrl Pts',(-0.676639394819978,0.0955156020780497,
-3.0231122027709));
#60602=CARTESIAN_POINT('Ctrl Pts',(-0.676728691753018,-1.42604622804399E-5,
-3.018617978381));
#60603=CARTESIAN_POINT('Ctrl Pts',(-0.676735096869437,-1.28530889786354E-5,
-3.179182021619));
#60604=CARTESIAN_POINT('Ctrl Pts',(-0.676747416170365,-0.0141695695630101,
-3.17851599739147));
#60605=CARTESIAN_POINT('Ctrl Pts',(-0.672869095986787,-0.140314265330913,
-3.17258101139126));
#60606=CARTESIAN_POINT('Ctrl Pts',(-0.597680051307391,-0.374181953217737,
-3.16137706361834));
#60607=CARTESIAN_POINT('Ctrl Pts',(-0.347217327542774,-0.613737488914194,
-3.14557017830025));
#60608=CARTESIAN_POINT('Ctrl Pts',(-0.0128761161877245,-0.705030342238238,
-3.12976329298216));
#60609=CARTESIAN_POINT('Ctrl Pts',(0.324575622972799,-0.6260065836846,-3.11395640766407));
#60610=CARTESIAN_POINT('Ctrl Pts',(0.583618509221664,-0.395756255210866,
-3.09814952234597));
#60611=CARTESIAN_POINT('Ctrl Pts',(0.701674658922178,-0.0699017229479336,
-3.08234263702789));
#60612=CARTESIAN_POINT('Ctrl Pts',(0.650224840739586,0.272839209663541,
-3.06653575170979));
#60613=CARTESIAN_POINT('Ctrl Pts',(0.441697964735771,0.549669433198649,
-3.0507288663917));
#60614=CARTESIAN_POINT('Ctrl Pts',(0.126468587690317,0.693714115592484,
-3.03492198107361));
#60615=CARTESIAN_POINT('Ctrl Pts',(-0.219312242355004,0.6701758860164,-3.01911509575552));
#60616=CARTESIAN_POINT('Ctrl Pts',(-0.51211305746562,0.484740955787583,
-3.00330821043742));
#60617=CARTESIAN_POINT('Ctrl Pts',(-0.654502474040477,0.229974940576465,
-2.98999718572525));
#60618=CARTESIAN_POINT('Ctrl Pts',(-0.676635558168333,0.0589639985686951,
-2.98195512278578));
#60619=CARTESIAN_POINT('Ctrl Pts',(-0.676643795884942,-2.68919649208318E-6,
-2.979182021619));
#60620=CARTESIAN_POINT('Origin',(0.,0.,-4.318617978381));
#60621=CARTESIAN_POINT('',(-0.67664523128147,-4.81506944670235E-6,-3.418617978381));
#60622=CARTESIAN_POINT('',(-0.67670343080534,1.70602472024106E-5,-3.37918202161899));
#60623=CARTESIAN_POINT('',(-0.6767,-7.33509820392354E-14,-4.318617978381));
#60624=CARTESIAN_POINT('Ctrl Pts',(-0.67664523128147,-4.81506944666546E-6,
-3.418617978381));
#60625=CARTESIAN_POINT('Ctrl Pts',(-0.676657944807875,-0.0506979848076553,
-3.4162339519823));
#60626=CARTESIAN_POINT('Ctrl Pts',(-0.658607477478239,-0.213419747977293,
-3.40858096381089));
#60627=CARTESIAN_POINT('Ctrl Pts',(-0.529539984287318,-0.465640403369804,
-3.39565901386679));
#60628=CARTESIAN_POINT('Ctrl Pts',(-0.243734273318034,-0.661685109564608,
-3.3798521285487));
#60629=CARTESIAN_POINT('Ctrl Pts',(0.100951166852987,-0.697884261264305,
-3.36404524323061));
#60630=CARTESIAN_POINT('Ctrl Pts',(0.421249485401818,-0.565493104518617,
-3.34823835791252));
#60631=CARTESIAN_POINT('Ctrl Pts',(0.639785112601671,-0.296493827764879,
-3.33243147259443));
#60632=CARTESIAN_POINT('Ctrl Pts',(0.703765643119916,0.0441304857599676,
-3.31662458727633));
#60633=CARTESIAN_POINT('Ctrl Pts',(0.597735079489259,0.374094045605343,
-3.30081770195824));
#60634=CARTESIAN_POINT('Ctrl Pts',(0.347307590733571,0.613686416362823,
-3.28501081664015));
#60635=CARTESIAN_POINT('Ctrl Pts',(0.0129798091970768,0.705028442520307,
-3.26920393132206));
#60636=CARTESIAN_POINT('Ctrl Pts',(-0.324483549622869,0.626054315721524,
-3.25339704600396));
#60637=CARTESIAN_POINT('Ctrl Pts',(-0.583560298007917,0.395842088209822,
-3.23759016068587));
#60638=CARTESIAN_POINT('Ctrl Pts',(-0.670179715173758,0.15686789833644,
-3.22599713814489));
#60639=CARTESIAN_POINT('Ctrl Pts',(-0.676733456052842,0.0224457002066953,
-3.2196730773766));
#60640=CARTESIAN_POINT('Ctrl Pts',(-0.676710664634451,1.66436917362969E-5,
-3.218617978381));
#60641=CARTESIAN_POINT('Ctrl Pts',(-0.67670343080534,1.70602472024037E-5,
-3.37918202161899));
#60642=CARTESIAN_POINT('Ctrl Pts',(-0.676614623171181,-0.0872519716669216,
-3.37507687199717));
#60643=CARTESIAN_POINT('Ctrl Pts',(-0.637884772482277,-0.2866073942538,
-3.36570276060266));
#60644=CARTESIAN_POINT('Ctrl Pts',(-0.44738674868464,-0.545049240845295,
-3.35105968743544));
#60645=CARTESIAN_POINT('Ctrl Pts',(-0.133671432891043,-0.692362279354891,
-3.33525280211735));
#60646=CARTESIAN_POINT('Ctrl Pts',(0.212335352064805,-0.672418973637837,
-3.31944591679926));
#60647=CARTESIAN_POINT('Ctrl Pts',(0.507047553541136,-0.490037096853488,
-3.30363903148117));
#60648=CARTESIAN_POINT('Ctrl Pts',(0.679270528375343,-0.18927526812906,
-3.28783214616308));
#60649=CARTESIAN_POINT('Ctrl Pts',(0.6873997784289,0.157210440049462,-3.27202526084499));
#60650=CARTESIAN_POINT('Ctrl Pts',(0.529471492723354,0.465718279905297,
-3.25621837552689));
#60651=CARTESIAN_POINT('Ctrl Pts',(0.243636952032847,0.66172094832247,-3.2404114902088));
#60652=CARTESIAN_POINT('Ctrl Pts',(-0.101053807620812,0.697869404552157,
-3.22460460489071));
#60653=CARTESIAN_POINT('Ctrl Pts',(-0.421332650367923,0.565431141323669,
-3.20879771957261));
#60654=CARTESIAN_POINT('Ctrl Pts',(-0.63062236438263,0.307735384374043,
-3.19365685848205));
#60655=CARTESIAN_POINT('Ctrl Pts',(-0.676649957364854,0.0978251520198036,
-3.18378495916417));
#60656=CARTESIAN_POINT('Ctrl Pts',(-0.676735096869437,-1.28530889786354E-5,
-3.179182021619));
#60657=CARTESIAN_POINT('Origin',(0.,0.,-4.318617978381));
#60658=CARTESIAN_POINT('',(-0.676741132471547,-1.11494260315432E-5,-3.618617978381));
#60659=CARTESIAN_POINT('',(-0.676647395625952,-6.81016621412178E-6,-3.579182021619));
#60660=CARTESIAN_POINT('',(-0.6767,-7.33509820392354E-14,-4.318617978381));
#60661=CARTESIAN_POINT('Ctrl Pts',(-0.676741132471547,-1.11494260315228E-5,
-3.618617978381));
#60662=CARTESIAN_POINT('Ctrl Pts',(-0.676750354590291,-0.011790463288482,
-3.61806378836069));
#60663=CARTESIAN_POINT('Ctrl Pts',(-0.673584757733222,-0.135556650969889,
-3.61224063656769));
#60664=CARTESIAN_POINT('Ctrl Pts',(-0.601590705440622,-0.367861663287755,
-3.60114852300198));
#60665=CARTESIAN_POINT('Ctrl Pts',(-0.353666792150765,-0.610043752821873,
-3.58534163768389));
#60666=CARTESIAN_POINT('Ctrl Pts',(-0.0203063718595239,-0.704855468490197,
-3.56953475236579));
#60667=CARTESIAN_POINT('Ctrl Pts',(0.317959528732968,-0.629392817167735,
-3.55372786704772));
#60668=CARTESIAN_POINT('Ctrl Pts',(0.579414849121761,-0.401885571804838,
-3.53792098172961));
#60669=CARTESIAN_POINT('Ctrl Pts',(0.700898925634034,-0.0772934425076206,
-3.52211409641153));
#60670=CARTESIAN_POINT('Ctrl Pts',(0.653064430829429,0.265970730335282,
-3.50630721109343));
#60671=CARTESIAN_POINT('Ctrl Pts',(0.447466908630123,0.544983436344741,
-3.49050032577534));
#60672=CARTESIAN_POINT('Ctrl Pts',(0.13377326171177,0.692342613639074,-3.47469344045725));
#60673=CARTESIAN_POINT('Ctrl Pts',(-0.212236453508304,0.672450197420986,
-3.45888655513916));
#60674=CARTESIAN_POINT('Ctrl Pts',(-0.506975476514332,0.490111667298897,
-3.44307966982107));
#60675=CARTESIAN_POINT('Ctrl Pts',(-0.653260996170914,0.234732857334829,
-3.42965681090168));
#60676=CARTESIAN_POINT('Ctrl Pts',(-0.676629846509692,0.0613395218375697,
-3.42150291375499));
#60677=CARTESIAN_POINT('Ctrl Pts',(-0.67664523128147,-4.81506944666546E-6,
-3.418617978381));
#60678=CARTESIAN_POINT('Ctrl Pts',(-0.676647395625952,-6.81016621412525E-6,
-3.579182021619));
#60679=CARTESIAN_POINT('Ctrl Pts',(-0.676664625586388,-0.0483878949866939,
-3.57690670837557));
#60680=CARTESIAN_POINT('Ctrl Pts',(-0.659695506058363,-0.208793550331727,
-3.56936243335945));
#60681=CARTESIAN_POINT('Ctrl Pts',(-0.534283043471572,-0.460190403314884,
-3.55654919657064));
#60682=CARTESIAN_POINT('Ctrl Pts',(-0.250500968703414,-0.659153125247455,
-3.54074231125254));
#60683=CARTESIAN_POINT('Ctrl Pts',(0.093795489213489,-0.698881952870262,
-3.52493542593445));
#60684=CARTESIAN_POINT('Ctrl Pts',(0.41543344724007,-0.569779456245059,
-3.50912854061636));
#60685=CARTESIAN_POINT('Ctrl Pts',(0.636713714319684,-0.303033370838706,
-3.49332165529827));
#60686=CARTESIAN_POINT('Ctrl Pts',(0.704180852995891,0.0369175313181082,
-3.47751476998018));
#60687=CARTESIAN_POINT('Ctrl Pts',(0.60153659384113,0.367950138082134,-3.46170788466208));
#60688=CARTESIAN_POINT('Ctrl Pts',(0.353577064625491,0.610095760692912,
-3.44590099934399));
#60689=CARTESIAN_POINT('Ctrl Pts',(0.0202027041935265,0.704858445780369,
-3.4300941140259));
#60690=CARTESIAN_POINT('Ctrl Pts',(-0.318052093182595,0.629346044610447,
-3.41428722870781));
#60691=CARTESIAN_POINT('Ctrl Pts',(-0.579473949242324,0.401800348424625,
-3.39848034338972));
#60692=CARTESIAN_POINT('Ctrl Pts',(-0.669372488353821,0.161493655533598,
-3.38677860769344));
#60693=CARTESIAN_POINT('Ctrl Pts',(-0.676728607817933,0.024757878266858,
-3.38034583376987));
#60694=CARTESIAN_POINT('Ctrl Pts',(-0.67670343080534,1.70602472024037E-5,
-3.37918202161899));
#60695=CARTESIAN_POINT('Origin',(0.,0.,-4.318617978381));
#60696=CARTESIAN_POINT('',(-0.676696040235193,1.73011422674059E-5,-3.818617978381));
#60697=CARTESIAN_POINT('',(-0.676746306964879,-9.26850736493456E-6,-3.779182021619));
#60698=CARTESIAN_POINT('',(-0.6767,-7.33509820392354E-14,-4.318617978381));
#60699=CARTESIAN_POINT('Ctrl Pts',(-0.676696040235193,1.73011422674348E-5,
-3.818617978381));
#60700=CARTESIAN_POINT('Ctrl Pts',(-0.676610863373156,-0.0848769969584761,
-3.8146246629664));
#60701=CARTESIAN_POINT('Ctrl Pts',(-0.639436142203106,-0.281857407337619,
-3.80536238577909));
#60702=CARTESIAN_POINT('Ctrl Pts',(-0.453106684122212,-0.54030344862574,
-3.79083114681908));
#60703=CARTESIAN_POINT('Ctrl Pts',(-0.140961456517365,-0.690914982312493,
-3.775024261501));
#60704=CARTESIAN_POINT('Ctrl Pts',(0.205236307704561,-0.674619600339438,
-3.7592173761829));
#60705=CARTESIAN_POINT('Ctrl Pts',(0.501854433527548,-0.495354136485513,
-3.74341049086481));
#60706=CARTESIAN_POINT('Ctrl Pts',(0.677237850353305,-0.196424212884838,
-3.72760360554672));
#60707=CARTESIAN_POINT('Ctrl Pts',(0.689018584600613,0.149956558745365,
-3.71179672022863));
#60708=CARTESIAN_POINT('Ctrl Pts',(0.534350721904737,0.46011182080935,-3.69598983491053));
#60709=CARTESIAN_POINT('Ctrl Pts',(0.250597912301867,0.659116276136679,
-3.68018294959245));
#60710=CARTESIAN_POINT('Ctrl Pts',(-0.0936926996039382,0.698895742478711,
-3.66437606427435));
#60711=CARTESIAN_POINT('Ctrl Pts',(-0.415349642780955,0.569840551551763,
-3.64856917895626));
#60712=CARTESIAN_POINT('Ctrl Pts',(-0.628909669716038,0.312478000882297,
-3.63331648365847));
#60713=CARTESIAN_POINT('Ctrl Pts',(-0.676662675293759,0.100201366544979,
-3.62333275013339));
#60714=CARTESIAN_POINT('Ctrl Pts',(-0.676741132471547,-1.11494260315228E-5,
-3.618617978381));
#60715=CARTESIAN_POINT('Ctrl Pts',(-0.676746306964879,-9.26850736500048E-6,
-3.779182021619));
#60716=CARTESIAN_POINT('Ctrl Pts',(-0.676752713979664,-0.0094776731315671,
-3.77873654475397));
#60717=CARTESIAN_POINT('Ctrl Pts',(-0.674256040567153,-0.130932040600602,
-3.77302210611625));
#60718=CARTESIAN_POINT('Ctrl Pts',(-0.605328161907258,-0.361678580640496,
-3.76203870570583));
#60719=CARTESIAN_POINT('Ctrl Pts',(-0.359898610147466,-0.606388132436475,
-3.74623182038774));
#60720=CARTESIAN_POINT('Ctrl Pts',(-0.0275271100694295,-0.704610414814641,
-3.73042493506964));
#60721=CARTESIAN_POINT('Ctrl Pts',(0.311494209180319,-0.632617526813099,
-3.71461804975155));
#60722=CARTESIAN_POINT('Ctrl Pts',(0.575266797655111,-0.407801041483892,
-3.69881116443346));
#60723=CARTESIAN_POINT('Ctrl Pts',(0.700070201416114,-0.0844706513202744,
-3.68300427911537));
#60724=CARTESIAN_POINT('Ctrl Pts',(0.655755231597374,0.259265605233607,
-3.66719739379728));
#60725=CARTESIAN_POINT('Ctrl Pts',(0.453027208375958,0.540370175281444,
-3.65139050847919));
#60726=CARTESIAN_POINT('Ctrl Pts',(0.140859839636748,0.690935657938768,
-3.63558362316109));
#60727=CARTESIAN_POINT('Ctrl Pts',(-0.20533552647555,0.674589430258686,
-3.61977673784301));
#60728=CARTESIAN_POINT('Ctrl Pts',(-0.501927281124956,0.495280306801541,
-3.6039698525249));
#60729=CARTESIAN_POINT('Ctrl Pts',(-0.652027592210673,0.239357621077411,
-3.59043828045024));
#60730=CARTESIAN_POINT('Ctrl Pts',(-0.676624726023924,0.0636485849035314,
-3.58217567014827));
#60731=CARTESIAN_POINT('Ctrl Pts',(-0.676647395625952,-6.81016621412525E-6,
-3.579182021619));
#60732=CARTESIAN_POINT('Ctrl Pts',(-0.292601934307088,0.610169646934154,
-4.01494887079529));
#60733=CARTESIAN_POINT('Ctrl Pts',(-0.393602898590677,0.561735448896361,
-4.0096799090226));
#60734=CARTESIAN_POINT('Ctrl Pts',(-0.570992886715937,0.413800223741275,
-3.9991419854772));
#60735=CARTESIAN_POINT('Ctrl Pts',(-0.699157014481291,0.0917216394468504,
-3.98333510015911));
#60736=CARTESIAN_POINT('Ctrl Pts',(-0.658413028863308,-0.252426258090312,
-3.96752821484101));
#60737=CARTESIAN_POINT('Ctrl Pts',(-0.458619399794603,-0.535637926938055,
-3.95172132952293));
#60738=CARTESIAN_POINT('Ctrl Pts',(-0.148032691342333,-0.689431756556144,
-3.93591444420484));
#60739=CARTESIAN_POINT('Ctrl Pts',(0.198313347812299,-0.676688375201064,
-3.92010755888674));
#60740=CARTESIAN_POINT('Ctrl Pts',(0.496752882142743,-0.50046932737395,
-3.90430067356866));
#60741=CARTESIAN_POINT('Ctrl Pts',(0.675189733576972,-0.203353101808354,
-3.88849378825056));
#60742=CARTESIAN_POINT('Ctrl Pts',(0.690518863850223,0.142889328597765,
-3.87268690293247));
#60743=CARTESIAN_POINT('Ctrl Pts',(0.539036872034762,0.454612727099145,
-3.85688001761438));
#60744=CARTESIAN_POINT('Ctrl Pts',(0.257337933699506,0.656514151291388,
-3.84107313229629));
#60745=CARTESIAN_POINT('Ctrl Pts',(-0.0865270426321366,0.699818987663747,
-3.82526624697819));
#60746=CARTESIAN_POINT('Ctrl Pts',(-0.409489369688631,0.574066239054321,
-3.8094593616601));
#60747=CARTESIAN_POINT('Ctrl Pts',(-0.633529943812292,0.309634276622324,
-3.79365247634201));
#60748=CARTESIAN_POINT('Ctrl Pts',(-0.704526500534943,-0.0295970794965726,
-3.77784559102392));
#60749=CARTESIAN_POINT('Ctrl Pts',(-0.605328161907258,-0.361678580640496,
-3.76203870570583));
#60750=CARTESIAN_POINT('Ctrl Pts',(-0.359898610147466,-0.606388132436475,
-3.74623182038774));
#60751=CARTESIAN_POINT('Ctrl Pts',(-0.0275271100694295,-0.704610414814641,
-3.73042493506964));
#60752=CARTESIAN_POINT('Ctrl Pts',(0.311494209180319,-0.632617526813099,
-3.71461804975155));
#60753=CARTESIAN_POINT('Ctrl Pts',(0.575266797655111,-0.407801041483892,
-3.69881116443346));
#60754=CARTESIAN_POINT('Ctrl Pts',(0.700070201416114,-0.0844706513202744,
-3.68300427911537));
#60755=CARTESIAN_POINT('Ctrl Pts',(0.655755231597374,0.259265605233607,
-3.66719739379728));
#60756=CARTESIAN_POINT('Ctrl Pts',(0.453027208375958,0.540370175281444,
-3.65139050847919));
#60757=CARTESIAN_POINT('Ctrl Pts',(0.140859839636748,0.690935657938768,
-3.63558362316109));
#60758=CARTESIAN_POINT('Ctrl Pts',(-0.20533552647555,0.674589430258686,
-3.61977673784301));
#60759=CARTESIAN_POINT('Ctrl Pts',(-0.501927281124956,0.495280306801541,
-3.6039698525249));
#60760=CARTESIAN_POINT('Ctrl Pts',(-0.677266731001841,0.19632461109843,
-3.58816296720682));
#60761=CARTESIAN_POINT('Ctrl Pts',(-0.688996520342533,-0.150057898161934,
-3.57235608188872));
#60762=CARTESIAN_POINT('Ctrl Pts',(-0.534283043471572,-0.460190403314884,
-3.55654919657064));
#60763=CARTESIAN_POINT('Ctrl Pts',(-0.250500968703414,-0.659153125247455,
-3.54074231125254));
#60764=CARTESIAN_POINT('Ctrl Pts',(0.093795489213489,-0.698881952870262,
-3.52493542593445));
#60765=CARTESIAN_POINT('Ctrl Pts',(0.41543344724007,-0.569779456245059,
-3.50912854061636));
#60766=CARTESIAN_POINT('Ctrl Pts',(0.636713714319684,-0.303033370838706,
-3.49332165529827));
#60767=CARTESIAN_POINT('Ctrl Pts',(0.704180852995891,0.0369175313181082,
-3.47751476998018));
#60768=CARTESIAN_POINT('Ctrl Pts',(0.60153659384113,0.367950138082134,-3.46170788466208));
#60769=CARTESIAN_POINT('Ctrl Pts',(0.353577064625491,0.610095760692912,
-3.44590099934399));
#60770=CARTESIAN_POINT('Ctrl Pts',(0.0202027041935265,0.704858445780369,
-3.4300941140259));
#60771=CARTESIAN_POINT('Ctrl Pts',(-0.318052093182595,0.629346044610447,
-3.41428722870781));
#60772=CARTESIAN_POINT('Ctrl Pts',(-0.579473949242324,0.401800348424625,
-3.39848034338972));
#60773=CARTESIAN_POINT('Ctrl Pts',(-0.700910284405168,0.0771903560019862,
-3.38267345807162));
#60774=CARTESIAN_POINT('Ctrl Pts',(-0.653025304273793,-0.266066776999244,
-3.36686657275354));
#60775=CARTESIAN_POINT('Ctrl Pts',(-0.44738674868464,-0.545049240845295,
-3.35105968743544));
#60776=CARTESIAN_POINT('Ctrl Pts',(-0.133671432891043,-0.692362279354891,
-3.33525280211735));
#60777=CARTESIAN_POINT('Ctrl Pts',(0.212335352064805,-0.672418973637837,
-3.31944591679926));
#60778=CARTESIAN_POINT('Ctrl Pts',(0.507047553541136,-0.490037096853488,
-3.30363903148117));
#60779=CARTESIAN_POINT('Ctrl Pts',(0.679270528375343,-0.18927526812906,
-3.28783214616308));
#60780=CARTESIAN_POINT('Ctrl Pts',(0.6873997784289,0.157210440049462,-3.27202526084499));
#60781=CARTESIAN_POINT('Ctrl Pts',(0.529471492723354,0.465718279905297,
-3.25621837552689));
#60782=CARTESIAN_POINT('Ctrl Pts',(0.243636952032847,0.66172094832247,-3.2404114902088));
#60783=CARTESIAN_POINT('Ctrl Pts',(-0.101053807620812,0.697869404552157,
-3.22460460489071));
#60784=CARTESIAN_POINT('Ctrl Pts',(-0.421332650367923,0.565431141323669,
-3.20879771957261));
#60785=CARTESIAN_POINT('Ctrl Pts',(-0.639828711318305,0.29639972674988,
-3.19299083425453));
#60786=CARTESIAN_POINT('Ctrl Pts',(-0.703759143294702,-0.0442339922882071,
-3.17718394893643));
#60787=CARTESIAN_POINT('Ctrl Pts',(-0.597680051307391,-0.374181953217737,
-3.16137706361834));
#60788=CARTESIAN_POINT('Ctrl Pts',(-0.347217327542774,-0.613737488914194,
-3.14557017830025));
#60789=CARTESIAN_POINT('Ctrl Pts',(-0.0128761161877245,-0.705030342238238,
-3.12976329298216));
#60790=CARTESIAN_POINT('Ctrl Pts',(0.324575622972799,-0.6260065836846,-3.11395640766407));
#60791=CARTESIAN_POINT('Ctrl Pts',(0.583618509221664,-0.395756255210866,
-3.09814952234597));
#60792=CARTESIAN_POINT('Ctrl Pts',(0.701674658922178,-0.0699017229479336,
-3.08234263702789));
#60793=CARTESIAN_POINT('Ctrl Pts',(0.650224840739586,0.272839209663541,
-3.06653575170979));
#60794=CARTESIAN_POINT('Ctrl Pts',(0.441697964735771,0.549669433198649,
-3.0507288663917));
#60795=CARTESIAN_POINT('Ctrl Pts',(0.126468587690317,0.693714115592484,
-3.03492198107361));
#60796=CARTESIAN_POINT('Ctrl Pts',(-0.219312242355004,0.6701758860164,-3.01911509575552));
#60797=CARTESIAN_POINT('Ctrl Pts',(-0.51211305746562,0.484740955787583,
-3.00330821043742));
#60798=CARTESIAN_POINT('Ctrl Pts',(-0.681200954676895,0.182205480685776,
-2.98750132511933));
#60799=CARTESIAN_POINT('Ctrl Pts',(-0.685728787366566,-0.164346000929208,
-2.97169443980124));
#60800=CARTESIAN_POINT('Ctrl Pts',(-0.524602751372391,-0.471195852164642,
-2.95588755448315));
#60801=CARTESIAN_POINT('Ctrl Pts',(-0.236746619036826,-0.664217295935056,
-2.94008066916506));
#60802=CARTESIAN_POINT('Ctrl Pts',(0.108301210750851,-0.696781476213702,
-2.92427378384697));
#60803=CARTESIAN_POINT('Ctrl Pts',(0.427186343456901,-0.56102175163586,
-2.90846689852887));
#60804=CARTESIAN_POINT('Ctrl Pts',(0.642874597533564,-0.289734067190421,
-2.89266001321078));
#60805=CARTESIAN_POINT('Ctrl Pts',(0.703261417396002,0.0515456753453884,
-2.87685312789269));
#60806=CARTESIAN_POINT('Ctrl Pts',(0.593758950657057,0.38037335127382,-2.8610462425746));
#60807=CARTESIAN_POINT('Ctrl Pts',(0.340820085951307,0.617312924582654,
-2.84523935725651));
#60808=CARTESIAN_POINT('Ctrl Pts',(0.00554813737457995,0.705126085190668,
-2.82943247193842));
#60809=CARTESIAN_POINT('Ctrl Pts',(-0.33106409388682,0.622599504965708,
-2.81362558662032));
#60810=CARTESIAN_POINT('Ctrl Pts',(-0.587700029934952,0.389669414579977,
-2.79781870130224));
#60811=CARTESIAN_POINT('Ctrl Pts',(-0.702363242396234,0.062605539493679,
-2.78201181598414));
#60812=CARTESIAN_POINT('Ctrl Pts',(-0.647354143489211,-0.279582171734887,
-2.76620493066605));
#60813=CARTESIAN_POINT('Ctrl Pts',(-0.435961470998621,-0.554230253278693,
-2.75039804534796));
#60814=CARTESIAN_POINT('Ctrl Pts',(-0.11925208204733,-0.694991020641291,
-2.73459116002987));
#60815=CARTESIAN_POINT('Ctrl Pts',(0.226265443741279,-0.667860409676459,
-2.71878427471177));
#60816=CARTESIAN_POINT('Ctrl Pts',(0.517123245750236,-0.479392455665905,
-2.70297738939368));
#60817=CARTESIAN_POINT('Ctrl Pts',(0.683057801392575,-0.17511601240717,
-2.68717050407559));
#60818=CARTESIAN_POINT('Ctrl Pts',(0.683983727646747,0.17146381005654,-2.6713636187575));
#60819=CARTESIAN_POINT('Ctrl Pts',(0.519677345313422,0.47662252843591,-2.65555673343941));
#60820=CARTESIAN_POINT('Ctrl Pts',(0.229830713971266,0.666641898443312,
-2.63974984812131));
#60821=CARTESIAN_POINT('Ctrl Pts',(-0.115536915778911,0.695618285367013,
-2.62394296280322));
#60822=CARTESIAN_POINT('Ctrl Pts',(-0.432993894223229,0.556551763459652,
-2.60813607748513));
#60823=CARTESIAN_POINT('Ctrl Pts',(-0.645851043965561,0.283037112148287,
-2.59232919216704));
#60824=CARTESIAN_POINT('Ctrl Pts',(-0.70268772906141,-0.0588517907218158,
-2.57652230684895));
#60825=CARTESIAN_POINT('Ctrl Pts',(-0.589773715425885,-0.386523663489563,
-2.56071542153086));
#60826=CARTESIAN_POINT('Ctrl Pts',(-0.334386030845991,-0.620821681499372,
-2.54490853621277));
#60827=CARTESIAN_POINT('Ctrl Pts',(0.00178044071789455,-0.705145664296035,
-2.52910165089467));
#60828=CARTESIAN_POINT('Ctrl Pts',(0.337516805075675,-0.619125176467695,
-2.51329476557658));
#60829=CARTESIAN_POINT('Ctrl Pts',(0.591718070518745,-0.383540483999043,
-2.49748788025849));
#60830=CARTESIAN_POINT('Ctrl Pts',(0.702975960450328,-0.0553025937328847,
-2.4816809949404));
#60831=CARTESIAN_POINT('Ctrl Pts',(0.644413522599621,0.286294934875548,
-2.46587410962231));
#60832=CARTESIAN_POINT('Ctrl Pts',(0.430177887097737,0.558731208450694,
-2.45006722430421));
#60833=CARTESIAN_POINT('Ctrl Pts',(0.112022695449392,0.69619285657704,-2.43426033898612));
#60834=CARTESIAN_POINT('Ctrl Pts',(-0.233194205177004,0.665472794723054,
-2.41845345366803));
#60835=CARTESIAN_POINT('Ctrl Pts',(-0.522077577221963,0.473992174204058,
-2.40264656834994));
#60836=CARTESIAN_POINT('Ctrl Pts',(-0.684840867956002,0.168007629058669,
-2.38683968303185));
#60837=CARTESIAN_POINT('Ctrl Pts',(-0.682164787761207,-0.178563098604814,
-2.37103279771376));
#60838=CARTESIAN_POINT('Ctrl Pts',(-0.514695806561756,-0.481997722559338,
-2.35522591239567));
#60839=CARTESIAN_POINT('Ctrl Pts',(-0.222889983854245,-0.668994493954996,
-2.33941902707757));
#60840=CARTESIAN_POINT('Ctrl Pts',(0.122760141143874,-0.694379957653575,
-2.32361214175949));
#60841=CARTESIAN_POINT('Ctrl Pts',(0.438754675367169,-0.55202165961862,
-2.30780525644139));
#60842=CARTESIAN_POINT('Ctrl Pts',(0.648757729114897,-0.276309584991779,
-2.2919983711233));
#60843=CARTESIAN_POINT('Ctrl Pts',(0.702038140257588,0.0661515492510317,
-2.2761914858052));
#60844=CARTESIAN_POINT('Ctrl Pts',(0.585724776077096,0.392632225542023,
-2.26038460048712));
#60845=CARTESIAN_POINT('Ctrl Pts',(0.327915857198116,0.624263380667703,
-2.24457771516902));
#60846=CARTESIAN_POINT('Ctrl Pts',(-0.0091088264969462,0.705089077439507,
-2.22877082985093));
#60847=CARTESIAN_POINT('Ctrl Pts',(-0.343933059552939,0.615583973468446,
-2.21296394453284));
#60848=CARTESIAN_POINT('Ctrl Pts',(-0.595672196966363,0.377370125481488,
-2.19715705921475));
#60849=CARTESIAN_POINT('Ctrl Pts',(-0.703512746902021,0.0479936744896455,
-2.18135017389665));
#60850=CARTESIAN_POINT('Ctrl Pts',(-0.641403295700533,-0.292976774009718,
-2.16554328857857));
#60851=CARTESIAN_POINT('Ctrl Pts',(-0.424347837744089,-0.563171812546191,
-2.14973640326047));
#60852=CARTESIAN_POINT('Ctrl Pts',(-0.104781208775136,-0.697319493584015,
-2.13392951794238));
#60853=CARTESIAN_POINT('Ctrl Pts',(0.240097778255422,-0.663013299053236,
-2.11812263262429));
#60854=CARTESIAN_POINT('Ctrl Pts',(0.526975516741124,-0.46854069471079,
-2.1023157473062));
#60855=CARTESIAN_POINT('Ctrl Pts',(0.68654996177012,-0.160881098448797,
-2.08650886198811));
#60856=CARTESIAN_POINT('Ctrl Pts',(0.680272164181842,0.185643099747873,
-2.07070197667002));
#60857=CARTESIAN_POINT('Ctrl Pts',(0.509658673195849,0.48732085393598,-2.05489509135192));
#60858=CARTESIAN_POINT('Ctrl Pts',(0.215925178385313,0.671274828355656,
-2.03908820603383));
#60859=CARTESIAN_POINT('Ctrl Pts',(-0.129970106632608,0.693066626830752,
-2.02328132071574));
#60860=CARTESIAN_POINT('Ctrl Pts',(-0.444468064640782,0.547431929429699,
-2.00747443539765));
#60861=CARTESIAN_POINT('Ctrl Pts',(-0.651594339017406,0.269552212391435,
-1.99166755007956));
#60862=CARTESIAN_POINT('Ctrl Pts',(-0.701312721149553,-0.0734441624532127,
-1.97586066476146));
#60863=CARTESIAN_POINT('Ctrl Pts',(-0.581612569954882,-0.398698377617872,
-1.96005377944337));
#60864=CARTESIAN_POINT('Ctrl Pts',(-0.321410263880308,-0.627637650334202,
-1.94424689412528));
#60865=CARTESIAN_POINT('Ctrl Pts',(0.0164362283905885,-0.704956330733284,
-1.92844000880719));
#60866=CARTESIAN_POINT('Ctrl Pts',(0.350312164270045,-0.611976278469258,
-1.9126331234891));
#60867=CARTESIAN_POINT('Ctrl Pts',(0.599561982174783,-0.37115900551555,
-1.896826238171));
#60868=CARTESIAN_POINT('Ctrl Pts',(0.70397354377059,-0.0406795712332764,
-1.88101935285292));
#60869=CARTESIAN_POINT('Ctrl Pts',(0.638323787940124,0.29962696740183,-1.86521246753482));
#60870=CARTESIAN_POINT('Ctrl Pts',(0.41847195266759,0.567551585915519,-1.84940558221673));
#60871=CARTESIAN_POINT('Ctrl Pts',(0.0975284042101817,0.698370809969075,
-1.83359869689864));
#60872=CARTESIAN_POINT('Ctrl Pts',(-0.246975417290485,0.660482188328222,
-1.81779181158055));
#60873=CARTESIAN_POINT('Ctrl Pts',(-0.531816535259198,0.46303860602497,
-1.80198492626245));
#60874=CARTESIAN_POINT('Ctrl Pts',(-0.688184898228003,0.153737190346249,
-1.78617804094436));
#60875=CARTESIAN_POINT('Ctrl Pts',(-0.678306061339454,-0.192703048742882,
-1.77037115562627));
#60876=CARTESIAN_POINT('Ctrl Pts',(-0.504566489299185,-0.492591347590416,
-1.75456427030818));
#60877=CARTESIAN_POINT('Ctrl Pts',(-0.208937049864503,-0.6734826553361,
-1.73875738499009));
#60878=CARTESIAN_POINT('Ctrl Pts',(0.137166033464237,-0.691678434757318,
-1.722950499672));
#60879=CARTESIAN_POINT('Ctrl Pts',(0.450133444915136,-0.542783068650339,
-1.70714361435391));
#60880=CARTESIAN_POINT('Ctrl Pts',(0.654360567278065,-0.262765724241526,
-1.69133672903581));
#60881=CARTESIAN_POINT('Ctrl Pts',(0.700511550093094,0.0807288426203301,
-1.67552984371772));
#60882=CARTESIAN_POINT('Ctrl Pts',(0.577437541237162,0.404721464484683,
-1.65972295839963));
#60883=CARTESIAN_POINT('Ctrl Pts',(0.314869953591033,0.630944126028784,
-1.64391607308154));
#60884=CARTESIAN_POINT('Ctrl Pts',(-0.0237618549331032,0.704747438515944,
-1.62810918776345));
#60885=CARTESIAN_POINT('Ctrl Pts',(-0.356653430191126,0.608302481153537,
-1.61230230244536));
#60886=CARTESIAN_POINT('Ctrl Pts',(-0.603387005990771,0.364907794992297,
-1.59649541712726));
#60887=CARTESIAN_POINT('Ctrl Pts',(-0.704358301283286,0.0333610739930403,
-1.58068853180917));
#60888=CARTESIAN_POINT('Ctrl Pts',(-0.63517533194991,-0.306244796734519,
-1.56488164649108));
#60889=CARTESIAN_POINT('Ctrl Pts',(-0.412550866549072,-0.571870055479614,
-1.54907476117299));
#60890=CARTESIAN_POINT('Ctrl Pts',(-0.0902650651626452,-0.699346692174796,
-1.5332678758549));
#60891=CARTESIAN_POINT('Ctrl Pts',(0.253826379397398,-0.65787973594469,
-1.5174609905368));
#60892=CARTESIAN_POINT('Ctrl Pts',(0.536600109875943,-0.457486502452008,
-1.50165410521871));
#60893=CARTESIAN_POINT('Ctrl Pts',(0.689745500732789,-0.146576676396754,
-1.48584721990062));
#60894=CARTESIAN_POINT('Ctrl Pts',(0.67626669160168,0.199742183012912,-1.47004033458253));
#60895=CARTESIAN_POINT('Ctrl Pts',(0.499419804901498,0.497808634232871,
-1.45423344926444));
#60896=CARTESIAN_POINT('Ctrl Pts',(0.201926353111081,0.675617736418978,
-1.43842656394635));
#60897=CARTESIAN_POINT('Ctrl Pts',(-0.144347144374269,0.690215531378164,
-1.42261967862825));
#60898=CARTESIAN_POINT('Ctrl Pts',(-0.455750204246968,0.538075579424947,
-1.40681279331016));
#60899=CARTESIAN_POINT('Ctrl Pts',(-0.657056115104094,0.255950853581234,
-1.39100590799207));
#60900=CARTESIAN_POINT('Ctrl Pts',(-0.699634713626303,-0.088004802901243,
-1.37519902267398));
#60901=CARTESIAN_POINT('Ctrl Pts',(-0.573200140887612,-0.410700835561685,
-1.35939213735589));
#60902=CARTESIAN_POINT('Ctrl Pts',(-0.308295632778683,-0.634182450604112,
-1.3435852520378));
#60903=CARTESIAN_POINT('Ctrl Pts',(0.0310849148505515,-0.704462423350869,
-1.3277783667197));
#60904=CARTESIAN_POINT('Ctrl Pts',(0.362956172367475,-0.604562978344687,
-1.31197148140161));
#60905=CARTESIAN_POINT('Ctrl Pts',(0.607146855256262,-0.358617169133155,
-1.29616459608352));
#60906=CARTESIAN_POINT('Ctrl Pts',(0.704666977880717,-0.026038973272816,
-1.28035771076543));
#60907=CARTESIAN_POINT('Ctrl Pts',(0.631958267808816,0.312829547186207,
-1.26455082544734));
#60908=CARTESIAN_POINT('Ctrl Pts',(0.40658521895174,0.57612675478111,-1.24874394012925));
#60909=CARTESIAN_POINT('Ctrl Pts',(0.0829919761785184,0.700247034791744,
-1.23293705481115));
#60910=CARTESIAN_POINT('Ctrl Pts',(-0.26064992457286,0.655206223005252,
-1.21713016949306));
#60911=CARTESIAN_POINT('Ctrl Pts',(-0.541325723895911,0.45188498369963,
-1.20132328417497));
#60912=CARTESIAN_POINT('Ctrl Pts',(-0.691231600716771,0.139400330039688,
-1.18551639885688));
#60913=CARTESIAN_POINT('Ctrl Pts',(-0.674154275250033,-0.206759742229352,
-1.16970951353879));
#60914=CARTESIAN_POINT('Ctrl Pts',(-0.494219175919373,-0.502972150320693,
-1.15390262822069));
#60915=CARTESIAN_POINT('Ctrl Pts',(-0.194893845382005,-0.677679840984561,
-1.1380957429026));
#60916=CARTESIAN_POINT('Ctrl Pts',(0.15151266369854,-0.688678074708074,
-1.12228885758451));
#60917=CARTESIAN_POINT('Ctrl Pts',(0.461317735944786,-0.533309970230656,
-1.10648197226642));
#60918=CARTESIAN_POINT('Ctrl Pts',(0.659680691337217,-0.249108336515458,
-1.09067508694833));
#60919=CARTESIAN_POINT('Ctrl Pts',(0.698682306460244,0.0952712573866783,
-1.07486820163024));
#60920=CARTESIAN_POINT('Ctrl Pts',(0.568900826606944,0.41663584499006,-1.05906131631215));
#60921=CARTESIAN_POINT('Ctrl Pts',(0.301688011565286,0.637352274274148,
-1.04325443099405));
#60922=CARTESIAN_POINT('Ctrl Pts',(-0.0384046171462246,0.704101316023837,
-1.02744754567596));
#60923=CARTESIAN_POINT('Ctrl Pts',(-0.369219710011492,0.600758173963263,
-1.01164066035787));
#60924=CARTESIAN_POINT('Ctrl Pts',(-0.610841123852988,0.352287807416983,
-0.99583377503978));
#60925=CARTESIAN_POINT('Ctrl Pts',(-0.704899540221332,0.0187140599657082,
-0.980026889721685));
#60926=CARTESIAN_POINT('Ctrl Pts',(-0.62867294300644,-0.319380507508313,
-0.964220004403597));
#60927=CARTESIAN_POINT('Ctrl Pts',(-0.400575654252081,-0.580321224034726,
-0.948413119085501));
#60928=CARTESIAN_POINT('Ctrl Pts',(-0.07570992285693,-0.701071740569853,
-0.932606233767413));
#60929=CARTESIAN_POINT('Ctrl Pts',(0.267445315774999,-0.652461938288095,
-0.916799348449319));
#60930=CARTESIAN_POINT('Ctrl Pts',(0.545992866884217,-0.446234654813134,
-0.900992463131228));
#60931=CARTESIAN_POINT('Ctrl Pts',(0.69264303765959,-0.132208926424586,
-0.885185577813137));
#60932=CARTESIAN_POINT('Ctrl Pts',(0.671969040456129,0.213754968393986,
-0.869378692495044));
#60933=CARTESIAN_POINT('Ctrl Pts',(0.488965164096191,0.508081338119234,
-0.853571807176953));
#60934=CARTESIAN_POINT('Ctrl Pts',(0.187840286290136,0.679668746295639,
-0.837764921858861));
#60935=CARTESIAN_POINT('Ctrl Pts',(-0.158661817457009,0.687066230814675,
-0.821958036540769));
#60936=CARTESIAN_POINT('Ctrl Pts',(-0.466835438634391,0.528486755822397,
-0.806151151222678));
#60937=CARTESIAN_POINT('Ctrl Pts',(-0.662234012485122,0.242238912135313,
-0.790344265904586));
#60938=CARTESIAN_POINT('Ctrl Pts',(-0.697654431468708,-0.102527421194134,
-0.774537380586495));
#60939=CARTESIAN_POINT('Ctrl Pts',(-0.564540062783472,-0.422525851702685,
-0.758730495268403));
#60940=CARTESIAN_POINT('Ctrl Pts',(-0.295047803669792,-0.640453254651953,
-0.742923609950312));
#60941=CARTESIAN_POINT('Ctrl Pts',(0.045720171186077,-0.703664155539672,
-0.727116724632219));
#60942=CARTESIAN_POINT('Ctrl Pts',(0.375443366570243,-0.596888478983344,
-0.711309839314129));
#60943=CARTESIAN_POINT('Ctrl Pts',(0.614469412746345,-0.345920393506668,
-0.695502953996035));
#60944=CARTESIAN_POINT('Ctrl Pts',(0.705055963185025,-0.0113871252686242,
-0.679696068677945));
#60945=CARTESIAN_POINT('Ctrl Pts',(0.625319712405524,0.325896970102082,
-0.663889183359852));
#60946=CARTESIAN_POINT('Ctrl Pts',(0.394522821570273,0.584453010176933,
-0.648082298041761));
#60947=CARTESIAN_POINT('Ctrl Pts',(0.0684196917652833,0.701820720428935,
-0.632275412723669));
#60948=CARTESIAN_POINT('Ctrl Pts',(-0.274211819002972,0.649647178215781,
-0.616468527405578));
#60949=CARTESIAN_POINT('Ctrl Pts',(-0.550601034721718,0.440536126110014,
-0.600661642087486));
#60950=CARTESIAN_POINT('Ctrl Pts',(-0.693979659105578,0.125003242327362,
-0.584854756769395));
#60951=CARTESIAN_POINT('Ctrl Pts',(-0.669711223257026,-0.220727105920912,
-0.569047871451302));
#60952=CARTESIAN_POINT('Ctrl Pts',(-0.483658336941455,-0.513135645762089,
-0.55324098613321));
#60953=CARTESIAN_POINT('Ctrl Pts',(-0.18076643772218,-0.681584237521583,
-0.537434100815119));
#60954=CARTESIAN_POINT('Ctrl Pts',(0.165793833437332,-0.685380173800492,
-0.521627215497027));
#60955=CARTESIAN_POINT('Ctrl Pts',(0.47230271632388,-0.523606457177304,
-0.505820330178935));
#60956=CARTESIAN_POINT('Ctrl Pts',(0.66471580275202,-0.235343322438281,
-0.490013444860844));
#60957=CARTESIAN_POINT('Ctrl Pts',(0.696551199677241,0.109772510552645,
-0.474206559542751));
#60958=CARTESIAN_POINT('Ctrl Pts',(0.560118320442681,0.428370219493409,
-0.458399674224661));
#60959=CARTESIAN_POINT('Ctrl Pts',(0.288375726331517,0.643485056786609,
-0.442592788906568));
#60960=CARTESIAN_POINT('Ctrl Pts',(-0.0530307867851691,0.703150989118139,
-0.426785903588478));
#60961=CARTESIAN_POINT('Ctrl Pts',(-0.381626469796513,0.59295431138796,
-0.410979018270385));
#60962=CARTESIAN_POINT('Ctrl Pts',(-0.618031330032434,0.339515615175607,
-0.395172132952294));
#60963=CARTESIAN_POINT('Ctrl Pts',(-0.705136229868134,0.00405896059619597,
-0.379365247634201));
#60964=CARTESIAN_POINT('Ctrl Pts',(-0.621898938218708,-0.332378231093819,
-0.36355836231611));
#60965=CARTESIAN_POINT('Ctrl Pts',(-0.388427374670541,-0.588521666917222,
-0.347751476998018));
#60966=CARTESIAN_POINT('Ctrl Pts',(-0.0611220704120482,-0.702493893463718,
-0.331944591679926));
#60967=CARTESIAN_POINT('Ctrl Pts',(0.280948703489239,-0.646762246832194,
-0.316137706361835));
#60968=CARTESIAN_POINT('Ctrl Pts',(0.555149729438401,-0.434790013096512,
-0.300330821043743));
#60969=CARTESIAN_POINT('Ctrl Pts',(0.695241321112673,-0.117784056100728,
-0.284523935725652));
#60970=CARTESIAN_POINT('Ctrl Pts',(0.667381066683655,0.227675401785218,
-0.268717050407559));
#60971=CARTESIAN_POINT('Ctrl Pts',(0.47829926932486,0.518134527179428,-0.252910165089469));
#60972=CARTESIAN_POINT('Ctrl Pts',(0.173673060517654,0.683426108018395,
-0.237103279771376));
#60973=CARTESIAN_POINT('Ctrl Pts',(-0.172907934941646,0.683620085281621,
-0.221296394453285));
#60974=CARTESIAN_POINT('Ctrl Pts',(-0.477718990865722,0.518669602421621,
-0.205489509135192));
#60975=CARTESIAN_POINT('Ctrl Pts',(-0.667125769812111,0.228422310324478,
-0.189682623817101));
#60976=CARTESIAN_POINT('Ctrl Pts',(-0.695372777708953,-0.117005739123839,
-0.173875738499009));
#60977=CARTESIAN_POINT('Ctrl Pts',(-0.555635984344507,-0.434168324449232,
-0.158068853180918));
#60978=CARTESIAN_POINT('Ctrl Pts',(-0.281672681898704,-0.646447338792661,
-0.142261967862826));
#60979=CARTESIAN_POINT('Ctrl Pts',(0.0603360297254143,-0.702561900375898,
-0.126455082544735));
#60980=CARTESIAN_POINT('Ctrl Pts',(0.38776765641086,-0.588956040974949,
-0.110648197226643));
#60981=CARTESIAN_POINT('Ctrl Pts',(0.621527851581432,-0.333074272139639,
-0.0948413119085513));
#60982=CARTESIAN_POINT('Ctrl Pts',(0.705137669332003,0.00326985369309036,
-0.0790344265904595));
#60983=CARTESIAN_POINT('Ctrl Pts',(0.618416201049889,0.338823176482188,
-0.0632275412723679));
#60984=CARTESIAN_POINT('Ctrl Pts',(0.38227975109817,0.59252757256583,-0.0474206559542765));
#60985=CARTESIAN_POINT('Ctrl Pts',(0.0538381161213402,0.703089501623881,
-0.0316137706361843));
#60986=CARTESIAN_POINT('Ctrl Pts',(-0.287697821498663,0.643811669165333,
-0.015806885318092));
#60987=CARTESIAN_POINT('Ctrl Pts',(-0.468914126304642,0.500589151378386,
-0.00526896177269799));
#60988=CARTESIAN_POINT('Ctrl Pts',(-0.537060862935893,0.41168983410154,
-8.88178419700125E-16));
#60989=CARTESIAN_POINT('Ctrl Pts',(-0.309090610374634,0.644553868208609,
-3.9929325805302));
#60990=CARTESIAN_POINT('Ctrl Pts',(-0.415783171285996,0.593390310900079,
-3.9876636187575));
#60991=CARTESIAN_POINT('Ctrl Pts',(-0.603169422965529,0.437118654161456,
-3.9771256952121));
#60992=CARTESIAN_POINT('Ctrl Pts',(-0.738555843335368,0.0968903284536621,
-3.96131880989401));
#60993=CARTESIAN_POINT('Ctrl Pts',(-0.695515856557493,-0.266650958314697,
-3.94551192457592));
#60994=CARTESIAN_POINT('Ctrl Pts',(-0.484463476114247,-0.565822143893725,
-3.92970503925783));
#60995=CARTESIAN_POINT('Ctrl Pts',(-0.156374615331088,-0.728282548610733,
-3.91389815393974));
#60996=CARTESIAN_POINT('Ctrl Pts',(0.209488682519811,-0.714821053454846,
-3.89809126862164));
#60997=CARTESIAN_POINT('Ctrl Pts',(0.524745852793018,-0.528671726788554,
-3.88228438330356));
#60998=CARTESIAN_POINT('Ctrl Pts',(0.713237960522051,-0.214812436248472,
-3.86647749798546));
#60999=CARTESIAN_POINT('Ctrl Pts',(0.72943091647052,0.150941414303679,-3.85067061266737));
#61000=CARTESIAN_POINT('Ctrl Pts',(0.56941262601771,0.4802310197843,-3.83486372734927));
#61001=CARTESIAN_POINT('Ctrl Pts',(0.271839416195556,0.693509973619221,
-3.81905684203119));
#61002=CARTESIAN_POINT('Ctrl Pts',(-0.0914030062187122,0.73925511996695,
-3.80324995671309));
#61003=CARTESIAN_POINT('Ctrl Pts',(-0.432564875275732,0.60641596455938,
-3.78744307139501));
#61004=CARTESIAN_POINT('Ctrl Pts',(-0.66923056229026,0.327082757606315,
-3.77163618607691));
#61005=CARTESIAN_POINT('Ctrl Pts',(-0.744227910150822,-0.0312649312745136,
-3.75582930075882));
#61006=CARTESIAN_POINT('Ctrl Pts',(-0.639439556283001,-0.382059857240302,
-3.74002241544073));
#61007=CARTESIAN_POINT('Ctrl Pts',(-0.380179582021205,-0.640559258169556,
-3.72421553012264));
#61008=CARTESIAN_POINT('Ctrl Pts',(-0.0290783151292548,-0.74431655315994,
-3.70840864480454));
#61009=CARTESIAN_POINT('Ctrl Pts',(0.329047500904973,-0.668266728856064,
-3.69260175948646));
#61010=CARTESIAN_POINT('Ctrl Pts',(0.607684176922999,-0.430781406562343,
-3.67679487416836));
#61011=CARTESIAN_POINT('Ctrl Pts',(0.739520490092536,-0.0892307333413812,
-3.66098798885027));
#61012=CARTESIAN_POINT('Ctrl Pts',(0.692708287355583,0.273875715690588,
-3.64518110353218));
#61013=CARTESIAN_POINT('Ctrl Pts',(0.478556154062485,0.570821063440742,
-3.62937421821409));
#61014=CARTESIAN_POINT('Ctrl Pts',(0.14879755977588,0.729871197699466,-3.613567332896));
#61015=CARTESIAN_POINT('Ctrl Pts',(-0.21690657431989,0.712603828968895,
-3.5977604475779));
#61016=CARTESIAN_POINT('Ctrl Pts',(-0.530211839009143,0.523190295027787,
-3.58195356225981));
#61017=CARTESIAN_POINT('Ctrl Pts',(-0.715432000706095,0.207387876705873,
-3.56614667694172));
#61018=CARTESIAN_POINT('Ctrl Pts',(-0.727822786007864,-0.158513946410649,
-3.55033979162363));
#61019=CARTESIAN_POINT('Ctrl Pts',(-0.564390910164421,-0.48612300867384,
-3.53453290630553));
#61020=CARTESIAN_POINT('Ctrl Pts',(-0.264617175205399,-0.696297658781914,
-3.51872602098745));
#61021=CARTESIAN_POINT('Ctrl Pts',(0.0990810436029352,-0.738265281478883,
-3.50291913566935));
#61022=CARTESIAN_POINT('Ctrl Pts',(0.438843912913809,-0.601887613377435,
-3.48711225035126));
#61023=CARTESIAN_POINT('Ctrl Pts',(0.672593744327157,-0.320109878214677,
-3.47130536503317));
#61024=CARTESIAN_POINT('Ctrl Pts',(0.743862784714884,0.0389979044932149,
-3.45549847971508));
#61025=CARTESIAN_POINT('Ctrl Pts',(0.635434326137781,0.388684828883862,
-3.43969159439698));
#61026=CARTESIAN_POINT('Ctrl Pts',(0.373501805373811,0.644475818337002,
-3.4238847090789));
#61027=CARTESIAN_POINT('Ctrl Pts',(0.0213411650376951,0.744578561142801,
-3.4080778237608));
#61028=CARTESIAN_POINT('Ctrl Pts',(-0.335974934155985,0.664810892402891,
-3.39227093844271));
#61029=CARTESIAN_POINT('Ctrl Pts',(-0.612128409511927,0.424442563024784,
-3.37646405312462));
#61030=CARTESIAN_POINT('Ctrl Pts',(-0.740407913357411,0.0815401795213381,
-3.36065716780653));
#61031=CARTESIAN_POINT('Ctrl Pts',(-0.689824523429956,-0.281060146433609,
-3.34485028248844));
#61032=CARTESIAN_POINT('Ctrl Pts',(-0.472597843728988,-0.575763803257342,
-3.32904339717034));
#61033=CARTESIAN_POINT('Ctrl Pts',(-0.141204072624427,-0.731378211948458,
-3.31323651185225));
#61034=CARTESIAN_POINT('Ctrl Pts',(0.224300853407697,-0.710311062985242,
-3.29742962653416));
#61035=CARTESIAN_POINT('Ctrl Pts',(0.535620648524191,-0.517651620216892,
-3.28162274121607));
#61036=CARTESIAN_POINT('Ctrl Pts',(0.717548715876518,-0.199941289839307,
-3.26581585589798));
#61037=CARTESIAN_POINT('Ctrl Pts',(0.726136064647445,0.166069547650886,
-3.25000897057989));
#61038=CARTESIAN_POINT('Ctrl Pts',(0.559308219371084,0.491962391634354,
-3.23420208526179));
#61039=CARTESIAN_POINT('Ctrl Pts',(0.257366358127407,0.699010183575949,
-3.21839519994371));
#61040=CARTESIAN_POINT('Ctrl Pts',(-0.106748382071239,0.737195674135314,
-3.20258831462561));
#61041=CARTESIAN_POINT('Ctrl Pts',(-0.445075547369097,0.5972942626317,-3.18678142930752));
#61042=CARTESIAN_POINT('Ctrl Pts',(-0.675884277337126,0.313102415652,-3.17097454398943));
#61043=CARTESIAN_POINT('Ctrl Pts',(-0.743417310869164,-0.0467266619684013,
-3.15516765867134));
#61044=CARTESIAN_POINT('Ctrl Pts',(-0.631360460089998,-0.39526781866678,
-3.13936077335324));
#61045=CARTESIAN_POINT('Ctrl Pts',(-0.366783684998515,-0.648322764876845,
-3.12355388803515));
#61046=CARTESIAN_POINT('Ctrl Pts',(-0.0136017098490641,-0.744760144293335,
-3.10774700271706));
#61047=CARTESIAN_POINT('Ctrl Pts',(0.342866077269672,-0.661283246496049,
-3.09194011739897));
#61048=CARTESIAN_POINT('Ctrl Pts',(0.616506523336708,-0.418057873651402,
-3.07613323208088));
#61049=CARTESIAN_POINT('Ctrl Pts',(0.741215361833708,-0.0738408181182466,
-3.06032634676279));
#61050=CARTESIAN_POINT('Ctrl Pts',(0.686866248443941,0.288214218572216,
-3.04451946144469));
#61051=CARTESIAN_POINT('Ctrl Pts',(0.466588485974026,0.580644352245946,
-3.0287125761266));
#61052=CARTESIAN_POINT('Ctrl Pts',(0.133595333383524,0.732806226731728,
-3.01290569080851));
#61053=CARTESIAN_POINT('Ctrl Pts',(-0.231670904748681,0.707941573105843,
-2.99709880549042));
#61054=CARTESIAN_POINT('Ctrl Pts',(-0.540971603238765,0.512057031518881,
-2.98129192017233));
#61055=CARTESIAN_POINT('Ctrl Pts',(-0.719587925375399,0.192473106413799,
-2.96548503485424));
#61056=CARTESIAN_POINT('Ctrl Pts',(-0.724370910057438,-0.173607210971222,
-2.94967814953614));
#61057=CARTESIAN_POINT('Ctrl Pts',(-0.554165115175655,-0.497748635518974,
-2.93387126421806));
#61058=CARTESIAN_POINT('Ctrl Pts',(-0.25008774174892,-0.701647205129168,
-2.91806437889996));
#61059=CARTESIAN_POINT('Ctrl Pts',(0.114404190165603,-0.736046438963738,
-2.90225749358187));
#61060=CARTESIAN_POINT('Ctrl Pts',(0.451259107208176,-0.592636395440179,
-2.88645060826378));
#61061=CARTESIAN_POINT('Ctrl Pts',(0.679101805039518,-0.306061133485969,
-2.87064372294568));
#61062=CARTESIAN_POINT('Ctrl Pts',(0.742891537168478,0.0544503722861812,
-2.85483683762759));
#61063=CARTESIAN_POINT('Ctrl Pts',(0.627218397952841,0.401808113790799,
-2.8390299523095));
#61064=CARTESIAN_POINT('Ctrl Pts',(0.360025946664,0.652099683152305,-2.82322306699141));
#61065=CARTESIAN_POINT('Ctrl Pts',(0.00586078547844685,0.744861282543416,
-2.80741618167332));
#61066=CARTESIAN_POINT('Ctrl Pts',(-0.349720185872753,0.65768417240479,
-2.79160929635523));
#61067=CARTESIAN_POINT('Ctrl Pts',(-0.620818045512782,0.411628027962548,
-2.77580241103713));
#61068=CARTESIAN_POINT('Ctrl Pts',(-0.741942748297485,0.0661334808355267,
-2.75999552571904));
#61069=CARTESIAN_POINT('Ctrl Pts',(-0.683833781938139,-0.295337159393851,
-2.74418864040095));
#61070=CARTESIAN_POINT('Ctrl Pts',(-0.46052872989338,-0.585462183220606,
-2.72838175508286));
#61071=CARTESIAN_POINT('Ctrl Pts',(-0.125972163908432,-0.734155087811067,
-2.71257486976477));
#61072=CARTESIAN_POINT('Ctrl Pts',(0.239015932270905,-0.705495615265834,
-2.69676798444668));
#61073=CARTESIAN_POINT('Ctrl Pts',(0.546264125171852,-0.506407133232618,
-2.68096109912858));
#61074=CARTESIAN_POINT('Ctrl Pts',(0.721549408938659,-0.184984133100431,
-2.66515421381049));
#61075=CARTESIAN_POINT('Ctrl Pts',(0.72252751290008,0.181126122194099,-2.6493473284924));
#61076=CARTESIAN_POINT('Ctrl Pts',(0.548962153108043,0.50348111532969,-2.63354044317431));
#61077=CARTESIAN_POINT('Ctrl Pts',(0.24278211226609,0.704208438604838,-2.61773355785622));
#61078=CARTESIAN_POINT('Ctrl Pts',(-0.12204764094767,0.734817700098301,
-2.60192667253813));
#61079=CARTESIAN_POINT('Ctrl Pts',(-0.457393924516876,0.587914514920067,
-2.58611978722003));
#61080=CARTESIAN_POINT('Ctrl Pts',(-0.682245979894656,0.298986792277233,
-2.57031290190194));
#61081=CARTESIAN_POINT('Ctrl Pts',(-0.742285520404017,-0.0621682011737976,
-2.55450601658385));
#61082=CARTESIAN_POINT('Ctrl Pts',(-0.623008587129114,-0.408305007809151,
-2.53869913126576));
#61083=CARTESIAN_POINT('Ctrl Pts',(-0.353229320304042,-0.65580616520142,
-2.52289224594767));
#61084=CARTESIAN_POINT('Ctrl Pts',(0.00188077194203051,-0.744881964968644,
-2.50708536062958));
#61085=CARTESIAN_POINT('Ctrl Pts',(0.356536519622077,-0.654014058881325,
-2.49127847531148));
#61086=CARTESIAN_POINT('Ctrl Pts',(0.625062510333207,-0.405153720474831,
-2.47547158999339));
#61087=CARTESIAN_POINT('Ctrl Pts',(0.742589994180448,-0.05841900017742,
-2.4596647046753));
#61088=CARTESIAN_POINT('Ctrl Pts',(0.680727451462928,0.302428199517563,
-2.44385781935721));
#61089=CARTESIAN_POINT('Ctrl Pts',(0.454419230028622,0.590216775785679,
-2.42805093403912));
#61090=CARTESIAN_POINT('Ctrl Pts',(0.118335387612053,0.735424649489908,
-2.41224404872103));
#61091=CARTESIAN_POINT('Ctrl Pts',(-0.246335142604835,0.70297345366415,
-2.39643716340293));
#61092=CARTESIAN_POINT('Ctrl Pts',(-0.5514976426543,0.500702535629088,-2.38063027808484));
#61093=CARTESIAN_POINT('Ctrl Pts',(-0.723432954697622,0.177475178816966,
-2.36482339276675));
#61094=CARTESIAN_POINT('Ctrl Pts',(-0.720606072289007,-0.188625469168028,
-2.34901650744866));
#61095=CARTESIAN_POINT('Ctrl Pts',(-0.543699895163633,-0.509159211875521,
-2.33320962213057));
#61096=CARTESIAN_POINT('Ctrl Pts',(-0.235450258792885,-0.706693607352586,
-2.31740273681248));
#61097=CARTESIAN_POINT('Ctrl Pts',(0.129677908813866,-0.733509590260626,
-2.30159585149438));
#61098=CARTESIAN_POINT('Ctrl Pts',(0.463479336645923,-0.583129131102968,
-2.28578896617629));
#61099=CARTESIAN_POINT('Ctrl Pts',(0.68531646228604,-0.291880156157272,
-2.2699820808582));
#61100=CARTESIAN_POINT('Ctrl Pts',(0.741599326034383,0.0698793149937588,
-2.2541751955401));
#61101=CARTESIAN_POINT('Ctrl Pts',(0.618731482339459,0.414757798963037,
-2.23836831022202));
#61102=CARTESIAN_POINT('Ctrl Pts',(0.346394540052889,0.659441810670354,
-2.22256142490392));
#61103=CARTESIAN_POINT('Ctrl Pts',(-0.00962212621185803,0.744822189335018,
-2.20675453958584));
#61104=CARTESIAN_POINT('Ctrl Pts',(-0.363314342254702,0.650273302351158,
-2.19094765426774));
#61105=CARTESIAN_POINT('Ctrl Pts',(-0.6292394593342,0.398635650507393,-2.17514076894965));
#61106=CARTESIAN_POINT('Ctrl Pts',(-0.743157029570654,0.0506982094197591,
-2.15933388363156));
#61107=CARTESIAN_POINT('Ctrl Pts',(-0.677547592547065,-0.309486573008144,
-2.14352699831347));
#61108=CARTESIAN_POINT('Ctrl Pts',(-0.448260646294373,-0.594907616376188,
-2.12772011299537));
#61109=CARTESIAN_POINT('Ctrl Pts',(-0.11068582937702,-0.736614774637171,
-2.11191322767728));
#61110=CARTESIAN_POINT('Ctrl Pts',(0.25362774516957,-0.700375360730835,
-2.09610634235919));
#61111=CARTESIAN_POINT('Ctrl Pts',(0.556671590390294,-0.49494385488759,
-2.0802994570411));
#61112=CARTESIAN_POINT('Ctrl Pts',(0.72523835920202,-0.169947054639404,
-2.06449257172301));
#61113=CARTESIAN_POINT('Ctrl Pts',(0.718606795767678,0.196104441854739,
-2.04868568640491));
#61114=CARTESIAN_POINT('Ctrl Pts',(0.538378909742626,0.514782311839664,
-2.03287880108683));
#61115=CARTESIAN_POINT('Ctrl Pts',(0.228092973275854,0.709102442938133,
-2.01707191576873));
#61116=CARTESIAN_POINT('Ctrl Pts',(-0.137294169584562,0.732122250745553,
-2.00126503045064));
#61117=CARTESIAN_POINT('Ctrl Pts',(-0.469514686282523,0.578280760879758,
-1.98545814513255));
#61118=CARTESIAN_POINT('Ctrl Pts',(-0.688312920557029,0.284741992745893,
-1.96965125981446));
#61119=CARTESIAN_POINT('Ctrl Pts',(-0.740833028178523,-0.077582880833902,
-1.95384437449636));
#61120=CARTESIAN_POINT('Ctrl Pts',(-0.614387545573247,-0.421165790257387,
-1.93803748917828));
#61121=CARTESIAN_POINT('Ctrl Pts',(-0.339522344165966,-0.663006226856653,
-1.92223060386018));
#61122=CARTESIAN_POINT('Ctrl Pts',(0.0173624411524594,-0.744681962099172,
-1.90642371854209));
#61123=CARTESIAN_POINT('Ctrl Pts',(0.370052921667457,-0.646462306870266,
-1.890616833224));
#61124=CARTESIAN_POINT('Ctrl Pts',(0.63334844134467,-0.392074522106352,
-1.87480994790591));
#61125=CARTESIAN_POINT('Ctrl Pts',(0.743643793220054,-0.0429719425199595,
-1.85900306258782));
#61126=CARTESIAN_POINT('Ctrl Pts',(0.674294548661445,0.316511517458853,
-1.84319617726972));
#61127=CARTESIAN_POINT('Ctrl Pts',(0.442053643907026,0.599534198313297,
-1.82738929195163));
#61128=CARTESIAN_POINT('Ctrl Pts',(0.103024315466599,0.737725334702074,
-1.81158240663354));
#61129=CARTESIAN_POINT('Ctrl Pts',(-0.260892952258233,0.697701617097619,
-1.79577552131545));
#61130=CARTESIAN_POINT('Ctrl Pts',(-0.56178540951842,0.489131713029189,
-1.77996863599736));
#61131=CARTESIAN_POINT('Ctrl Pts',(-0.726965427441973,0.162400573714369,
-1.76416175067926));
#61132=CARTESIAN_POINT('Ctrl Pts',(-0.716529899286962,-0.203562232416679,
-1.74835486536118));
#61133=CARTESIAN_POINT('Ctrl Pts',(-0.532999771588644,-0.520349807845742,
-1.73254798004308));
#61134=CARTESIAN_POINT('Ctrl Pts',(-0.220711050408569,-0.711434685172289,
-1.71674109472499));
#61135=CARTESIAN_POINT('Ctrl Pts',(0.144895600593098,-0.730655831405877,
-1.7009342094069));
#61136=CARTESIAN_POINT('Ctrl Pts',(0.475499321521354,-0.57336992794476,
-1.68512732408881));
#61137=CARTESIAN_POINT('Ctrl Pts',(0.691235031046653,-0.277573073068302,
-1.66932043877072));
#61138=CARTESIAN_POINT('Ctrl Pts',(0.739986709607724,0.0852780665973542,
-1.65351355345262));
#61139=CARTESIAN_POINT('Ctrl Pts',(0.609977246038668,0.427528289536178,
-1.63770666813453));
#61140=CARTESIAN_POINT('Ctrl Pts',(0.33261347494014,0.666499028751649,-1.62189978281644));
#61141=CARTESIAN_POINT('Ctrl Pts',(-0.025100880697518,0.744461298407685,
-1.60609289749835));
#61142=CARTESIAN_POINT('Ctrl Pts',(-0.376751529995992,0.642581484081456,
-1.59028601218026));
#61143=CARTESIAN_POINT('Ctrl Pts',(-0.637389012534951,0.385471043968764,
-1.57447912686217));
#61144=CARTESIAN_POINT('Ctrl Pts',(-0.744050232551108,0.0352410340269367,
-1.55867224154407));
#61145=CARTESIAN_POINT('Ctrl Pts',(-0.670968671182005,-0.323502274073774,
-1.54286535622598));
#61146=CARTESIAN_POINT('Ctrl Pts',(-0.435798893312887,-0.604096021859034,
-1.52705847090789));
#61147=CARTESIAN_POINT('Ctrl Pts',(-0.0953516734354473,-0.738756209728018,
-1.5112515855898));
#61148=CARTESIAN_POINT('Ctrl Pts',(0.268129979123054,-0.694952511567602,
-1.49544470027171));
#61149=CARTESIAN_POINT('Ctrl Pts',(0.566838547672013,-0.483266737849533,
-1.47963781495361));
#61150=CARTESIAN_POINT('Ctrl Pts',(0.728613972869053,-0.154836551171296,
-1.46383092963552));
#61151=CARTESIAN_POINT('Ctrl Pts',(0.714375607181817,0.210998035304261,
-1.44802404431743));
#61152=CARTESIAN_POINT('Ctrl Pts',(0.527563061726648,0.525861098523415,
-1.43221715899934));
#61153=CARTESIAN_POINT('Ctrl Pts',(0.213305287545797,0.713690082139056,
-1.41641027368125));
#61154=CARTESIAN_POINT('Ctrl Pts',(-0.152481380774647,0.729110490636162,
-1.40060338836316));
#61155=CARTESIAN_POINT('Ctrl Pts',(-0.481432595934987,0.568397162739177,
-1.38479650304506));
#61156=CARTESIAN_POINT('Ctrl Pts',(-0.694082478124588,0.270374171471832,
-1.36898961772697));
#61157=CARTESIAN_POINT('Ctrl Pts',(-0.739060461736668,-0.0929640410924126,
-1.35318273240888));
#61158=CARTESIAN_POINT('Ctrl Pts',(-0.605501060112058,-0.433844609557178,
-1.33737584709079));
#61159=CARTESIAN_POINT('Ctrl Pts',(-0.325668678633513,-0.669919839082071,
-1.3215689617727));
#61160=CARTESIAN_POINT('Ctrl Pts',(0.0328366089833011,-0.744160222095434,
-1.30576207645461));
#61161=CARTESIAN_POINT('Ctrl Pts',(0.383409443693435,-0.638631253169886,
-1.28995519113651));
#61162=CARTESIAN_POINT('Ctrl Pts',(0.64136073646473,-0.37882592936607,-1.27414830581842));
#61163=CARTESIAN_POINT('Ctrl Pts',(0.744376303662479,-0.0275063189909673,
-1.25834142050033));
#61164=CARTESIAN_POINT('Ctrl Pts',(0.66757031935176,0.330458087749772,-1.24253453518224));
#61165=CARTESIAN_POINT('Ctrl Pts',(0.429497070115765,0.608592594270275,
-1.22672764986415));
#61166=CARTESIAN_POINT('Ctrl Pts',(0.0876687320402154,0.739707288365545,
-1.21092076454605));
#61167=CARTESIAN_POINT('Ctrl Pts',(-0.27533804406014,0.692128341084069,
-1.19511387922797));
#61168=CARTESIAN_POINT('Ctrl Pts',(-0.571830459038853,0.477349562851023,
-1.17930699390987));
#61169=CARTESIAN_POINT('Ctrl Pts',(-0.73018381741644,0.147255804034344,
-1.16350010859178));
#61170=CARTESIAN_POINT('Ctrl Pts',(-0.712144152147036,-0.218411047342909,
-1.14769322327369));
#61171=CARTESIAN_POINT('Ctrl Pts',(-0.522069367400179,-0.531315588573331,
-1.1318863379556));
#61172=CARTESIAN_POINT('Ctrl Pts',(-0.205876484617368,-0.715868390222842,
-1.11607945263751));
#61173=CARTESIAN_POINT('Ctrl Pts',(0.160050690754894,-0.72748639535563,
-1.10027256731941));
#61174=CARTESIAN_POINT('Ctrl Pts',(0.487313868643706,-0.563363002393797,
-1.08446568200132));
#61175=CARTESIAN_POINT('Ctrl Pts',(0.696854954225239,-0.263146065542292,
-1.06865879668323));
#61176=CARTESIAN_POINT('Ctrl Pts',(0.738054384613563,0.10063997412232,-1.05285191136514));
#61177=CARTESIAN_POINT('Ctrl Pts',(0.600959471286436,0.440114068066193,
-1.03704502604705));
#61178=CARTESIAN_POINT('Ctrl Pts',(0.318688705384841,0.673268288350774,
-1.02123814072895));
#61179=CARTESIAN_POINT('Ctrl Pts',(-0.0405687904389292,0.743778765683029,
-1.00543125541086));
#61180=CARTESIAN_POINT('Ctrl Pts',(-0.39002594360851,0.634612040817805,
-0.989624370092771));
#61181=CARTESIAN_POINT('Ctrl Pts',(-0.645263184130204,0.372139896067054,
-0.973817484774681));
#61182=CARTESIAN_POINT('Ctrl Pts',(-0.744621971333751,0.0197686328734897,
-0.958010599456587));
#61183=CARTESIAN_POINT('Ctrl Pts',(-0.664099860242016,-0.337378207158056,
-0.942203714138499));
#61184=CARTESIAN_POINT('Ctrl Pts',(-0.423148855003988,-0.61302342985196,
-0.926396828820403));
#61185=CARTESIAN_POINT('Ctrl Pts',(-0.0799763211500396,-0.740578467884366,
-0.910589943502316));
#61186=CARTESIAN_POINT('Ctrl Pts',(0.282516368493905,-0.6892294106984,-0.89478305818422));
#61187=CARTESIAN_POINT('Ctrl Pts',(0.576760604420077,-0.471380827174412,
-0.878976172866131));
#61188=CARTESIAN_POINT('Ctrl Pts',(0.731674791518147,-0.139659151134197,
-0.863169287548039));
#61189=CARTESIAN_POINT('Ctrl Pts',(0.709835775212143,0.22580046781976,-0.847362402229946));
#61190=CARTESIAN_POINT('Ctrl Pts',(0.516519282007925,0.536712688831433,
-0.831555516911855));
#61191=CARTESIAN_POINT('Ctrl Pts',(0.198425444041774,0.717969374134769,
-0.815748631593762));
#61192=CARTESIAN_POINT('Ctrl Pts',(-0.167602712938549,0.725783720990135,
-0.799941746275672));
#61193=CARTESIAN_POINT('Ctrl Pts',(-0.493142504384733,0.55826799067097,
-0.784134860957579));
#61194=CARTESIAN_POINT('Ctrl Pts',(-0.699552159880962,0.255889536019993,
-0.768327975639488));
#61195=CARTESIAN_POINT('Ctrl Pts',(-0.736968586909338,-0.108305036574953,
-0.752521090321397));
#61196=CARTESIAN_POINT('Ctrl Pts',(-0.596352970119284,-0.446335987870746,
-0.736714205003304));
#61197=CARTESIAN_POINT('Ctrl Pts',(-0.311674309132495,-0.67654401487666,
-0.720907319685214));
#61198=CARTESIAN_POINT('Ctrl Pts',(0.0482965898766236,-0.743316970373296,
-0.705100434367121));
#61199=CARTESIAN_POINT('Ctrl Pts',(0.396600315063237,-0.630524281158457,
-0.689293549049029));
#61200=CARTESIAN_POINT('Ctrl Pts',(0.649095934010409,-0.365413666260311,
-0.673486663730938));
#61201=CARTESIAN_POINT('Ctrl Pts',(0.744787209029253,-0.0120288114568608,
-0.657679778412846));
#61202=CARTESIAN_POINT('Ctrl Pts',(0.660557668712699,0.344261884825333,
-0.641872893094754));
#61203=CARTESIAN_POINT('Ctrl Pts',(0.416754933676891,0.617388050009569,
-0.626066007776663));
#61204=CARTESIAN_POINT('Ctrl Pts',(0.0722752716568935,0.74136965418445,
-0.61025912245857));
#61205=CARTESIAN_POINT('Ctrl Pts',(-0.289664177061162,0.686256033537139,
-0.59445223714048));
#61206=CARTESIAN_POINT('Ctrl Pts',(-0.581628451288467,0.465361175529743,
-0.578645351822388));
#61207=CARTESIAN_POINT('Ctrl Pts',(-0.733086734127339,0.132047413019573,
-0.562838466504297));
#61208=CARTESIAN_POINT('Ctrl Pts',(-0.707450725715331,-0.233165498570212,
-0.547031581186204));
#61209=CARTESIAN_POINT('Ctrl Pts',(-0.510913405039632,-0.542051816332592,
-0.531224695868112));
#61210=CARTESIAN_POINT('Ctrl Pts',(-0.190952970639487,-0.719992806938097,
-0.515417810550021));
#61211=CARTESIAN_POINT('Ctrl Pts',(0.17513663159763,-0.724002651453208,
-0.499610925231929));
#61212=CARTESIAN_POINT('Ctrl Pts',(0.498917873580885,-0.553112677905884,
-0.483804039913837));
#61213=CARTESIAN_POINT('Ctrl Pts',(0.702173803754348,-0.248605366715384,
-0.467997154595746));
#61214=CARTESIAN_POINT('Ctrl Pts',(0.735803185906037,0.115958400512358,
-0.452190269277653));
#61215=CARTESIAN_POINT('Ctrl Pts',(0.591682054179269,0.45250969691326,-0.436383383959563));
#61216=CARTESIAN_POINT('Ctrl Pts',(0.304626247533592,0.679746664833693,
-0.42057649864147));
#61217=CARTESIAN_POINT('Ctrl Pts',(-0.0560191725830189,0.742774886046918,
-0.40476961332338));
#61218=CARTESIAN_POINT('Ctrl Pts',(-0.403131847927991,0.626368415729021,
-0.388962728005286));
#61219=CARTESIAN_POINT('Ctrl Pts',(-0.652858572116915,0.358647966476576,
-0.373155842687196));
#61220=CARTESIAN_POINT('Ctrl Pts',(-0.744871998892771,0.00428769075343641,
-0.357348957369103));
#61221=CARTESIAN_POINT('Ctrl Pts',(-0.656944127387824,-0.351108377213285,
-0.341542072051012));
#61222=CARTESIAN_POINT('Ctrl Pts',(-0.410315996739561,-0.621685983303274,
-0.32573518673292));
#61223=CARTESIAN_POINT('Ctrl Pts',(-0.0645664154468477,-0.742080761801361,
-0.309928301414828));
#61224=CARTESIAN_POINT('Ctrl Pts',(0.296780697814228,-0.683208530777618,
-0.294121416096737));
#61225=CARTESIAN_POINT('Ctrl Pts',(0.586433473612455,-0.45929125810821,
-0.278314530778645));
#61226=CARTESIAN_POINT('Ctrl Pts',(0.734419493190546,-0.124421411904842,
-0.262507645460554));
#61227=CARTESIAN_POINT('Ctrl Pts',(0.704989260382789,0.240505344134964,
-0.246700760142461));
#61228=CARTESIAN_POINT('Ctrl Pts',(0.505252343759996,0.547332394234904,
-0.230893874824371));
#61229=CARTESIAN_POINT('Ctrl Pts',(0.183459868124781,0.721938470344044,
-0.215086989506278));
#61230=CARTESIAN_POINT('Ctrl Pts',(-0.182651626265875,0.72214337859536,
-0.199280104188187));
#61231=CARTESIAN_POINT('Ctrl Pts',(-0.504639365504918,0.547897621985701,
-0.183473218870095));
#61232=CARTESIAN_POINT('Ctrl Pts',(-0.704719577046485,0.241294342392419,
-0.167666333552003));
#61233=CARTESIAN_POINT('Ctrl Pts',(-0.734558357616299,-0.123599235284501,
-0.151859448233911));
#61234=CARTESIAN_POINT('Ctrl Pts',(-0.586947129908281,-0.458634536122048,
-0.13605256291582));
#61235=CARTESIAN_POINT('Ctrl Pts',(-0.297545473785419,-0.682875877070518,
-0.120245677597728));
#61236=CARTESIAN_POINT('Ctrl Pts',(0.0637360798710123,-0.742152601032517,
-0.104438792279637));
#61237=CARTESIAN_POINT('Ctrl Pts',(0.409619102099937,-0.622144835166141,
-0.0886319069615454));
#61238=CARTESIAN_POINT('Ctrl Pts',(0.656552129312043,-0.351843641497199,
-0.0728250216434533));
#61239=CARTESIAN_POINT('Ctrl Pts',(0.744873519473169,0.00345411617399305,
-0.0570181363253616));
#61240=CARTESIAN_POINT('Ctrl Pts',(0.653265131348944,0.357916507544478,
-0.0412112510072698));
#61241=CARTESIAN_POINT('Ctrl Pts',(0.403821942874752,0.625917629361813,
-0.0254043656891785));
#61242=CARTESIAN_POINT('Ctrl Pts',(0.0568719964643233,0.742709933615296,
-0.00959748037108637));
#61243=CARTESIAN_POINT('Ctrl Pts',(-0.303910141472772,0.680091682441782,
0.00620940494700605));
#61244=CARTESIAN_POINT('Ctrl Pts',(-0.495338330062706,0.528798303103765,
0.0167473284924));
#61245=CARTESIAN_POINT('Ctrl Pts',(-0.567325265044095,0.434889340047662,
0.0220162902650971));
#61246=CARTESIAN_POINT('Ctrl Pts',(-0.325579286442179,0.678938089483064,
-3.9709162902651));
#61247=CARTESIAN_POINT('Ctrl Pts',(-0.437963443981315,0.625045172903798,
-3.9656473284924));
#61248=CARTESIAN_POINT('Ctrl Pts',(-0.635345959215123,0.460437084581636,
-3.95510940494701));
#61249=CARTESIAN_POINT('Ctrl Pts',(-0.777954672189442,0.102059017460474,
-3.93930251962892));
#61250=CARTESIAN_POINT('Ctrl Pts',(-0.732618684251679,-0.280875658539082,
-3.92349563431082));
#61251=CARTESIAN_POINT('Ctrl Pts',(-0.510307552433891,-0.596006360849397,
-3.90768874899273));
#61252=CARTESIAN_POINT('Ctrl Pts',(-0.164716539319843,-0.767133340665321,
-3.89188186367464));
#61253=CARTESIAN_POINT('Ctrl Pts',(0.220664017227322,-0.752953731708629,
-3.87607497835654));
#61254=CARTESIAN_POINT('Ctrl Pts',(0.552738823443294,-0.556874126203156,
-3.86026809303846));
#61255=CARTESIAN_POINT('Ctrl Pts',(0.751286187467129,-0.22627177068859,
-3.84446120772036));
#61256=CARTESIAN_POINT('Ctrl Pts',(0.768342969090818,0.158993500009593,
-3.82865432240228));
#61257=CARTESIAN_POINT('Ctrl Pts',(0.599788380000657,0.505849312469457,
-3.81284743708418));
#61258=CARTESIAN_POINT('Ctrl Pts',(0.286340898691607,0.730505795947052,
-3.79704055176609));
#61259=CARTESIAN_POINT('Ctrl Pts',(-0.0962789698052883,0.778691252270154,
-3.781233666448));
#61260=CARTESIAN_POINT('Ctrl Pts',(-0.455640380862832,0.638765690064438,
-3.76542678112991));
#61261=CARTESIAN_POINT('Ctrl Pts',(-0.704931180768228,0.344531238590307,
-3.74961989581181));
#61262=CARTESIAN_POINT('Ctrl Pts',(-0.783929319766703,-0.0329327830524558,
-3.73381301049372));
#61263=CARTESIAN_POINT('Ctrl Pts',(-0.673550950658744,-0.402441133840107,
-3.71800612517563));
#61264=CARTESIAN_POINT('Ctrl Pts',(-0.400460553894944,-0.674730383902638,
-3.70219923985754));
#61265=CARTESIAN_POINT('Ctrl Pts',(-0.0306295201890803,-0.784022691505241,
-3.68639235453945));
#61266=CARTESIAN_POINT('Ctrl Pts',(0.346600792629627,-0.703915930899028,
-3.67058546922136));
#61267=CARTESIAN_POINT('Ctrl Pts',(0.640101556190887,-0.453761771640795,
-3.65477858390327));
#61268=CARTESIAN_POINT('Ctrl Pts',(0.778970778768956,-0.093990815362487,
-3.63897169858517));
#61269=CARTESIAN_POINT('Ctrl Pts',(0.729661343113795,0.288485826147569,
-3.62316481326708));
#61270=CARTESIAN_POINT('Ctrl Pts',(0.50408509974901,0.601271951600041,-3.60735792794899));
#61271=CARTESIAN_POINT('Ctrl Pts',(0.156735279915013,0.768806737460164,
-3.59155104263089));
#61272=CARTESIAN_POINT('Ctrl Pts',(-0.22847762216423,0.750618227679105,
-3.57574415731281));
#61273=CARTESIAN_POINT('Ctrl Pts',(-0.55849639689333,0.551100283254033,
-3.55993727199471));
#61274=CARTESIAN_POINT('Ctrl Pts',(-0.753597270410352,0.218451142313315,
-3.54413038667662));
#61275=CARTESIAN_POINT('Ctrl Pts',(-0.766649051673194,-0.166969994659364,
-3.52832350135853));
#61276=CARTESIAN_POINT('Ctrl Pts',(-0.594498776857272,-0.512055614032796,
-3.51251661604044));
#61277=CARTESIAN_POINT('Ctrl Pts',(-0.278733381707383,-0.733442192316373,
-3.49670973072235));
#61278=CARTESIAN_POINT('Ctrl Pts',(0.104366597992381,-0.777648610087503,
-3.48090284540425));
#61279=CARTESIAN_POINT('Ctrl Pts',(0.462254378587548,-0.633995770509813,
-3.46509596008616));
#61280=CARTESIAN_POINT('Ctrl Pts',(0.708473774334626,-0.337186385590646,
-3.44928907476807));
#61281=CARTESIAN_POINT('Ctrl Pts',(0.78354471643388,0.0410782776683208,
-3.43348218944998));
#61282=CARTESIAN_POINT('Ctrl Pts',(0.66933205843443,0.40941951968559,-3.41767530413189));
#61283=CARTESIAN_POINT('Ctrl Pts',(0.393426546122131,0.678855875981091,
-3.4018684188138));
#61284=CARTESIAN_POINT('Ctrl Pts',(0.0224796258818643,0.784298676505233,
-3.3860615334957));
#61285=CARTESIAN_POINT('Ctrl Pts',(-0.353897775129376,0.700275740195334,
-3.37025464817762));
#61286=CARTESIAN_POINT('Ctrl Pts',(-0.644782869781527,0.447084777624944,
-3.35444776285952));
#61287=CARTESIAN_POINT('Ctrl Pts',(-0.779905542309655,0.08589000304069,
-3.33864087754143));
#61288=CARTESIAN_POINT('Ctrl Pts',(-0.726623742586119,-0.296053515867974,
-3.32283399222334));
#61289=CARTESIAN_POINT('Ctrl Pts',(-0.497808938773334,-0.606478365669389,
-3.30702710690525));
#61290=CARTESIAN_POINT('Ctrl Pts',(-0.148736712357813,-0.770394144542023,
-3.29122022158715));
#61291=CARTESIAN_POINT('Ctrl Pts',(0.23626635475059,-0.748203152332651,
-3.27541333626906));
#61292=CARTESIAN_POINT('Ctrl Pts',(0.564193743507245,-0.545266143580295,
-3.25960645095097));
#61293=CARTESIAN_POINT('Ctrl Pts',(0.755826903377695,-0.210607311549555,
-3.24379956563288));
#61294=CARTESIAN_POINT('Ctrl Pts',(0.764872350865989,0.17492865525231,-3.22799268031479));
#61295=CARTESIAN_POINT('Ctrl Pts',(0.589144946018815,0.518206503363411,
-3.2121857949967));
#61296=CARTESIAN_POINT('Ctrl Pts',(0.271095764221967,0.736299418829429,
-3.19637890967861));
#61297=CARTESIAN_POINT('Ctrl Pts',(-0.112442956521666,0.776521943718472,
-3.18057202436051));
#61298=CARTESIAN_POINT('Ctrl Pts',(-0.468818444370271,0.629157383939731,
-3.16476513904242));
#61299=CARTESIAN_POINT('Ctrl Pts',(-0.711939843355949,0.32980510455412,
-3.14895825372433));
#61300=CARTESIAN_POINT('Ctrl Pts',(-0.783075478443625,-0.0492193316485955,
-3.13315136840624));
#61301=CARTESIAN_POINT('Ctrl Pts',(-0.665040868872605,-0.416353684115822,
-3.11734448308815));
#61302=CARTESIAN_POINT('Ctrl Pts',(-0.386350042454257,-0.682908040839498,
-3.10153759777006));
#61303=CARTESIAN_POINT('Ctrl Pts',(-0.0143273035104027,-0.784489946348433,
-3.08573071245196));
#61304=CARTESIAN_POINT('Ctrl Pts',(0.361156531566544,-0.696559909307498,
-3.06992382713387));
#61305=CARTESIAN_POINT('Ctrl Pts',(0.649394537451754,-0.440359492091936,
-3.05411694181578));
#61306=CARTESIAN_POINT('Ctrl Pts',(0.780756064745238,-0.0777799132885599,
-3.03831005649769));
#61307=CARTESIAN_POINT('Ctrl Pts',(0.723507656148297,0.303589227480892,
-3.0225031711796));
#61308=CARTESIAN_POINT('Ctrl Pts',(0.491479007212279,0.611619271293245,
-3.0066962858615));
#61309=CARTESIAN_POINT('Ctrl Pts',(0.140722079076732,0.771898337870972,
-2.99088940054342));
#61310=CARTESIAN_POINT('Ctrl Pts',(-0.244029567142358,0.745707260195287,
-2.97508251522532));
#61311=CARTESIAN_POINT('Ctrl Pts',(-0.569830149011909,0.539373107250178,
-2.95927562990723));
#61312=CARTESIAN_POINT('Ctrl Pts',(-0.757974896073903,0.202740732141823,
-2.94346874458914));
#61313=CARTESIAN_POINT('Ctrl Pts',(-0.763013032748309,-0.182868421013236,
-2.92766185927105));
#61314=CARTESIAN_POINT('Ctrl Pts',(-0.583727478978919,-0.524301418873305,
-2.91185497395296));
#61315=CARTESIAN_POINT('Ctrl Pts',(-0.263428864461014,-0.73907711432328,
-2.89604808863486));
#61316=CARTESIAN_POINT('Ctrl Pts',(0.120507169580355,-0.775311401713775,
-2.88024120331677));
#61317=CARTESIAN_POINT('Ctrl Pts',(0.475331870959451,-0.624251039244497,
-2.86443431799868));
#61318=CARTESIAN_POINT('Ctrl Pts',(0.715329012545471,-0.322388199781518,
-2.84862743268059));
#61319=CARTESIAN_POINT('Ctrl Pts',(0.782521656940954,0.0573550692269745,
-2.83282054736249));
#61320=CARTESIAN_POINT('Ctrl Pts',(0.660677845248626,0.423242876307776,
-2.81701366204441));
#61321=CARTESIAN_POINT('Ctrl Pts',(0.379231807376692,0.686886441721958,
-2.80120677672631));
#61322=CARTESIAN_POINT('Ctrl Pts',(0.00617343358231456,0.784596479896164,
-2.78539989140822));
#61323=CARTESIAN_POINT('Ctrl Pts',(-0.368376277858687,0.692768839843872,
-2.76959300609013));
#61324=CARTESIAN_POINT('Ctrl Pts',(-0.653936061090613,0.433586641345119,
-2.75378612077204));
#61325=CARTESIAN_POINT('Ctrl Pts',(-0.781522254198735,0.0696614221773742,
-2.73797923545394));
#61326=CARTESIAN_POINT('Ctrl Pts',(-0.720313420387067,-0.311092147052815,
-2.72217235013585));
#61327=CARTESIAN_POINT('Ctrl Pts',(-0.485095988788138,-0.616694113162519,
-2.70636546481776));
#61328=CARTESIAN_POINT('Ctrl Pts',(-0.132692245769534,-0.773319154980843,
-2.69055857949967));
#61329=CARTESIAN_POINT('Ctrl Pts',(0.251766420800531,-0.74313082085521,
-2.67475169418158));
#61330=CARTESIAN_POINT('Ctrl Pts',(0.575405004593468,-0.533421810799332,
-2.65894480886349));
#61331=CARTESIAN_POINT('Ctrl Pts',(0.760041016484745,-0.194852253793691,
-2.6431379235454));
#61332=CARTESIAN_POINT('Ctrl Pts',(0.761071298153412,0.190788434331659,
-2.6273310382273));
#61333=CARTESIAN_POINT('Ctrl Pts',(0.578246960902665,0.530339702223469,
-2.61152415290921));
#61334=CARTESIAN_POINT('Ctrl Pts',(0.255733510560913,0.741774978766363,
-2.59571726759112));
#61335=CARTESIAN_POINT('Ctrl Pts',(-0.12855836611643,0.774017114829589,
-2.57991038227303));
#61336=CARTESIAN_POINT('Ctrl Pts',(-0.481793954810521,0.619277266380483,
-2.56410349695494));
#61337=CARTESIAN_POINT('Ctrl Pts',(-0.718640915823752,0.314936472406177,
-2.54829661163684));
#61338=CARTESIAN_POINT('Ctrl Pts',(-0.781883311746624,-0.0654846116257782,
-2.53248972631876));
#61339=CARTESIAN_POINT('Ctrl Pts',(-0.656243458832344,-0.430086352128742,
-2.51668284100066));
#61340=CARTESIAN_POINT('Ctrl Pts',(-0.372072609762093,-0.690790648903465,
-2.50087595568257));
#61341=CARTESIAN_POINT('Ctrl Pts',(0.00198110316616631,-0.784618265641255,
-2.48506907036448));
#61342=CARTESIAN_POINT('Ctrl Pts',(0.375556234168478,-0.688902941294953,
-2.46926218504639));
#61343=CARTESIAN_POINT('Ctrl Pts',(0.658406950147669,-0.42676695695062,
-2.45345529972829));
#61344=CARTESIAN_POINT('Ctrl Pts',(0.782204027910568,-0.0615354066219549,
-2.4376484144102));
#61345=CARTESIAN_POINT('Ctrl Pts',(0.717041380326235,0.318561464159578,
-2.42184152909211));
#61346=CARTESIAN_POINT('Ctrl Pts',(0.478660572959506,0.621702343120665,
-2.40603464377402));
#61347=CARTESIAN_POINT('Ctrl Pts',(0.124648079774715,0.774656442402774,
-2.39022775845593));
#61348=CARTESIAN_POINT('Ctrl Pts',(-0.259476080032666,0.740474112605248,
-2.37442087313784));
#61349=CARTESIAN_POINT('Ctrl Pts',(-0.580917708086637,0.527412897054116,
-2.35861398781974));
#61350=CARTESIAN_POINT('Ctrl Pts',(-0.762025041439243,0.186942728575264,
-2.34280710250165));
#61351=CARTESIAN_POINT('Ctrl Pts',(-0.759047356816805,-0.198687839731243,
-2.32700021718356));
#61352=CARTESIAN_POINT('Ctrl Pts',(-0.572703983765511,-0.536320701191704,
-2.31119333186547));
#61353=CARTESIAN_POINT('Ctrl Pts',(-0.248010533731526,-0.744392720750176,
-2.29538644654738));
#61354=CARTESIAN_POINT('Ctrl Pts',(0.136595676483858,-0.772639222867675,
-2.27957956122929));
#61355=CARTESIAN_POINT('Ctrl Pts',(0.488203997924677,-0.614236602587317,
-2.26377267591119));
#61356=CARTESIAN_POINT('Ctrl Pts',(0.721875195457185,-0.307450727322765,
-2.2479657905931));
#61357=CARTESIAN_POINT('Ctrl Pts',(0.781160511811177,0.0736070807364849,
-2.23215890527501));
#61358=CARTESIAN_POINT('Ctrl Pts',(0.651738188601823,0.436883372384051,
-2.21635201995692));
#61359=CARTESIAN_POINT('Ctrl Pts',(0.36487322290766,0.694620240673004,-2.20054513463883));
#61360=CARTESIAN_POINT('Ctrl Pts',(-0.0101354259267691,0.784555301230531,
-2.18473824932074));
#61361=CARTESIAN_POINT('Ctrl Pts',(-0.382695624956466,0.68496263123387,
-2.16893136400264));
#61362=CARTESIAN_POINT('Ctrl Pts',(-0.662806721702037,0.419901175533298,
-2.15312447868456));
#61363=CARTESIAN_POINT('Ctrl Pts',(-0.782801312239287,0.0534027443498731,
-2.13731759336646));
#61364=CARTESIAN_POINT('Ctrl Pts',(-0.713691889393596,-0.325996372006569,
-2.12151070804837));
#61365=CARTESIAN_POINT('Ctrl Pts',(-0.472173454844658,-0.626643420206186,
-2.10570382273027));
#61366=CARTESIAN_POINT('Ctrl Pts',(-0.116590449978903,-0.775910055690326,
-2.08989693741219));
#61367=CARTESIAN_POINT('Ctrl Pts',(0.267157712083718,-0.737737422408434,
-2.07409005209409));
#61368=CARTESIAN_POINT('Ctrl Pts',(0.586367664039463,-0.521347015064389,
-2.058283166776));
#61369=CARTESIAN_POINT('Ctrl Pts',(0.76392675663392,-0.179013010830011,
-2.04247628145791));
#61370=CARTESIAN_POINT('Ctrl Pts',(0.756941427353513,0.206565783961604,
-2.02666939613982));
#61371=CARTESIAN_POINT('Ctrl Pts',(0.567099146289403,0.542243769743349,
-2.01086251082173));
#61372=CARTESIAN_POINT('Ctrl Pts',(0.240260768166395,0.746930057520609,
-1.99505562550364));
#61373=CARTESIAN_POINT('Ctrl Pts',(-0.144618232536515,0.771177874660354,
-1.97924874018554));
#61374=CARTESIAN_POINT('Ctrl Pts',(-0.494561307924264,0.609129592329817,
-1.96344185486745));
#61375=CARTESIAN_POINT('Ctrl Pts',(-0.725031502096651,0.299931773100352,
-1.94763496954936));
#61376=CARTESIAN_POINT('Ctrl Pts',(-0.780353335207492,-0.0817215992145918,
-1.93182808423127));
#61377=CARTESIAN_POINT('Ctrl Pts',(-0.647162521191612,-0.443633202896902,
-1.91602119891318));
#61378=CARTESIAN_POINT('Ctrl Pts',(-0.357634424451625,-0.698374803379104,
-1.90021431359509));
#61379=CARTESIAN_POINT('Ctrl Pts',(0.0182886539143304,-0.78440759346506,
-1.88440742827699));
#61380=CARTESIAN_POINT('Ctrl Pts',(0.389793679064869,-0.680948335271274,
-1.8686005429589));
#61381=CARTESIAN_POINT('Ctrl Pts',(0.667134900514558,-0.412990038697154,
-1.85279365764081));
#61382=CARTESIAN_POINT('Ctrl Pts',(0.783314042669518,-0.0452643138066422,
-1.83698677232272));
#61383=CARTESIAN_POINT('Ctrl Pts',(0.710265309382765,0.333396067515875,
-1.82117988700462));
#61384=CARTESIAN_POINT('Ctrl Pts',(0.465635335146463,0.631516810711076,
-1.80537300168654));
#61385=CARTESIAN_POINT('Ctrl Pts',(0.108520226723017,0.777079859435072,
-1.78956611636844));
#61386=CARTESIAN_POINT('Ctrl Pts',(-0.274810487225979,0.734921045867015,
-1.77375923105035));
#61387=CARTESIAN_POINT('Ctrl Pts',(-0.591754283777642,0.515224820033407,
-1.75795234573226));
#61388=CARTESIAN_POINT('Ctrl Pts',(-0.765745956655943,0.171063957082489,
-1.74214546041417));
#61389=CARTESIAN_POINT('Ctrl Pts',(-0.75475373723447,-0.214421416090478,
-1.72633857509608));
#61390=CARTESIAN_POINT('Ctrl Pts',(-0.561433053878104,-0.548108268101068,
-1.71053168977799));
#61391=CARTESIAN_POINT('Ctrl Pts',(-0.232485050952634,-0.749386715008478,
-1.69472480445989));
#61392=CARTESIAN_POINT('Ctrl Pts',(0.152625167721958,-0.769633228054435,
-1.6789179191418));
#61393=CARTESIAN_POINT('Ctrl Pts',(0.500865198127574,-0.603956787239182,
-1.66311103382371));
#61394=CARTESIAN_POINT('Ctrl Pts',(0.728109494815239,-0.292380421895079,
-1.64730414850562));
#61395=CARTESIAN_POINT('Ctrl Pts',(0.779461869122354,0.0898272905743789,
-1.63149726318753));
#61396=CARTESIAN_POINT('Ctrl Pts',(0.642516950840174,0.450335114587673,
-1.61569037786943));
#61397=CARTESIAN_POINT('Ctrl Pts',(0.350356996289247,0.702053931474515,
-1.59988349255134));
#61398=CARTESIAN_POINT('Ctrl Pts',(-0.0264399064619325,0.784175158299426,
-1.58407660723325));
#61399=CARTESIAN_POINT('Ctrl Pts',(-0.396849629800857,0.676860487009376,
-1.56826972191516));
#61400=CARTESIAN_POINT('Ctrl Pts',(-0.671391019079131,0.406034292945231,
-1.55246283659707));
#61401=CARTESIAN_POINT('Ctrl Pts',(-0.783742163818932,0.037120994060833,
-1.53665595127897));
#61402=CARTESIAN_POINT('Ctrl Pts',(-0.706762010414098,-0.340759751413029,
-1.52084906596088));
#61403=CARTESIAN_POINT('Ctrl Pts',(-0.459046920076702,-0.636321988238455,
-1.50504218064279));
#61404=CARTESIAN_POINT('Ctrl Pts',(-0.100438281708249,-0.778165727281241,
-1.4892352953247));
#61405=CARTESIAN_POINT('Ctrl Pts',(0.28243357884871,-0.732025287190515,
-1.47342841000661));
#61406=CARTESIAN_POINT('Ctrl Pts',(0.597076985468083,-0.509046973247059,
-1.45762152468852));
#61407=CARTESIAN_POINT('Ctrl Pts',(0.767482445005317,-0.163096425945838,
-1.44181463937043));
#61408=CARTESIAN_POINT('Ctrl Pts',(0.752484522761953,0.22225388759561,-1.42600775405233));
#61409=CARTESIAN_POINT('Ctrl Pts',(0.555706318551799,0.55391356281396,-1.41020086873424));
#61410=CARTESIAN_POINT('Ctrl Pts',(0.224684221980512,0.751762427859133,
-1.39439398341615));
#61411=CARTESIAN_POINT('Ctrl Pts',(-0.160615617175025,0.768005449894162,
-1.37858709809806));
#61412=CARTESIAN_POINT('Ctrl Pts',(-0.507114987623006,0.598718746053408,
-1.36278021277997));
#61413=CARTESIAN_POINT('Ctrl Pts',(-0.731108841145082,0.284797489362429,
-1.34697332746188));
#61414=CARTESIAN_POINT('Ctrl Pts',(-0.778486209847032,-0.0979232792835823,
-1.33116644214378));
#61415=CARTESIAN_POINT('Ctrl Pts',(-0.637801979336504,-0.456988383552671,
-1.31535955682569));
#61416=CARTESIAN_POINT('Ctrl Pts',(-0.343041724488343,-0.705657227560031,
-1.2995526715076));
#61417=CARTESIAN_POINT('Ctrl Pts',(0.0345883031160503,-0.783858020839999,
-1.28374578618951));
#61418=CARTESIAN_POINT('Ctrl Pts',(0.403862715019395,-0.672699527995084,
-1.26793890087142));
#61419=CARTESIAN_POINT('Ctrl Pts',(0.675574617673198,-0.399034689598986,
-1.25213201555332));
#61420=CARTESIAN_POINT('Ctrl Pts',(0.784085629444241,-0.0289736647091182,
-1.23632513023523));
#61421=CARTESIAN_POINT('Ctrl Pts',(0.703182370894705,0.348086628313337,
-1.22051824491714));
#61422=CARTESIAN_POINT('Ctrl Pts',(0.452408921279789,0.64105843375944,-1.20471135959905));
#61423=CARTESIAN_POINT('Ctrl Pts',(0.0923454879019127,0.779167541939348,
-1.18890447428096));
#61424=CARTESIAN_POINT('Ctrl Pts',(-0.290026163547421,0.729050459162884,
-1.17309758896287));
#61425=CARTESIAN_POINT('Ctrl Pts',(-0.602335194181794,0.502814142002418,
-1.15729070364477));
#61426=CARTESIAN_POINT('Ctrl Pts',(-0.769136034116109,0.155111278028998,
-1.14148381832668));
#61427=CARTESIAN_POINT('Ctrl Pts',(-0.750134029044039,-0.230062352456464,
-1.12567693300859));
#61428=CARTESIAN_POINT('Ctrl Pts',(-0.549919558880984,-0.559659026825969,
-1.1098700476905));
#61429=CARTESIAN_POINT('Ctrl Pts',(-0.21685912385273,-0.754056939461121,
-1.09406316237241));
#61430=CARTESIAN_POINT('Ctrl Pts',(0.168588717811249,-0.766294716003188,
-1.07825627705431));
#61431=CARTESIAN_POINT('Ctrl Pts',(0.513310001342625,-0.593416034556938,
-1.06244939173622));
#61432=CARTESIAN_POINT('Ctrl Pts',(0.734029217113261,-0.277183794569127,
-1.04664250641813));
#61433=CARTESIAN_POINT('Ctrl Pts',(0.777426462766882,0.106008690857963,
-1.03083562110004));
#61434=CARTESIAN_POINT('Ctrl Pts',(0.63301811596593,0.463592291142325,-1.01502873578195));
#61435=CARTESIAN_POINT('Ctrl Pts',(0.335689399204394,0.709184302427401,
-0.999221850463857));
#61436=CARTESIAN_POINT('Ctrl Pts',(-0.0427329637316332,0.783456215342222,
-0.983414965145766));
#61437=CARTESIAN_POINT('Ctrl Pts',(-0.410832177205529,0.668465907672345,
-0.967608079827673));
#61438=CARTESIAN_POINT('Ctrl Pts',(-0.679685244407421,0.391991984717126,
-0.951801194509583));
#61439=CARTESIAN_POINT('Ctrl Pts',(-0.784344402446169,0.02082320578127,
-0.935994309191489));
#61440=CARTESIAN_POINT('Ctrl Pts',(-0.69952677747759,-0.355375906807799,
-0.920187423873401));
#61441=CARTESIAN_POINT('Ctrl Pts',(-0.445722055755895,-0.645725635669195,
-0.904380538555305));
#61442=CARTESIAN_POINT('Ctrl Pts',(-0.0842427194431486,-0.780085195198877,
-0.888573653237217));
#61443=CARTESIAN_POINT('Ctrl Pts',(0.297587421212811,-0.725996883108706,
-0.872766767919122));
#61444=CARTESIAN_POINT('Ctrl Pts',(0.607528341955938,-0.49652699953569,
-0.856959882601033));
#61445=CARTESIAN_POINT('Ctrl Pts',(0.770706545376702,-0.147109375843807,
-0.84115299728294));
#61446=CARTESIAN_POINT('Ctrl Pts',(0.747702509968158,0.237845967245534,
-0.825346111964849));
#61447=CARTESIAN_POINT('Ctrl Pts',(0.544073399919657,0.565344039543632,
-0.809539226646757));
#61448=CARTESIAN_POINT('Ctrl Pts',(0.209010601793413,0.7562700019739,-0.793732341328665));
#61449=CARTESIAN_POINT('Ctrl Pts',(-0.176543608420089,0.764501211165595,
-0.777925456010573));
#61450=CARTESIAN_POINT('Ctrl Pts',(-0.519449570135073,0.588049225519544,
-0.762118570692482));
#61451=CARTESIAN_POINT('Ctrl Pts',(-0.736870307276803,0.269540159904672,
-0.74631168537439));
#61452=CARTESIAN_POINT('Ctrl Pts',(-0.776282742349966,-0.114082651955772,
-0.730504800056299));
#61453=CARTESIAN_POINT('Ctrl Pts',(-0.628165877455098,-0.470146124038807,
-0.714697914738207));
#61454=CARTESIAN_POINT('Ctrl Pts',(-0.328300814595196,-0.712634775101368,
-0.698891029420116));
#61455=CARTESIAN_POINT('Ctrl Pts',(0.0508730085671695,-0.782969785206921,
-0.683084144102023));
#61456=CARTESIAN_POINT('Ctrl Pts',(0.417757263556233,-0.664160083333571,
-0.667277258783932));
#61457=CARTESIAN_POINT('Ctrl Pts',(0.683722455274473,-0.384906939013955,
-0.65147037346584));
#61458=CARTESIAN_POINT('Ctrl Pts',(0.784518454873481,-0.0126704976450974,
-0.635663488147748));
#61459=CARTESIAN_POINT('Ctrl Pts',(0.695795625019874,0.362626799548583,
-0.619856602829656));
#61460=CARTESIAN_POINT('Ctrl Pts',(0.438987045783509,0.650323089842206,
-0.604049717511565));
#61461=CARTESIAN_POINT('Ctrl Pts',(0.0761308515485031,0.780918587939964,
-0.588242832193473));
#61462=CARTESIAN_POINT('Ctrl Pts',(-0.305116535119352,0.722864888858496,
-0.572435946875381));
#61463=CARTESIAN_POINT('Ctrl Pts',(-0.612655867855218,0.490186224949473,
-0.55662906155729));
#61464=CARTESIAN_POINT('Ctrl Pts',(-0.7721938091491,0.139091583711784,-0.540822176239198));
#61465=CARTESIAN_POINT('Ctrl Pts',(-0.745190228173637,-0.245603891219511,
-0.525015290921106));
#61466=CARTESIAN_POINT('Ctrl Pts',(-0.538168473137809,-0.570967986903094,
-0.509208405603014));
#61467=CARTESIAN_POINT('Ctrl Pts',(-0.201139503556795,-0.758401376354612,
-0.493401520284923));
#61468=CARTESIAN_POINT('Ctrl Pts',(0.184479429757929,-0.762625129105924,
-0.477594634966831));
#61469=CARTESIAN_POINT('Ctrl Pts',(0.525533030837889,-0.582618898634463,
-0.461787749648739));
#61470=CARTESIAN_POINT('Ctrl Pts',(0.739631804756678,-0.261867410992487,
-0.445980864330648));
#61471=CARTESIAN_POINT('Ctrl Pts',(0.775055172134831,0.122144290472071,
-0.430173979012556));
#61472=CARTESIAN_POINT('Ctrl Pts',(0.623245787915859,0.476649174333111,
-0.414367093694465));
#61473=CARTESIAN_POINT('Ctrl Pts',(0.320876768735667,0.716008272880776,
-0.398560208376372));
#61474=CARTESIAN_POINT('Ctrl Pts',(-0.0590075583808678,0.782398782975698,
-0.382753323058282));
#61475=CARTESIAN_POINT('Ctrl Pts',(-0.42463722605947,0.659782520070082,
-0.366946437740189));
#61476=CARTESIAN_POINT('Ctrl Pts',(-0.687685814201396,0.377780317777545,
-0.351139552422098));
#61477=CARTESIAN_POINT('Ctrl Pts',(-0.784607767917408,0.00451642091067697,
-0.335332667104006));
#61478=CARTESIAN_POINT('Ctrl Pts',(-0.691989316556942,-0.36983852333275,
-0.319525781785914));
#61479=CARTESIAN_POINT('Ctrl Pts',(-0.432204618808581,-0.654850299689326,
-0.303718896467823));
#61480=CARTESIAN_POINT('Ctrl Pts',(-0.0680107604816475,-0.781667630139005,
-0.287912011149731));
#61481=CARTESIAN_POINT('Ctrl Pts',(0.312612692139218,-0.719654814723043,
-0.272105125831638));
#61482=CARTESIAN_POINT('Ctrl Pts',(0.61771721778651,-0.483792503119908,
-0.256298240513548));
#61483=CARTESIAN_POINT('Ctrl Pts',(0.773597665268418,-0.131058767708956,
-0.240491355195456));
#61484=CARTESIAN_POINT('Ctrl Pts',(0.742597454081923,0.253335286484711,
-0.224684469877363));
#61485=CARTESIAN_POINT('Ctrl Pts',(0.532205418195133,0.576530261290379,
-0.208877584559272));
#61486=CARTESIAN_POINT('Ctrl Pts',(0.193246675731908,0.760450832669695,
-0.19307069924118));
#61487=CARTESIAN_POINT('Ctrl Pts',(-0.192395317590102,0.760666671909099,
-0.177263813923089));
#61488=CARTESIAN_POINT('Ctrl Pts',(-0.531559740144116,0.57712564154978,
-0.161456928604996));
#61489=CARTESIAN_POINT('Ctrl Pts',(-0.742313384280858,0.254166374460362,
-0.145650043286905));
#61490=CARTESIAN_POINT('Ctrl Pts',(-0.773743937523648,-0.130192731445162,
-0.129843157968813));
#61491=CARTESIAN_POINT('Ctrl Pts',(-0.618258275472054,-0.483100747794865,
-0.114036272650722));
#61492=CARTESIAN_POINT('Ctrl Pts',(-0.313418265672134,-0.719304415348375,
-0.0982293873326304));
#61493=CARTESIAN_POINT('Ctrl Pts',(0.0671361300166105,-0.781743301689138,
-0.0824225020145388));
#61494=CARTESIAN_POINT('Ctrl Pts',(0.431470547789015,-0.655333629357333,
-0.0666156166964473));
#61495=CARTESIAN_POINT('Ctrl Pts',(0.691576407042652,-0.370613010854759,
-0.0508087313783553));
#61496=CARTESIAN_POINT('Ctrl Pts',(0.784609369614335,0.00363837865489593,
-0.0350018460602636));
#61497=CARTESIAN_POINT('Ctrl Pts',(0.688114061647999,0.377009838606768,
-0.0191949607421719));
#61498=CARTESIAN_POINT('Ctrl Pts',(0.425364134651334,0.659307686157797,
-0.00338807542408051));
#61499=CARTESIAN_POINT('Ctrl Pts',(0.0599058768073062,0.782330365606711,
0.0124188098940116));
#61500=CARTESIAN_POINT('Ctrl Pts',(-0.320122461446881,0.716371695718231,
0.028225695212104));
#61501=CARTESIAN_POINT('Ctrl Pts',(-0.521762533820769,0.557007454829145,
0.038763618757498));
#61502=CARTESIAN_POINT('Ctrl Pts',(-0.597589667152297,0.458088845993785,
0.0440325805301951));
#61503=CARTESIAN_POINT('Ctrl Pts',(-0.342067962509724,0.713322310757519,
-3.9489));
#61504=CARTESIAN_POINT('Ctrl Pts',(-0.460143716676633,0.656700034907516,
-3.9436310382273));
#61505=CARTESIAN_POINT('Ctrl Pts',(-0.667522495464715,0.483755515001817,
-3.93309311468191));
#61506=CARTESIAN_POINT('Ctrl Pts',(-0.817353501043518,0.107227706467285,
-3.91728622936382));
#61507=CARTESIAN_POINT('Ctrl Pts',(-0.769721511945864,-0.295100358763466,
-3.90147934404572));
#61508=CARTESIAN_POINT('Ctrl Pts',(-0.536151628753535,-0.626190577805068,
-3.88567245872763));
#61509=CARTESIAN_POINT('Ctrl Pts',(-0.173058463308598,-0.805984132719911,
-3.86986557340955));
#61510=CARTESIAN_POINT('Ctrl Pts',(0.231839351934833,-0.791086409962412,
-3.85405868809145));
#61511=CARTESIAN_POINT('Ctrl Pts',(0.580731794093568,-0.58507652561776,
-3.83825180277336));
#61512=CARTESIAN_POINT('Ctrl Pts',(0.789334414412207,-0.237731105128708,
-3.82244491745526));
#61513=CARTESIAN_POINT('Ctrl Pts',(0.807255021711117,0.167045585715507,
-3.80663803213718));
#61514=CARTESIAN_POINT('Ctrl Pts',(0.630164133983604,0.531467605154613,
-3.79083114681908));
#61515=CARTESIAN_POINT('Ctrl Pts',(0.300842381187657,0.767501618274884,
-3.775024261501));
#61516=CARTESIAN_POINT('Ctrl Pts',(-0.101154933391865,0.818127384573358,
-3.7592173761829));
#61517=CARTESIAN_POINT('Ctrl Pts',(-0.478715886449932,0.671115415569497,
-3.74341049086481));
#61518=CARTESIAN_POINT('Ctrl Pts',(-0.740631799246196,0.361979719574299,
-3.72760360554672));
#61519=CARTESIAN_POINT('Ctrl Pts',(-0.823630729382582,-0.0346006348303968,
-3.71179672022863));
#61520=CARTESIAN_POINT('Ctrl Pts',(-0.707662345034486,-0.422822410439913,
-3.69598983491053));
#61521=CARTESIAN_POINT('Ctrl Pts',(-0.420741525768683,-0.708901509635718,
-3.68018294959245));
#61522=CARTESIAN_POINT('Ctrl Pts',(-0.0321807252489052,-0.823728829850542,
-3.66437606427435));
#61523=CARTESIAN_POINT('Ctrl Pts',(0.364154084354281,-0.739565132941993,
-3.64856917895626));
#61524=CARTESIAN_POINT('Ctrl Pts',(0.672518935458776,-0.476742136719247,
-3.63276229363817));
#61525=CARTESIAN_POINT('Ctrl Pts',(0.818421067445377,-0.0987508973835936,
-3.61695540832007));
#61526=CARTESIAN_POINT('Ctrl Pts',(0.766614398872004,0.303095936604549,
-3.60114852300198));
#61527=CARTESIAN_POINT('Ctrl Pts',(0.529614045435536,0.63172283975934,-3.58534163768389));
#61528=CARTESIAN_POINT('Ctrl Pts',(0.164673000054145,0.807742277220862,
-3.5695347523658));
#61529=CARTESIAN_POINT('Ctrl Pts',(-0.240048670008569,0.788632626389314,
-3.55372786704771));
#61530=CARTESIAN_POINT('Ctrl Pts',(-0.586780954777519,0.579010271480279,
-3.53792098172961));
#61531=CARTESIAN_POINT('Ctrl Pts',(-0.791762540114605,0.229514407920758,
-3.52211409641153));
#61532=CARTESIAN_POINT('Ctrl Pts',(-0.805475317338525,-0.175426042908079,
-3.50630721109343));
#61533=CARTESIAN_POINT('Ctrl Pts',(-0.62460664355012,-0.537988219391752,
-3.49050032577534));
#61534=CARTESIAN_POINT('Ctrl Pts',(-0.292849588209368,-0.770586725850833,
-3.47469344045725));
#61535=CARTESIAN_POINT('Ctrl Pts',(0.109652152381827,-0.817031938696122,
-3.45888655513916));
#61536=CARTESIAN_POINT('Ctrl Pts',(0.485664844261286,-0.666103927642191,
-3.44307966982107));
#61537=CARTESIAN_POINT('Ctrl Pts',(0.744353804342099,-0.354262892966616,
-3.42727278450297));
#61538=CARTESIAN_POINT('Ctrl Pts',(0.823226648152874,0.043158650843427,
-3.41146589918488));
#61539=CARTESIAN_POINT('Ctrl Pts',(0.703229790731081,0.430154210487319,
-3.39565901386679));
#61540=CARTESIAN_POINT('Ctrl Pts',(0.41335128687045,0.713235933625179,-3.3798521285487));
#61541=CARTESIAN_POINT('Ctrl Pts',(0.0236180867260336,0.824018791867665,
-3.36404524323061));
#61542=CARTESIAN_POINT('Ctrl Pts',(-0.371820616102767,0.735740587987778,
-3.34823835791252));
#61543=CARTESIAN_POINT('Ctrl Pts',(-0.677437330051128,0.469726992225103,
-3.33243147259442));
#61544=CARTESIAN_POINT('Ctrl Pts',(-0.819403171261899,0.0902398265600419,
-3.31662458727633));
#61545=CARTESIAN_POINT('Ctrl Pts',(-0.763422961742281,-0.31104688530234,
-3.30081770195824));
#61546=CARTESIAN_POINT('Ctrl Pts',(-0.523020033817682,-0.637192928081435,
-3.28501081664015));
#61547=CARTESIAN_POINT('Ctrl Pts',(-0.156269352091197,-0.80941007713559,
-3.26920393132206));
#61548=CARTESIAN_POINT('Ctrl Pts',(0.248231856093482,-0.786095241680057,
-3.25339704600397));
#61549=CARTESIAN_POINT('Ctrl Pts',(0.592766838490301,-0.572880666943699,
-3.23759016068587));
#61550=CARTESIAN_POINT('Ctrl Pts',(0.79410509087887,-0.221273333259802,
-3.22178327536778));
#61551=CARTESIAN_POINT('Ctrl Pts',(0.803608637084535,0.183787762853733,
-3.20597639004969));
#61552=CARTESIAN_POINT('Ctrl Pts',(0.618981672666545,0.544450615092468,
-3.1901695047316));
#61553=CARTESIAN_POINT('Ctrl Pts',(0.284825170316527,0.773588654082908,
-3.17436261941351));
#61554=CARTESIAN_POINT('Ctrl Pts',(-0.118137530972093,0.815848213301628,
-3.15855573409542));
#61555=CARTESIAN_POINT('Ctrl Pts',(-0.492561341371445,0.661020505247762,
-3.14274884877732));
#61556=CARTESIAN_POINT('Ctrl Pts',(-0.74799540937477,0.34650779345624,-3.12694196345923));
#61557=CARTESIAN_POINT('Ctrl Pts',(-0.822733646018086,-0.0517120013287895,
-3.11113507814114));
#61558=CARTESIAN_POINT('Ctrl Pts',(-0.698721277655212,-0.437439549564865,
-3.09532819282305));
#61559=CARTESIAN_POINT('Ctrl Pts',(-0.405916399909998,-0.71749331680215,
-3.07952130750496));
#61560=CARTESIAN_POINT('Ctrl Pts',(-0.0150528971717421,-0.824219748403531,
-3.06371442218686));
#61561=CARTESIAN_POINT('Ctrl Pts',(0.379446985863416,-0.731836572118947,
-3.04790753686877));
#61562=CARTESIAN_POINT('Ctrl Pts',(0.6822825515668,-0.462661110532472,-3.03210065155068));
#61563=CARTESIAN_POINT('Ctrl Pts',(0.820296767656767,-0.0817190084588727,
-3.01629376623259));
#61564=CARTESIAN_POINT('Ctrl Pts',(0.760149063852653,0.318964236389567,
-3.0004868809145));
#61565=CARTESIAN_POINT('Ctrl Pts',(0.516369528450532,0.642594190340542,
-2.9846799955964));
#61566=CARTESIAN_POINT('Ctrl Pts',(0.14784882476994,0.810990449010216,-2.96887311027832));
#61567=CARTESIAN_POINT('Ctrl Pts',(-0.256388229536036,0.783472947284729,
-2.95306622496022));
#61568=CARTESIAN_POINT('Ctrl Pts',(-0.598688694785053,0.566689182981476,
-2.93725933964213));
#61569=CARTESIAN_POINT('Ctrl Pts',(-0.796361866772409,0.213008357869846,
-2.92145245432404));
#61570=CARTESIAN_POINT('Ctrl Pts',(-0.801655155439179,-0.19212963105525,
-2.90564556900595));
#61571=CARTESIAN_POINT('Ctrl Pts',(-0.613289842782184,-0.550854202227637,
-2.88983868368786));
#61572=CARTESIAN_POINT('Ctrl Pts',(-0.276769987173107,-0.776507023517393,
-2.87403179836976));
#61573=CARTESIAN_POINT('Ctrl Pts',(0.126610148995108,-0.814576364463811,
-2.85822491305167));
#61574=CARTESIAN_POINT('Ctrl Pts',(0.499404634710725,-0.655865683048816,
-2.84241802773358));
#61575=CARTESIAN_POINT('Ctrl Pts',(0.751556220051425,-0.338715266077066,
-2.82661114241549));
#61576=CARTESIAN_POINT('Ctrl Pts',(0.82215177671343,0.0602597661677676,
-2.8108042570974));
#61577=CARTESIAN_POINT('Ctrl Pts',(0.69413729254441,0.444677638824754,-2.79499737177931));
#61578=CARTESIAN_POINT('Ctrl Pts',(0.398437668089385,0.721673200291612,
-2.77919048646121));
#61579=CARTESIAN_POINT('Ctrl Pts',(0.00648608168618137,0.82433167724891,
-2.76338360114312));
#61580=CARTESIAN_POINT('Ctrl Pts',(-0.387032369844621,0.727853507282956,
-2.74757671582503));
#61581=CARTESIAN_POINT('Ctrl Pts',(-0.687054076668443,0.455545254727689,
-2.73176983050694));
#61582=CARTESIAN_POINT('Ctrl Pts',(-0.821101760099986,0.0731893635192228,
-2.71596294518885));
#61583=CARTESIAN_POINT('Ctrl Pts',(-0.756793058835995,-0.32684713471178,
-2.70015605987076));
#61584=CARTESIAN_POINT('Ctrl Pts',(-0.509663247682897,-0.647926043104431,
-2.68434917455266));
#61585=CARTESIAN_POINT('Ctrl Pts',(-0.139412327630636,-0.81248322215062,
-2.66854228923457));
#61586=CARTESIAN_POINT('Ctrl Pts',(0.264516909330157,-0.780766026444583,
-2.65273540391648));
#61587=CARTESIAN_POINT('Ctrl Pts',(0.604545884015083,-0.560436488366046,
-2.63692851859839));
#61588=CARTESIAN_POINT('Ctrl Pts',(0.79853262403083,-0.204720374486952,
-2.6211216332803));
#61589=CARTESIAN_POINT('Ctrl Pts',(0.799615083406745,0.200450746469219,
-2.6053147479622));
#61590=CARTESIAN_POINT('Ctrl Pts',(0.607531768697286,0.557198289117249,
-2.58950786264412));
#61591=CARTESIAN_POINT('Ctrl Pts',(0.268684908855737,0.779341518927888,
-2.57370097732602));
#61592=CARTESIAN_POINT('Ctrl Pts',(-0.13506909128519,0.813216529560877,
-2.55789409200793));
#61593=CARTESIAN_POINT('Ctrl Pts',(-0.506193985104167,0.650640017840899,
-2.54208720668984));
#61594=CARTESIAN_POINT('Ctrl Pts',(-0.755035851752847,0.330886152535123,
-2.52628032137175));
#61595=CARTESIAN_POINT('Ctrl Pts',(-0.82148110308923,-0.0688010220777596,
-2.51047343605365));
#61596=CARTESIAN_POINT('Ctrl Pts',(-0.689478330535574,-0.451867696448331,
-2.49466655073557));
#61597=CARTESIAN_POINT('Ctrl Pts',(-0.390915899220144,-0.725775132605511,
-2.47885966541747));
#61598=CARTESIAN_POINT('Ctrl Pts',(0.00208143439030202,-0.824354566313865,
-2.46305278009938));
#61599=CARTESIAN_POINT('Ctrl Pts',(0.39457594871488,-0.723791823708583,
-2.44724589478129));
#61600=CARTESIAN_POINT('Ctrl Pts',(0.69175138996213,-0.448380193426408,
-2.4314390094632));
#61601=CARTESIAN_POINT('Ctrl Pts',(0.821818061640689,-0.06465181306649,
-2.4156321241451));
#61602=CARTESIAN_POINT('Ctrl Pts',(0.753355309189543,0.334694728801593,
-2.39982523882701));
#61603=CARTESIAN_POINT('Ctrl Pts',(0.50290191589039,0.653187910455651,-2.38401835350892));
#61604=CARTESIAN_POINT('Ctrl Pts',(0.130960771937376,0.813888235315641,
-2.36821146819083));
#61605=CARTESIAN_POINT('Ctrl Pts',(-0.272617017460498,0.777974771546345,
-2.35240458287274));
#61606=CARTESIAN_POINT('Ctrl Pts',(-0.610337773518973,0.554123258479144,
-2.33659769755465));
#61607=CARTESIAN_POINT('Ctrl Pts',(-0.800617128180865,0.196410278333562,
-2.32079081223656));
#61608=CARTESIAN_POINT('Ctrl Pts',(-0.797488641344603,-0.208750210294458,
-2.30498392691846));
#61609=CARTESIAN_POINT('Ctrl Pts',(-0.601708072367388,-0.563482190507886,
-2.28917704160037));
#61610=CARTESIAN_POINT('Ctrl Pts',(-0.260570808670166,-0.782091834147768,
-2.27337015628228));
#61611=CARTESIAN_POINT('Ctrl Pts',(0.143513444153849,-0.811768855474724,
-2.25756327096419));
#61612=CARTESIAN_POINT('Ctrl Pts',(0.51292865920343,-0.645344074071665,
-2.2417563856461));
#61613=CARTESIAN_POINT('Ctrl Pts',(0.75843392862833,-0.323021298488259,
-2.22594950032801));
#61614=CARTESIAN_POINT('Ctrl Pts',(0.82072169758797,0.077334846479212,-2.21014261500991));
#61615=CARTESIAN_POINT('Ctrl Pts',(0.684744894864187,0.459008945805065,
-2.19433572969182));
#61616=CARTESIAN_POINT('Ctrl Pts',(0.383351905762432,0.729798670675655,
-2.17852884437373));
#61617=CARTESIAN_POINT('Ctrl Pts',(-0.0106487256416806,0.824288413126043,
-2.16272195905564));
#61618=CARTESIAN_POINT('Ctrl Pts',(-0.402076907658228,0.719651960116582,
-2.14691507373754));
#61619=CARTESIAN_POINT('Ctrl Pts',(-0.696373984069875,0.441166700559203,
-2.13110818841946));
#61620=CARTESIAN_POINT('Ctrl Pts',(-0.822445594907919,0.0561072792799869,
-2.11530130310136));
#61621=CARTESIAN_POINT('Ctrl Pts',(-0.749836186240129,-0.342506171004995,
-2.09949441778327));
#61622=CARTESIAN_POINT('Ctrl Pts',(-0.49608626339494,-0.658379224036185,
-2.08368753246518));
#61623=CARTESIAN_POINT('Ctrl Pts',(-0.122495070580787,-0.815205336743481,
-2.06788064714709));
#61624=CARTESIAN_POINT('Ctrl Pts',(0.280687678997866,-0.775099484086033,
-2.052073761829));
#61625=CARTESIAN_POINT('Ctrl Pts',(0.616063737688632,-0.547750175241189,
-2.0362668765109));
#61626=CARTESIAN_POINT('Ctrl Pts',(0.80261515406582,-0.188078967020618,
-2.02045999119281));
#61627=CARTESIAN_POINT('Ctrl Pts',(0.795276058939349,0.21702712606847,-2.00465310587472));
#61628=CARTESIAN_POINT('Ctrl Pts',(0.59581938283618,0.569705227647034,-1.98884622055663));
#61629=CARTESIAN_POINT('Ctrl Pts',(0.252428563056937,0.784757672103085,
-1.97303933523854));
#61630=CARTESIAN_POINT('Ctrl Pts',(-0.15194229548847,0.810233498575157,
-1.95723244992045));
#61631=CARTESIAN_POINT('Ctrl Pts',(-0.519607929566004,0.639978423779874,
-1.94142556460235));
#61632=CARTESIAN_POINT('Ctrl Pts',(-0.761750083636275,0.315121553454813,
-1.92561867928426));
#61633=CARTESIAN_POINT('Ctrl Pts',(-0.819873642236459,-0.0858603175952819,
-1.90981179396617));
#61634=CARTESIAN_POINT('Ctrl Pts',(-0.679937496809979,-0.466100615536416,
-1.89400490864808));
#61635=CARTESIAN_POINT('Ctrl Pts',(-0.375746504737283,-0.733743379901555,
-1.87819802332999));
#61636=CARTESIAN_POINT('Ctrl Pts',(0.0192148666762014,-0.824133224830948,
-1.86239113801189));
#61637=CARTESIAN_POINT('Ctrl Pts',(0.409534436462281,-0.715434363672282,
-1.84658425269381));
#61638=CARTESIAN_POINT('Ctrl Pts',(0.700921359684447,-0.433905555287956,
-1.83077736737571));
#61639=CARTESIAN_POINT('Ctrl Pts',(0.82298429211898,-0.0475566850933253,
-1.81497048205762));
#61640=CARTESIAN_POINT('Ctrl Pts',(0.746236070104087,0.350280617572898,
-1.79916359673953));
#61641=CARTESIAN_POINT('Ctrl Pts',(0.489217026385898,0.663499423108855,
-1.78335671142144));
#61642=CARTESIAN_POINT('Ctrl Pts',(0.114016137979435,0.816434384168071,
-1.76754982610334));
#61643=CARTESIAN_POINT('Ctrl Pts',(-0.288728022193726,0.772140474636412,
-1.75174294078526));
#61644=CARTESIAN_POINT('Ctrl Pts',(-0.621723158036865,0.541317927037625,
-1.73593605546716));
#61645=CARTESIAN_POINT('Ctrl Pts',(-0.804526485869913,0.179727340450608,
-1.72012917014907));
#61646=CARTESIAN_POINT('Ctrl Pts',(-0.792977575181979,-0.225280599764276,
-1.70432228483098));
#61647=CARTESIAN_POINT('Ctrl Pts',(-0.589866336167564,-0.575866728356393,
-1.68851539951288));
#61648=CARTESIAN_POINT('Ctrl Pts',(-0.2442590514967,-0.787338744844668,
-1.6727085141948));
#61649=CARTESIAN_POINT('Ctrl Pts',(0.160354734850819,-0.808610624702993,
-1.6569016288767));
#61650=CARTESIAN_POINT('Ctrl Pts',(0.526231074733792,-0.634543646533604,
-1.64109474355861));
#61651=CARTESIAN_POINT('Ctrl Pts',(0.764983958583825,-0.307187770721855,
-1.62528785824052));
#61652=CARTESIAN_POINT('Ctrl Pts',(0.818937028636985,0.0943765145514026,
-1.60948097292243));
#61653=CARTESIAN_POINT('Ctrl Pts',(0.675056655641679,0.473141939639169,
-1.59367408760433));
#61654=CARTESIAN_POINT('Ctrl Pts',(0.368100517638354,0.737608834197379,
-1.57786720228624));
#61655=CARTESIAN_POINT('Ctrl Pts',(-0.0277789322263472,0.823889018191168,
-1.56206031696815));
#61656=CARTESIAN_POINT('Ctrl Pts',(-0.416947729605723,0.711139489937295,
-1.54625343165006));
#61657=CARTESIAN_POINT('Ctrl Pts',(-0.705393025623311,0.426597541921698,
-1.53044654633197));
#61658=CARTESIAN_POINT('Ctrl Pts',(-0.823434095086754,0.0390009540947295,
-1.51463966101388));
#61659=CARTESIAN_POINT('Ctrl Pts',(-0.742555349646192,-0.358017228752285,
-1.49883277569579));
#61660=CARTESIAN_POINT('Ctrl Pts',(-0.482294946840517,-0.668547954617876,
-1.48302589037769));
#61661=CARTESIAN_POINT('Ctrl Pts',(-0.105524889981051,-0.817575244834462,
-1.4672190050596));
#61662=CARTESIAN_POINT('Ctrl Pts',(0.296737178574367,-0.769098062813428,
-1.45141211974151));
#61663=CARTESIAN_POINT('Ctrl Pts',(0.627315423264153,-0.534827208644584,
-1.43560523442342));
#61664=CARTESIAN_POINT('Ctrl Pts',(0.806350917141581,-0.171356300720379,
-1.41979834910533));
#61665=CARTESIAN_POINT('Ctrl Pts',(0.79059343834209,0.23350973988696,-1.40399146378723));
#61666=CARTESIAN_POINT('Ctrl Pts',(0.583849575376949,0.581966027104503,
-1.38818457846915));
#61667=CARTESIAN_POINT('Ctrl Pts',(0.236063156415228,0.789834773579211,
-1.37237769315105));
#61668=CARTESIAN_POINT('Ctrl Pts',(-0.168749853575404,0.80690040915216,
-1.35657080783296));
#61669=CARTESIAN_POINT('Ctrl Pts',(-0.532797379311024,0.629040329367638,
-1.34076392251487));
#61670=CARTESIAN_POINT('Ctrl Pts',(-0.768135204165577,0.299220807253026,
-1.32495703719678));
#61671=CARTESIAN_POINT('Ctrl Pts',(-0.817911957957395,-0.102882517474752,
-1.30915015187868));
#61672=CARTESIAN_POINT('Ctrl Pts',(-0.67010289856095,-0.480132157548163,
-1.29334326656059));
#61673=CARTESIAN_POINT('Ctrl Pts',(-0.360414770343172,-0.741394616037992,
-1.2775363812425));
#61674=CARTESIAN_POINT('Ctrl Pts',(0.0363399972487994,-0.823555819584562,
-1.26172949592441));
#61675=CARTESIAN_POINT('Ctrl Pts',(0.424315986345355,-0.706767802820285,
-1.24592261060632));
#61676=CARTESIAN_POINT('Ctrl Pts',(0.709788498881667,-0.419243449831899,
-1.23011572528823));
#61677=CARTESIAN_POINT('Ctrl Pts',(0.823794955226002,-0.0304410104272703,
-1.21430883997013));
#61678=CARTESIAN_POINT('Ctrl Pts',(0.73879442243765,0.365715168876903,-1.19850195465204));
#61679=CARTESIAN_POINT('Ctrl Pts',(0.475320772443814,0.673524273248605,
-1.18269506933395));
#61680=CARTESIAN_POINT('Ctrl Pts',(0.0970222437636098,0.818627795513149,
-1.16688818401586));
#61681=CARTESIAN_POINT('Ctrl Pts',(-0.304714283034701,0.7659725772417,-1.15108129869777));
#61682=CARTESIAN_POINT('Ctrl Pts',(-0.632839929324736,0.528278721153811,
-1.13527441337968));
#61683=CARTESIAN_POINT('Ctrl Pts',(-0.808088250815778,0.162966752023653,
-1.11946752806158));
#61684=CARTESIAN_POINT('Ctrl Pts',(-0.788123905941042,-0.241713657570019,
-1.10366064274349));
#61685=CARTESIAN_POINT('Ctrl Pts',(-0.577769750361789,-0.588002465078608,
-1.0878537574254));
#61686=CARTESIAN_POINT('Ctrl Pts',(-0.227841763088093,-0.792245488699401,
-1.07204687210731));
#61687=CARTESIAN_POINT('Ctrl Pts',(0.177126744867603,-0.805103036650745,
-1.05623998678922));
#61688=CARTESIAN_POINT('Ctrl Pts',(0.539306134041545,-0.623469066720079,
-1.04043310147113));
#61689=CARTESIAN_POINT('Ctrl Pts',(0.771203480001284,-0.291221523595961,
-1.02462621615303));
#61690=CARTESIAN_POINT('Ctrl Pts',(0.816798540920201,0.111377407593605,
-1.00881933083494));
#61691=CARTESIAN_POINT('Ctrl Pts',(0.665076760645423,0.487070514218457,
-0.993012445516851));
#61692=CARTESIAN_POINT('Ctrl Pts',(0.352690093023949,0.745100316504026,
-0.97720556019876));
#61693=CARTESIAN_POINT('Ctrl Pts',(-0.0448971370243381,0.823133665001416,
-0.961398674880668));
#61694=CARTESIAN_POINT('Ctrl Pts',(-0.431638410802547,0.702319774526884,
-0.945591789562575));
#61695=CARTESIAN_POINT('Ctrl Pts',(-0.714107304684638,0.411844073367198,
-0.929784904244485));
#61696=CARTESIAN_POINT('Ctrl Pts',(-0.824066833558586,0.0218777786890507,
-0.913978018926392));
#61697=CARTESIAN_POINT('Ctrl Pts',(-0.734953694713166,-0.373373606457542,
-0.898171133608302));
#61698=CARTESIAN_POINT('Ctrl Pts',(-0.468295256507801,-0.67842784148643,
-0.882364248290208));
#61699=CARTESIAN_POINT('Ctrl Pts',(-0.0885091177362583,-0.819591922513389,
-0.866557362972118));
#61700=CARTESIAN_POINT('Ctrl Pts',(0.312658473931717,-0.762764355519012,
-0.850750477654025));
#61701=CARTESIAN_POINT('Ctrl Pts',(0.638296079491797,-0.521673171896967,
-0.834943592335934));
#61702=CARTESIAN_POINT('Ctrl Pts',(0.809738299235259,-0.154559600553418,
-0.819136707017843));
#61703=CARTESIAN_POINT('Ctrl Pts',(0.785569244724172,0.249891466671308,
-0.80332982169975));
#61704=CARTESIAN_POINT('Ctrl Pts',(0.571627517831392,0.593975390255831,
-0.78752293638166));
#61705=CARTESIAN_POINT('Ctrl Pts',(0.21959575954505,0.79457062981303,-0.771716051063566));
#61706=CARTESIAN_POINT('Ctrl Pts',(-0.185484503901628,0.803218701341055,
-0.755909165745476));
#61707=CARTESIAN_POINT('Ctrl Pts',(-0.545756635885414,0.617830460368116,
-0.740102280427384));
#61708=CARTESIAN_POINT('Ctrl Pts',(-0.774188454672643,0.283190783789352,
-0.724295395109292));
#61709=CARTESIAN_POINT('Ctrl Pts',(-0.815596897790595,-0.119860267336591,
-0.708488509791201));
#61710=CARTESIAN_POINT('Ctrl Pts',(-0.659978784790912,-0.493956260206867,
-0.692681624473109));
#61711=CARTESIAN_POINT('Ctrl Pts',(-0.344927320057899,-0.748725535326077,
-0.676874739155018));
#61712=CARTESIAN_POINT('Ctrl Pts',(0.0534494272577162,-0.822622600040544,
-0.661067853836925));
#61713=CARTESIAN_POINT('Ctrl Pts',(0.438914212049227,-0.697795885508685,
-0.645260968518834));
#61714=CARTESIAN_POINT('Ctrl Pts',(0.718348976538538,-0.404400211767597,
-0.629454083200741));
#61715=CARTESIAN_POINT('Ctrl Pts',(0.824249700717708,-0.0133121838333343,
-0.613647197882651));
#61716=CARTESIAN_POINT('Ctrl Pts',(0.73103358132705,0.380991714271834,-0.597840312564558));
#61717=CARTESIAN_POINT('Ctrl Pts',(0.461219157890128,0.683258129674842,
-0.582033427246467));
#61718=CARTESIAN_POINT('Ctrl Pts',(0.0799864314401131,0.820467521695479,
-0.566226541928375));
#61719=CARTESIAN_POINT('Ctrl Pts',(-0.320568893177542,0.759473744179854,
-0.550419656610283));
#61720=CARTESIAN_POINT('Ctrl Pts',(-0.643683284421967,0.515011274369203,
-0.534612771292192));
#61721=CARTESIAN_POINT('Ctrl Pts',(-0.811300884170861,0.146135754403996,
-0.5188058859741));
#61722=CARTESIAN_POINT('Ctrl Pts',(-0.782929730631943,-0.258042283868811,
-0.502999000656008));
#61723=CARTESIAN_POINT('Ctrl Pts',(-0.565423541235985,-0.599884157473597,
-0.487192115337916));
#61724=CARTESIAN_POINT('Ctrl Pts',(-0.211326036474102,-0.796809945771127,
-0.471385230019825));
#61725=CARTESIAN_POINT('Ctrl Pts',(0.193822227918228,-0.801247606758639,
-0.455578344701732));
#61726=CARTESIAN_POINT('Ctrl Pts',(0.552148188094894,-0.612125119363043,
-0.439771459383642));
#61727=CARTESIAN_POINT('Ctrl Pts',(0.777089805759007,-0.275129455269591,
-0.423964574065549));
#61728=CARTESIAN_POINT('Ctrl Pts',(0.814307158363627,0.128330180431784,
-0.408157688747458));
#61729=CARTESIAN_POINT('Ctrl Pts',(0.654809521652447,0.500788651752962,
-0.392350803429367));
#61730=CARTESIAN_POINT('Ctrl Pts',(0.337127289937743,0.75226988092786,-0.376543918111274));
#61731=CARTESIAN_POINT('Ctrl Pts',(-0.0619959441787181,0.822022679904477,
-0.360737032793183));
#61732=CARTESIAN_POINT('Ctrl Pts',(-0.446142604190946,0.693196624411143,
-0.344930147475091));
#61733=CARTESIAN_POINT('Ctrl Pts',(-0.722513056285879,0.396912669078513,
-0.329123262156999));
#61734=CARTESIAN_POINT('Ctrl Pts',(-0.824343536942043,0.00474515106791719,
-0.313316376838907));
#61735=CARTESIAN_POINT('Ctrl Pts',(-0.727034505726059,-0.388568669452214,
-0.297509491520816));
#61736=CARTESIAN_POINT('Ctrl Pts',(-0.4540932408776,-0.68801461607538,-0.281702606202724));
#61737=CARTESIAN_POINT('Ctrl Pts',(-0.0714551055164477,-0.821254498476647,
-0.265895720884633));
#61738=CARTESIAN_POINT('Ctrl Pts',(0.328444686464207,-0.756101098668467,
-0.250088835566541));
#61739=CARTESIAN_POINT('Ctrl Pts',(0.649000961960564,-0.508293748131606,
-0.23428195024845));
#61740=CARTESIAN_POINT('Ctrl Pts',(0.812775837346289,-0.13769612351307,
-0.218475064930358));
#61741=CARTESIAN_POINT('Ctrl Pts',(0.780205647781058,0.266165228834457,
-0.202668179612265));
#61742=CARTESIAN_POINT('Ctrl Pts',(0.559158492630269,0.605728128345855,
-0.186861294294174));
#61743=CARTESIAN_POINT('Ctrl Pts',(0.203033483339035,0.798963194995345,
-0.171054408976082));
#61744=CARTESIAN_POINT('Ctrl Pts',(-0.202139008914331,0.799189965222836,
-0.155247523657991));
#61745=CARTESIAN_POINT('Ctrl Pts',(-0.55848011478331,0.606353661113862,
-0.139440638339899));
#61746=CARTESIAN_POINT('Ctrl Pts',(-0.779907191515234,0.267038406528302,
-0.123633753021807));
#61747=CARTESIAN_POINT('Ctrl Pts',(-0.812929517430994,-0.136786227605823,
-0.107826867703715));
#61748=CARTESIAN_POINT('Ctrl Pts',(-0.649569421035828,-0.507566959467682,
-0.092019982385624));
#61749=CARTESIAN_POINT('Ctrl Pts',(-0.329291057558848,-0.755732953626231,
-0.0762130970675324));
#61750=CARTESIAN_POINT('Ctrl Pts',(0.0705361801622086,-0.821334002345758,
-0.0604062117494408));
#61751=CARTESIAN_POINT('Ctrl Pts',(0.453321993478091,-0.688522423548524,
-0.0445993264313493));
#61752=CARTESIAN_POINT('Ctrl Pts',(0.726600684773263,-0.389382380212319,
-0.0287924411132574));
#61753=CARTESIAN_POINT('Ctrl Pts',(0.824345219755501,0.00382264113579923,
-0.0129855557951656));
#61754=CARTESIAN_POINT('Ctrl Pts',(0.722962991947054,0.396103169669058,
0.00282132952292606));
#61755=CARTESIAN_POINT('Ctrl Pts',(0.446906326427915,0.69269774295378,0.0186282148410175));
#61756=CARTESIAN_POINT('Ctrl Pts',(0.0629397571502896,0.821950797598125,
0.0344351001591095));
#61757=CARTESIAN_POINT('Ctrl Pts',(-0.33633478142099,0.752651708994679,
0.0502419854772021));
#61758=CARTESIAN_POINT('Ctrl Pts',(-0.548186737578833,0.585216606554525,
0.060779909022596));
#61759=CARTESIAN_POINT('Ctrl Pts',(-0.6278540692605,0.481288351939907,0.0660488707952931));
#61760=CARTESIAN_POINT('',(0.724715087996802,0.317217986926636,0.));
#61761=CARTESIAN_POINT('Ctrl Pts',(0.724729084696739,0.317243391110698,
-1.2490009027033E-16));
#61762=CARTESIAN_POINT('Ctrl Pts',(0.713907354081786,0.337969935177431,
-1.34446060076413E-16));
#61763=CARTESIAN_POINT('Ctrl Pts',(0.702180150875317,0.358180103462127,
3.85806153241612E-16));
#61764=CARTESIAN_POINT('Ctrl Pts',(0.689564616760934,0.377807260377953,
-5.82867087928207E-16));
#61765=CARTESIAN_POINT('Ctrl Pts',(0.672244619169851,0.404753587613862,
-1.91276862451717E-15));
#61766=CARTESIAN_POINT('Ctrl Pts',(0.653250778881373,0.430602076305703,
-3.21975719476629E-15));
#61767=CARTESIAN_POINT('Ctrl Pts',(0.632711953898066,0.455219340276035,
-3.78863607153335E-15));
#61768=CARTESIAN_POINT('Ctrl Pts',(0.625547182264457,0.463806836139848,
-3.98708399844897E-15));
#61769=CARTESIAN_POINT('Ctrl Pts',(0.61819423311545,0.472244298684595,-4.0830565983226E-15));
#61770=CARTESIAN_POINT('Ctrl Pts',(0.610658093425067,0.480525354174928,
-4.08700850940136E-15));
#61771=CARTESIAN_POINT('Ctrl Pts',(0.604662511634519,0.487113574078511,
-4.09015256021187E-15));
#61772=CARTESIAN_POINT('Ctrl Pts',(0.598551877745966,0.493601597685676,
-2.69712728464847E-15));
#61773=CARTESIAN_POINT('Ctrl Pts',(0.592337307151538,0.499977911351174,
-2.74780198594726E-15));
#61774=CARTESIAN_POINT('Ctrl Pts',(0.565761588131446,0.52724530139582,-2.96450507149132E-15));
#61775=CARTESIAN_POINT('Ctrl Pts',(0.537247897169337,0.552518599336613,
-4.23026249514447E-15));
#61776=CARTESIAN_POINT('Ctrl Pts',(0.507012766460455,0.575566644314705,
-4.4200754167889E-15));
#61777=CARTESIAN_POINT('Ctrl Pts',(0.496246418684442,0.583773761729892,
-4.4876653983399E-15));
#61778=CARTESIAN_POINT('Ctrl Pts',(0.485261491302899,0.591698223213175,
-3.12877767334142E-15));
#61779=CARTESIAN_POINT('Ctrl Pts',(0.474066915172834,0.599327810659463,
-2.80331313717852E-15));
#61780=CARTESIAN_POINT('Ctrl Pts',(0.466141780357405,0.604729132549227,
-2.57290241891962E-15));
#61781=CARTESIAN_POINT('Ctrl Pts',(0.458111564520058,0.609982647732742,
-3.13860258315148E-15));
#61782=CARTESIAN_POINT('Ctrl Pts',(0.449979348609982,0.615083700351862,
-3.02535774210355E-15));
#61783=CARTESIAN_POINT('Ctrl Pts',(0.443252675142053,0.619303105701028,
-2.93168572501986E-15));
#61784=CARTESIAN_POINT('Ctrl Pts',(0.436464975643143,0.623412692684743,
-2.97751776474101E-15));
#61785=CARTESIAN_POINT('Ctrl Pts',(0.429618472148824,0.627410530315628,
-2.95596880306448E-15));
#61786=CARTESIAN_POINT('Ctrl Pts',(0.423599928014177,0.630924902614511,
-2.93702579412369E-15));
#61787=CARTESIAN_POINT('Ctrl Pts',(0.417535907052476,0.634352939367129,
-2.51730515131399E-15));
#61788=CARTESIAN_POINT('Ctrl Pts',(0.41142778494146,0.637693315483735,-2.60902410786912E-15));
#61789=CARTESIAN_POINT('Ctrl Pts',(0.380168859262236,0.654788024278328,
-3.07741582773577E-15));
#61790=CARTESIAN_POINT('Ctrl Pts',(0.347756368125765,0.669590917142619,
-3.72554565325771E-15));
#61791=CARTESIAN_POINT('Ctrl Pts',(0.314455649451757,0.682041649083386,
-4.48946435582798E-15));
#61792=CARTESIAN_POINT('Ctrl Pts',(0.281473214350202,0.694373378684276,
-5.24608163117986E-15));
#61793=CARTESIAN_POINT('Ctrl Pts',(0.247618206494094,0.704397831449753,
-3.41330364724715E-15));
#61794=CARTESIAN_POINT('Ctrl Pts',(0.213141916409858,0.712006350953311,
-3.27515792264421E-15));
#61795=CARTESIAN_POINT('Ctrl Pts',(0.203917316012092,0.714042113846228,
-3.23819515481135E-15));
#61796=CARTESIAN_POINT('Ctrl Pts',(0.194648258593662,0.715904633490244,
-9.99391481991553E-16));
#61797=CARTESIAN_POINT('Ctrl Pts',(0.185339650976527,0.717591192759321,
-7.7715611723761E-16));
#61798=CARTESIAN_POINT('Ctrl Pts',(0.178247624911564,0.718876145653285,
-6.0783981729064E-16));
#61799=CARTESIAN_POINT('Ctrl Pts',(0.171133535383714,0.720058667660844,
-2.77537615559827E-15));
#61800=CARTESIAN_POINT('Ctrl Pts',(0.164012249108394,0.721135991470167,
-2.692290834716E-15));
#61801=CARTESIAN_POINT('Ctrl Pts',(0.128128177472471,0.726564612544256,
-2.27362495173283E-15));
#61802=CARTESIAN_POINT('Ctrl Pts',(0.091976494893039,0.72934310385842,-1.96570673819932E-15));
#61803=CARTESIAN_POINT('Ctrl Pts',(0.0558355686356328,0.729384403288966,
-1.9151347174784E-15));
#61804=CARTESIAN_POINT('Ctrl Pts',(0.0260765608470435,0.729418409890416,
-1.88146767879442E-15));
#61805=CARTESIAN_POINT('Ctrl Pts',(-0.00367576053293546,0.727595271520012,
-2.24940245056296E-15));
#61806=CARTESIAN_POINT('Ctrl Pts',(-0.0332514200405915,0.72394427085901,
-1.68962066560141E-15));
#61807=CARTESIAN_POINT('Ctrl Pts',(-0.0500595780777836,0.721869368823837,
-1.37149079581644E-15));
#61808=CARTESIAN_POINT('Ctrl Pts',(-0.0668105374205609,0.719203620011991,
-7.85849759292755E-16));
#61809=CARTESIAN_POINT('Ctrl Pts',(-0.0834712766367304,0.715948760770118,
-6.34908792207511E-16));
#61810=CARTESIAN_POINT('Ctrl Pts',(-0.0901507004907692,0.714643861618909,
-5.74395349015123E-16));
#61811=CARTESIAN_POINT('Ctrl Pts',(-0.0968164869457153,0.713244048991127,
-2.32306328507138E-15));
#61812=CARTESIAN_POINT('Ctrl Pts',(-0.103463703234474,0.711749937291047,
-2.18575157973078E-15));
#61813=CARTESIAN_POINT('Ctrl Pts',(-0.136683088775137,0.704283131571225,
-1.49953794069666E-15));
#61814=CARTESIAN_POINT('Ctrl Pts',(-0.169254000740599,0.694507641639826,
-8.76017226149467E-16));
#61815=CARTESIAN_POINT('Ctrl Pts',(-0.200928233818616,0.682489165262991,
-9.54097911787244E-16));
#61816=CARTESIAN_POINT('Ctrl Pts',(-0.230560396894032,0.67124553227465,
-1.0271446562549E-15));
#61817=CARTESIAN_POINT('Ctrl Pts',(-0.259408473741469,0.658038049136935,
-7.82058107895715E-16));
#61818=CARTESIAN_POINT('Ctrl Pts',(-0.287249018522639,0.642884462366263,
-8.11850586757146E-16));
#61819=CARTESIAN_POINT('Ctrl Pts',(-0.301188758766257,0.635297072643733,
-8.23187715172432E-16));
#61820=CARTESIAN_POINT('Ctrl Pts',(-0.31487550720896,0.627221248807101,
-7.66959557371012E-16));
#61821=CARTESIAN_POINT('Ctrl Pts',(-0.328286140734374,0.618672793771468,
-9.74914593498966E-16));
#61822=CARTESIAN_POINT('Ctrl Pts',(-0.33584241127504,0.613856135495664,
-1.0920876196874E-15));
#61823=CARTESIAN_POINT('Ctrl Pts',(-0.34331098503277,0.608889399167942,
5.25293495758233E-16));
#61824=CARTESIAN_POINT('Ctrl Pts',(-0.350687424397269,0.603775227006381,
6.67868538251071E-16));
#61825=CARTESIAN_POINT('Ctrl Pts',(-0.356960524220523,0.59942601312452,
7.89117752088122E-16));
#61826=CARTESIAN_POINT('Ctrl Pts',(-0.363160963461047,0.594974248859294,
-2.75203808569037E-16));
#61827=CARTESIAN_POINT('Ctrl Pts',(-0.369280669163366,0.590426553784604,
-2.8796409701215E-16));
#61828=CARTESIAN_POINT('Ctrl Pts',(-0.396035202864505,0.570544640003655,
-3.43750369064118E-16));
#61829=CARTESIAN_POINT('Ctrl Pts',(-0.421285868070597,0.548807068655703,
-5.37172934782348E-16));
#61830=CARTESIAN_POINT('Ctrl Pts',(-0.444845541212416,0.525391300388644,
-8.48279779752659E-16));
#61831=CARTESIAN_POINT('Ctrl Pts',(-0.467944926988566,0.502433008005308,
-1.15330850346674E-15));
#61832=CARTESIAN_POINT('Ctrl Pts',(-0.489419406519805,0.477860456590935,
-3.48883792920152E-16));
#61833=CARTESIAN_POINT('Ctrl Pts',(-0.50905162937919,0.45181388155706,5.46437894932694E-17));
#61834=CARTESIAN_POINT('Ctrl Pts',(-0.51885910579262,0.438802050338303,
2.56230093552368E-16));
#61835=CARTESIAN_POINT('Ctrl Pts',(-0.528206121608575,0.425422027334627,
-8.75593447961903E-16));
#61836=CARTESIAN_POINT('Ctrl Pts',(-0.537060862935893,0.41168983410154,
-8.88178419700125E-16));
#61837=CARTESIAN_POINT('Ctrl Pts',(-0.791061003003137,-1.6759841323199E-5,
-0.113133150823703));
#61838=CARTESIAN_POINT('Ctrl Pts',(-0.791095254159769,-0.04398138852515,
-0.111364389783707));
#61839=CARTESIAN_POINT('Ctrl Pts',(-0.787491390648307,-0.0879404613601665,
-0.109595628743711));
#61840=CARTESIAN_POINT('Ctrl Pts',(-0.780199113712507,-0.131278910560445,
-0.107826867703715));
#61841=CARTESIAN_POINT('Ctrl Pts',(-0.75847615196594,-0.260379804893108,
-0.102557905931018));
#61842=CARTESIAN_POINT('Ctrl Pts',(-0.704022786500887,-0.38397338218039,
-0.0972889441583214));
#61843=CARTESIAN_POINT('Ctrl Pts',(-0.623416376522197,-0.487131169850458,
-0.0920199823856242));
#61844=CARTESIAN_POINT('Ctrl Pts',(-0.542809966543505,-0.590288957520528,
-0.086751020612927));
#61845=CARTESIAN_POINT('Ctrl Pts',(-0.43605051205117,-0.673010955573384,
-0.0814820588402293));
#61846=CARTESIAN_POINT('Ctrl Pts',(-0.316032911851495,-0.72530546271973,
-0.0762130970675321));
#61847=CARTESIAN_POINT('Ctrl Pts',(-0.196015311651824,-0.777599969866074,
-0.0709441352948349));
#61848=CARTESIAN_POINT('Ctrl Pts',(-0.0627395657448089,-0.799466986105916,
-0.0656751735221379));
#61849=CARTESIAN_POINT('Ctrl Pts',(0.0676959427613463,-0.788265231092965,
-0.0604062117494408));
#61850=CARTESIAN_POINT('Ctrl Pts',(0.198131451267501,-0.777063476080014,
-0.0551372499767437));
#61851=CARTESIAN_POINT('Ctrl Pts',(0.325726722372791,-0.73279294981427,
-0.0498682882040467));
#61852=CARTESIAN_POINT('Ctrl Pts',(0.435070806474632,-0.660801012792033,
-0.0445993264313496));
#61853=CARTESIAN_POINT('Ctrl Pts',(0.544414890576473,-0.588809075769796,
-0.0393303646586525));
#61854=CARTESIAN_POINT('Ctrl Pts',(0.63550778767486,-0.489095727991068,
-0.0340614028859554));
#61855=CARTESIAN_POINT('Ctrl Pts',(0.69734499205443,-0.37370488387702,-0.0287924411132583));
#61856=CARTESIAN_POINT('Ctrl Pts',(0.759182196434005,-0.258314039762962,
-0.0235234793405607));
#61857=CARTESIAN_POINT('Ctrl Pts',(0.791763708094756,-0.127245699313574,
-0.0182545175678628));
#61858=CARTESIAN_POINT('Ctrl Pts',(0.791157425957054,0.00366855899999786,
-0.0129855557951652));
#61859=CARTESIAN_POINT('Ctrl Pts',(0.79065935752875,0.111216274536829,-0.00865703719677685));
#61860=CARTESIAN_POINT('Ctrl Pts',(0.767763411681256,0.21866000266156,-0.00432851859838852));
#61861=CARTESIAN_POINT('Ctrl Pts',(0.724729084696739,0.317243391110698,
-1.2490009027033E-16));
#61862=CARTESIAN_POINT('',(-0.392911963072353,-0.550971611700039,-3.9489));
#61863=CARTESIAN_POINT('Ctrl Pts',(-0.392911963072352,-0.55097161170004,
-3.9489));
#61864=CARTESIAN_POINT('Ctrl Pts',(-0.410226675319238,-0.540659270969453,
-3.9489));
#61865=CARTESIAN_POINT('Ctrl Pts',(-0.427051408450124,-0.52958559429897,
-3.9489));
#61866=CARTESIAN_POINT('Ctrl Pts',(-0.443332390878944,-0.517780552977276,
-3.9489));
#61867=CARTESIAN_POINT('Ctrl Pts',(-0.466677690336157,-0.500853305130619,
-3.9489));
#61868=CARTESIAN_POINT('Ctrl Pts',(-0.488905894728908,-0.482423482892805,
-3.9489));
#61869=CARTESIAN_POINT('Ctrl Pts',(-0.509923806362163,-0.462642074974146,
-3.9489));
#61870=CARTESIAN_POINT('Ctrl Pts',(-0.517327269552611,-0.455674164558665,
-3.9489));
#61871=CARTESIAN_POINT('Ctrl Pts',(-0.524580430635456,-0.448538306246225,
-3.9489));
#61872=CARTESIAN_POINT('Ctrl Pts',(-0.531678725979323,-0.441240346778602,
-3.9489));
#61873=CARTESIAN_POINT('Ctrl Pts',(-0.538225005850256,-0.434509930129616,
-3.9489));
#61874=CARTESIAN_POINT('Ctrl Pts',(-0.544633942965916,-0.427647286739263,
-3.9489));
#61875=CARTESIAN_POINT('Ctrl Pts',(-0.550897879416926,-0.42066290979901,
-3.9489));
#61876=CARTESIAN_POINT('Ctrl Pts',(-0.573293465677302,-0.395691517214845,
-3.9489));
#61877=CARTESIAN_POINT('Ctrl Pts',(-0.593857165977117,-0.369147438134823,
-3.9489));
#61878=CARTESIAN_POINT('Ctrl Pts',(-0.612442003359716,-0.341256039200072,
-3.9489));
#61879=CARTESIAN_POINT('Ctrl Pts',(-0.62054720638056,-0.329092066696705,
-3.9489));
#61880=CARTESIAN_POINT('Ctrl Pts',(-0.628275646226725,-0.316671295724295,
-3.9489));
#61881=CARTESIAN_POINT('Ctrl Pts',(-0.635613055626581,-0.304010218159141,
-3.9489));
#61882=CARTESIAN_POINT('Ctrl Pts',(-0.640795026572562,-0.295068460583405,
-3.9489));
#61883=CARTESIAN_POINT('Ctrl Pts',(-0.645783514374678,-0.286003276249334,
-3.9489));
#61884=CARTESIAN_POINT('Ctrl Pts',(-0.650560922240377,-0.276844901871744,
-3.9489));
#61885=CARTESIAN_POINT('Ctrl Pts',(-0.654529773316609,-0.269236544991434,
-3.9489));
#61886=CARTESIAN_POINT('Ctrl Pts',(-0.658354827363553,-0.26156085373562,
-3.9489));
#61887=CARTESIAN_POINT('Ctrl Pts',(-0.662033934973313,-0.253821649227226,
-3.9489));
#61888=CARTESIAN_POINT('Ctrl Pts',(-0.676643520622293,-0.223089585065688,
-3.9489));
#61889=CARTESIAN_POINT('Ctrl Pts',(-0.688955077275006,-0.191358774899916,
-3.9489));
#61890=CARTESIAN_POINT('Ctrl Pts',(-0.698971541765702,-0.158905930467818,
-3.9489));
#61891=CARTESIAN_POINT('Ctrl Pts',(-0.705986454727241,-0.136177963004147,
-3.9489));
#61892=CARTESIAN_POINT('Ctrl Pts',(-0.711874862372623,-0.113094947092123,
-3.9489));
#61893=CARTESIAN_POINT('Ctrl Pts',(-0.716624788120144,-0.0897440668667491,
-3.9489));
#61894=CARTESIAN_POINT('Ctrl Pts',(-0.720306876758467,-0.0716427290053002,
-3.9489));
#61895=CARTESIAN_POINT('Ctrl Pts',(-0.723304625101438,-0.0533802762630154,
-3.9489));
#61896=CARTESIAN_POINT('Ctrl Pts',(-0.72560763940422,-0.0349959353965368,
-3.9489));
#61897=CARTESIAN_POINT('Ctrl Pts',(-0.726507866913688,-0.0278096624448529,
-3.9489));
#61898=CARTESIAN_POINT('Ctrl Pts',(-0.727301722894688,-0.0206050118170668,
-3.9489));
#61899=CARTESIAN_POINT('Ctrl Pts',(-0.727987512495698,-0.0133983183097541,
-3.9489));
#61900=CARTESIAN_POINT('Ctrl Pts',(-0.731448056449583,0.0229671786407993,
-3.9489));
#61901=CARTESIAN_POINT('Ctrl Pts',(-0.73217341076392,0.0594719055121494,
-3.9489));
#61902=CARTESIAN_POINT('Ctrl Pts',(-0.730147114733274,0.0958034382110051,
-3.9489));
#61903=CARTESIAN_POINT('Ctrl Pts',(-0.728417200964393,0.126820830393477,
-3.9489));
#61904=CARTESIAN_POINT('Ctrl Pts',(-0.724681055099625,0.157713114353514,
-3.9489));
#61905=CARTESIAN_POINT('Ctrl Pts',(-0.719015395369232,0.188308180357181,
-3.9489));
#61906=CARTESIAN_POINT('Ctrl Pts',(-0.715645853912015,0.206504003648978,
-3.9489));
#61907=CARTESIAN_POINT('Ctrl Pts',(-0.711593191576187,0.224594773207228,
-3.9489));
#61908=CARTESIAN_POINT('Ctrl Pts',(-0.706868098144863,0.24254386435619,
-3.9489));
#61909=CARTESIAN_POINT('Ctrl Pts',(-0.704394402297967,0.251940629282866,
-3.9489));
#61910=CARTESIAN_POINT('Ctrl Pts',(-0.701734975730179,0.261302326828154,
-3.9489));
#61911=CARTESIAN_POINT('Ctrl Pts',(-0.698899697272481,0.270596942138144,
-3.9489));
#61912=CARTESIAN_POINT('Ctrl Pts',(-0.688418916117528,0.304955059140368,
-3.9489));
#61913=CARTESIAN_POINT('Ctrl Pts',(-0.675523352479239,0.338465571894,-3.9489));
#61914=CARTESIAN_POINT('Ctrl Pts',(-0.660343917061696,0.370874272183928,
-3.9489));
#61915=CARTESIAN_POINT('Ctrl Pts',(-0.64790738084614,0.397426773233408,
-3.9489));
#61916=CARTESIAN_POINT('Ctrl Pts',(-0.633936685218803,0.423240167834942,
-3.9489));
#61917=CARTESIAN_POINT('Ctrl Pts',(-0.618478081309822,0.448170731169764,
-3.9489));
#61918=CARTESIAN_POINT('Ctrl Pts',(-0.609699449374064,0.462328299392362,
-3.9489));
#61919=CARTESIAN_POINT('Ctrl Pts',(-0.600440569466785,0.476201051310872,
-3.9489));
#61920=CARTESIAN_POINT('Ctrl Pts',(-0.590720974703061,0.489771952996098,
-3.9489));
#61921=CARTESIAN_POINT('Ctrl Pts',(-0.585324176843069,0.497307186198035,
-3.9489));
#61922=CARTESIAN_POINT('Ctrl Pts',(-0.579785301520311,0.504749336264221,
-3.9489));
#61923=CARTESIAN_POINT('Ctrl Pts',(-0.574107424317768,0.512095298656615,
-3.9489));
#61924=CARTESIAN_POINT('Ctrl Pts',(-0.569610147766929,0.51791381554808,
-3.9489));
#61925=CARTESIAN_POINT('Ctrl Pts',(-0.565026451224481,0.523670769178515,
-3.9489));
#61926=CARTESIAN_POINT('Ctrl Pts',(-0.560365993088301,0.529355290390339,
-3.9489));
#61927=CARTESIAN_POINT('Ctrl Pts',(-0.537332412930287,0.557450140975096,
-3.9489));
#61928=CARTESIAN_POINT('Ctrl Pts',(-0.512378533159309,0.583841839277855,
-3.9489));
#61929=CARTESIAN_POINT('Ctrl Pts',(-0.485742425179841,0.608380818598942,
-3.9489));
#61930=CARTESIAN_POINT('Ctrl Pts',(-0.4588904163952,0.633118700304628,-3.9489));
#61931=CARTESIAN_POINT('Ctrl Pts',(-0.430328032424734,0.655974654499438,
-3.9489));
#61932=CARTESIAN_POINT('Ctrl Pts',(-0.400255088118573,0.676767567817735,
-3.9489));
#61933=CARTESIAN_POINT('Ctrl Pts',(-0.381437541314102,0.689778319794161,
-3.9489));
#61934=CARTESIAN_POINT('Ctrl Pts',(-0.362027717551045,0.701980711486138,
-3.9489));
#61935=CARTESIAN_POINT('Ctrl Pts',(-0.342067962509724,0.713322310757519,
-3.9489));
#61936=CARTESIAN_POINT('Ctrl Pts',(-0.392911963072353,-0.550971611700039,
-3.9489));
#61937=CARTESIAN_POINT('Ctrl Pts',(-0.317943423445919,-0.604318458484074,
-3.94457148140162));
#61938=CARTESIAN_POINT('Ctrl Pts',(-0.12742655914631,-0.688673578978978,
-3.93497400103053));
#61939=CARTESIAN_POINT('Ctrl Pts',(0.198313347812299,-0.676688375201064,
-3.92010755888674));
#61940=CARTESIAN_POINT('Ctrl Pts',(0.496752882142743,-0.50046932737395,
-3.90430067356866));
#61941=CARTESIAN_POINT('Ctrl Pts',(0.675189733576972,-0.203353101808354,
-3.88849378825056));
#61942=CARTESIAN_POINT('Ctrl Pts',(0.690518863850223,0.142889328597765,
-3.87268690293247));
#61943=CARTESIAN_POINT('Ctrl Pts',(0.539036872034762,0.454612727099145,
-3.85688001761438));
#61944=CARTESIAN_POINT('Ctrl Pts',(0.257337933699506,0.656514151291388,
-3.84107313229629));
#61945=CARTESIAN_POINT('Ctrl Pts',(-0.0865270426321366,0.699818987663747,
-3.82526624697819));
#61946=CARTESIAN_POINT('Ctrl Pts',(-0.409489369688631,0.574066239054321,
-3.8094593616601));
#61947=CARTESIAN_POINT('Ctrl Pts',(-0.627215929976506,0.31708661902035,
-3.79409795320704));
#61948=CARTESIAN_POINT('Ctrl Pts',(-0.676676933801994,0.102511671164669,
-3.78400550652667));
#61949=CARTESIAN_POINT('Ctrl Pts',(-0.676746306964879,-9.26850736500048E-6,
-3.779182021619));
#61950=CARTESIAN_POINT('Origin',(-1.87869726832665E-16,-4.25270154953079E-17,
-3.9489));
#61951=CARTESIAN_POINT('',(-0.7911,-9.68818082805472E-17,-3.9489));
#61952=CARTESIAN_POINT('Origin',(0.,0.,-3.9489));
#61953=CARTESIAN_POINT('Origin',(0.,0.,-3.9489));
#61954=CARTESIAN_POINT('',(0.392888236737263,-0.550964357679773,-3.9489));
#61955=CARTESIAN_POINT('Ctrl Pts',(0.342093838304107,0.713335417936174,
-3.9489));
#61956=CARTESIAN_POINT('Ctrl Pts',(0.36243410985328,0.701804032951062,-3.9489));
#61957=CARTESIAN_POINT('Ctrl Pts',(0.382227029135937,0.689385557357458,
-3.9489));
#61958=CARTESIAN_POINT('Ctrl Pts',(0.401406592559599,0.67609942500637,-3.9489));
#61959=CARTESIAN_POINT('Ctrl Pts',(0.427738414049162,0.657858756142971,
-3.9489));
#61960=CARTESIAN_POINT('Ctrl Pts',(0.452915219791259,0.637983175646837,
-3.9489));
#61961=CARTESIAN_POINT('Ctrl Pts',(0.476808155612978,0.616606072714045,
-3.9489));
#61962=CARTESIAN_POINT('Ctrl Pts',(0.485142977099612,0.609148875399504,
-3.9489));
#61963=CARTESIAN_POINT('Ctrl Pts',(0.493321353159824,0.60150879667183,-3.9489));
#61964=CARTESIAN_POINT('Ctrl Pts',(0.501337086175958,0.59369104072589,-3.9489));
#61965=CARTESIAN_POINT('Ctrl Pts',(0.507714221250369,0.587471411710591,
-3.9489));
#61966=CARTESIAN_POINT('Ctrl Pts',(0.513987244720764,0.581140261137621,
-3.9489));
#61967=CARTESIAN_POINT('Ctrl Pts',(0.520145033866962,0.574709095554839,
-3.9489));
#61968=CARTESIAN_POINT('Ctrl Pts',(0.546477934368195,0.547207140002666,
-3.9489));
#61969=CARTESIAN_POINT('Ctrl Pts',(0.570750975301364,0.517837266684296,
-3.9489));
#61970=CARTESIAN_POINT('Ctrl Pts',(0.592740615567436,0.486823864488614,
-3.9489));
#61971=CARTESIAN_POINT('Ctrl Pts',(0.600570848422469,0.475780384109644,
-3.9489));
#61972=CARTESIAN_POINT('Ctrl Pts',(0.608111042112103,0.46452822046729,-3.9489));
#61973=CARTESIAN_POINT('Ctrl Pts',(0.615349294412633,0.453076721193327,
-3.9489));
#61974=CARTESIAN_POINT('Ctrl Pts',(0.62047357290034,0.444969699091146,-3.9489));
#61975=CARTESIAN_POINT('Ctrl Pts',(0.625446502357492,0.43676276545034,-3.9489));
#61976=CARTESIAN_POINT('Ctrl Pts',(0.63026353616155,0.428459160230405,-3.9489));
#61977=CARTESIAN_POINT('Ctrl Pts',(0.634248011417182,0.421590719842154,
-3.9489));
#61978=CARTESIAN_POINT('Ctrl Pts',(0.638120625423605,0.414665084097462,
-3.9489));
#61979=CARTESIAN_POINT('Ctrl Pts',(0.641879525123554,0.407684540413875,
-3.9489));
#61980=CARTESIAN_POINT('Ctrl Pts',(0.645183854741995,0.401548165653247,
-3.9489));
#61981=CARTESIAN_POINT('Ctrl Pts',(0.648400329135512,0.395369324114637,
-3.9489));
#61982=CARTESIAN_POINT('Ctrl Pts',(0.651527671538601,0.389149436432343,
-3.9489));
#61983=CARTESIAN_POINT('Ctrl Pts',(0.667532158485783,0.357318540293221,
-3.9489));
#61984=CARTESIAN_POINT('Ctrl Pts',(0.681206342360694,0.324413949743605,
-3.9489));
#61985=CARTESIAN_POINT('Ctrl Pts',(0.692499081100256,0.290702930386092,
-3.9489));
#61986=CARTESIAN_POINT('Ctrl Pts',(0.703683883584329,0.257314121723617,
-3.9489));
#61987=CARTESIAN_POINT('Ctrl Pts',(0.712532639875156,0.223132979179132,
-3.9489));
#61988=CARTESIAN_POINT('Ctrl Pts',(0.718945440041857,0.18841439839863,-3.9489));
#61989=CARTESIAN_POINT('Ctrl Pts',(0.720661271767476,0.17912497087507,-3.9489));
#61990=CARTESIAN_POINT('Ctrl Pts',(0.722202427728805,0.169797098620667,
-3.9489));
#61991=CARTESIAN_POINT('Ctrl Pts',(0.723566361944834,0.16043577942429,-3.9489));
#61992=CARTESIAN_POINT('Ctrl Pts',(0.724605514495829,0.15330358887633,-3.9489));
#61993=CARTESIAN_POINT('Ctrl Pts',(0.725541534912411,0.146152887091712,
-3.9489));
#61994=CARTESIAN_POINT('Ctrl Pts',(0.726372171175049,0.13899862758013,-3.9489));
#61995=CARTESIAN_POINT('Ctrl Pts',(0.730557736333052,0.102948408380828,
-3.9489));
#61996=CARTESIAN_POINT('Ctrl Pts',(0.732085505672932,0.0667223030632399,
-3.9489));
#61997=CARTESIAN_POINT('Ctrl Pts',(0.730878086010825,0.0306015222127752,
-3.9489));
#61998=CARTESIAN_POINT('Ctrl Pts',(0.729883877878345,0.000859109363216645,
-3.9489));
#61999=CARTESIAN_POINT('Ctrl Pts',(0.727033863426423,-0.028812453629752,
-3.9489));
#62000=CARTESIAN_POINT('Ctrl Pts',(0.722363181286008,-0.0582443055791226,
-3.9489));
#62001=CARTESIAN_POINT('Ctrl Pts',(0.719708783610423,-0.0749707359064128,
-3.9489));
#62002=CARTESIAN_POINT('Ctrl Pts',(0.716465868037568,-0.0916195872890394,
-3.9489));
#62003=CARTESIAN_POINT('Ctrl Pts',(0.712637310914196,-0.108157918201531,
-3.9489));
#62004=CARTESIAN_POINT('Ctrl Pts',(0.711102411545406,-0.114788268189906,
-3.9489));
#62005=CARTESIAN_POINT('Ctrl Pts',(0.70947312652975,-0.121401709586236,
-3.9489));
#62006=CARTESIAN_POINT('Ctrl Pts',(0.707750240343777,-0.127993333808553,
-3.9489));
#62007=CARTESIAN_POINT('Ctrl Pts',(0.699140135230816,-0.160934904691981,
-3.9489));
#62008=CARTESIAN_POINT('Ctrl Pts',(0.688245128415544,-0.193148622364025,
-3.9489));
#62009=CARTESIAN_POINT('Ctrl Pts',(0.675139455165793,-0.224388701026552,
-3.9489));
#62010=CARTESIAN_POINT('Ctrl Pts',(0.662878724445518,-0.253614684679756,
-3.9489));
#62011=CARTESIAN_POINT('Ctrl Pts',(0.648682408810677,-0.281989199846348,
-3.9489));
#62012=CARTESIAN_POINT('Ctrl Pts',(0.63257596521799,-0.309289548789184,
-3.9489));
#62013=CARTESIAN_POINT('Ctrl Pts',(0.624511476822419,-0.322958820095266,
-3.9489));
#62014=CARTESIAN_POINT('Ctrl Pts',(0.615967587212459,-0.336358375532833,
-3.9489));
#62015=CARTESIAN_POINT('Ctrl Pts',(0.606960888675029,-0.349465651586987,
-3.9489));
#62016=CARTESIAN_POINT('Ctrl Pts',(0.601886026129267,-0.356851001951248,
-3.9489));
#62017=CARTESIAN_POINT('Ctrl Pts',(0.596664204853623,-0.364143522529331,
-3.9489));
#62018=CARTESIAN_POINT('Ctrl Pts',(0.591298218799256,-0.371338869599802,
-3.9489));
#62019=CARTESIAN_POINT('Ctrl Pts',(0.586734870194414,-0.377457945699274,
-3.9489));
#62020=CARTESIAN_POINT('Ctrl Pts',(0.582071543364956,-0.38350086171868,
-3.9489));
#62021=CARTESIAN_POINT('Ctrl Pts',(0.577315132755829,-0.389459778321814,
-3.9489));
#62022=CARTESIAN_POINT('Ctrl Pts',(0.556520706295363,-0.415511409114614,
-3.9489));
#62023=CARTESIAN_POINT('Ctrl Pts',(0.533923690776528,-0.439995956565335,
-3.9489));
#62024=CARTESIAN_POINT('Ctrl Pts',(0.50970790495092,-0.462732538395585,
-3.9489));
#62025=CARTESIAN_POINT('Ctrl Pts',(0.485965238395172,-0.485024901108929,
-3.9489));
#62026=CARTESIAN_POINT('Ctrl Pts',(0.4606654197042,-0.505637555568327,-3.9489));
#62027=CARTESIAN_POINT('Ctrl Pts',(0.433956108776739,-0.524358124969866,
-3.9489));
#62028=CARTESIAN_POINT('Ctrl Pts',(0.420613178308345,-0.533710191615534,
-3.9489));
#62029=CARTESIAN_POINT('Ctrl Pts',(0.406918183931599,-0.542589349743738,
-3.9489));
#62030=CARTESIAN_POINT('Ctrl Pts',(0.392888236737269,-0.550964357679769,
-3.9489));
#62031=CARTESIAN_POINT('Origin',(0.,0.,-3.9489));
#62032=CARTESIAN_POINT('Origin',(0.,0.,-4.318617978381));
#62033=CARTESIAN_POINT('Ctrl Pts',(0.392888236737263,-0.550964357679773,
-3.9489));
#62034=CARTESIAN_POINT('Ctrl Pts',(0.484088989988678,-0.485929836599401,
-3.9436310382273));
#62035=CARTESIAN_POINT('Ctrl Pts',(0.633487089009969,-0.309770083749072,
-3.93309311468191));
#62036=CARTESIAN_POINT('Ctrl Pts',(0.704529888150662,0.0295137395378967,
-3.91728622936382));
#62037=CARTESIAN_POINT('Ctrl Pts',(0.605381802721961,0.361579326443786,
-3.90147934404573));
#62038=CARTESIAN_POINT('Ctrl Pts',(0.359987565129825,0.606340404497349,
-3.88567245872763));
#62039=CARTESIAN_POINT('Ctrl Pts',(0.0276308569381634,0.704603699753987,
-3.86986557340955));
#62040=CARTESIAN_POINT('Ctrl Pts',(-0.311401222734635,0.632664694044287,
-3.85405868809145));
#62041=CARTESIAN_POINT('Ctrl Pts',(-0.575206784816063,0.407884951603224,
-3.83825180277336));
#62042=CARTESIAN_POINT('Ctrl Pts',(-0.668516504975362,0.166252472050367,
-3.82643823286988));
#62043=CARTESIAN_POINT('Ctrl Pts',(-0.676723249594477,0.0271363966683822,
-3.81989362473909));
#62044=CARTESIAN_POINT('Ctrl Pts',(-0.676696040235193,1.73011422674348E-5,
-3.818617978381));
#62045=CARTESIAN_POINT('Ctrl Pts',(0.459308237155079,-0.644108029201231,
-4.0149488707953));
#62046=CARTESIAN_POINT('Ctrl Pts',(0.565926998640516,-0.568079050884871,
-4.0096799090226));
#62047=CARTESIAN_POINT('Ctrl Pts',(0.740581699594772,-0.362138485671492,
-3.9991419854772));
#62048=CARTESIAN_POINT('Ctrl Pts',(0.823634689694088,0.0345032057757077,
-3.98333510015911));
#62049=CARTESIAN_POINT('Ctrl Pts',(0.707725054135285,0.422706376754354,
-3.96752821484102));
#62050=CARTESIAN_POINT('Ctrl Pts',(0.42084551909888,0.708845713015883,-3.95172132952292));
#62051=CARTESIAN_POINT('Ctrl Pts',(0.0323020111183534,0.823720979570532,
-3.93591444420484));
#62052=CARTESIAN_POINT('Ctrl Pts',(-0.364045378018858,0.73962027406301,
-3.92010755888674));
#62053=CARTESIAN_POINT('Ctrl Pts',(-0.672448777106521,0.476840232323508,
-3.90430067356865));
#62054=CARTESIAN_POINT('Ctrl Pts',(-0.818406554677498,0.0988716815199221,
-3.88849378825056));
#62055=CARTESIAN_POINT('Ctrl Pts',(-0.766658961359266,-0.302983395308224,
-3.87268690293247));
#62056=CARTESIAN_POINT('Ctrl Pts',(-0.529706957010623,-0.631644832581376,
-3.85688001761438));
#62057=CARTESIAN_POINT('Ctrl Pts',(-0.16479179584882,-0.807718106261876,
-3.84107313229629));
#62058=CARTESIAN_POINT('Ctrl Pts',(0.239932677737653,-0.788667896894534,
-3.82526624697819));
#62059=CARTESIAN_POINT('Ctrl Pts',(0.586695791877696,-0.579096582494008,
-3.80945936166011));
#62060=CARTESIAN_POINT('Ctrl Pts',(0.791728777027483,-0.229630847958036,
-3.79365247634201));
#62061=CARTESIAN_POINT('Ctrl Pts',(0.805501111685453,0.175307571484335,
-3.77784559102392));
#62062=CARTESIAN_POINT('Ctrl Pts',(0.624685763408961,0.53789635206483,-3.76203870570583));
#62063=CARTESIAN_POINT('Ctrl Pts',(0.292962920676836,0.770543647187415,
-3.74623182038774));
#62064=CARTESIAN_POINT('Ctrl Pts',(-0.109531985601694,0.817048059516638,
-3.73042493506964));
#62065=CARTESIAN_POINT('Ctrl Pts',(-0.485566872179705,0.666175351459444,
-3.71461804975155));
#62066=CARTESIAN_POINT('Ctrl Pts',(-0.74430169445999,0.354372366768378,
-3.69881116443346));
#62067=CARTESIAN_POINT('Ctrl Pts',(-0.8232329888101,-0.0430375735757952,
-3.68300427911537));
#62068=CARTESIAN_POINT('Ctrl Pts',(-0.703293050205527,-0.430050778523623,
-3.66719739379728));
#62069=CARTESIAN_POINT('Ctrl Pts',(-0.413456183346354,-0.713175133526495,
-3.65139050847919));
#62070=CARTESIAN_POINT('Ctrl Pts',(-0.0237392800030705,-0.824015311249586,
-3.63558362316109));
#62071=CARTESIAN_POINT('Ctrl Pts',(0.371712403104245,-0.735795267713018,
-3.61977673784301));
#62072=CARTESIAN_POINT('Ctrl Pts',(0.677368238717631,-0.4698266231045,-3.60396985252491));
#62073=CARTESIAN_POINT('Ctrl Pts',(0.819389892225629,-0.0903603404282356,
-3.58816296720682));
#62074=CARTESIAN_POINT('Ctrl Pts',(0.763468702865619,0.310934601401261,
-3.57235608188873));
#62075=CARTESIAN_POINT('Ctrl Pts',(0.523113745259786,0.637115998954219,
-3.55654919657064));
#62076=CARTESIAN_POINT('Ctrl Pts',(0.156388395655667,0.809387086818189,
-3.54074231125254));
#62077=CARTESIAN_POINT('Ctrl Pts',(-0.24811623817114,0.786131744022086,
-3.52493542593445));
#62078=CARTESIAN_POINT('Ctrl Pts',(-0.592682576430445,0.572967843948815,
-3.50912854061636));
#62079=CARTESIAN_POINT('Ctrl Pts',(-0.794072540157967,0.221390125277976,
-3.49332165529827));
#62080=CARTESIAN_POINT('Ctrl Pts',(-0.803635661092522,-0.183669569673137,
-3.47751476998018));
#62081=CARTESIAN_POINT('Ctrl Pts',(-0.61906174312059,-0.544359573083855,
-3.46170788466209));
#62082=CARTESIAN_POINT('Ctrl Pts',(-0.284938944320829,-0.773546756578334,
-3.44590099934399));
#62083=CARTESIAN_POINT('Ctrl Pts',(0.118017538196231,-0.81586558162582,
-3.4300941140259));
#62084=CARTESIAN_POINT('Ctrl Pts',(0.49246411689282,-0.661092943674721,
-3.41428722870781));
#62085=CARTESIAN_POINT('Ctrl Pts',(0.747944440046074,-0.346617802785286,
-3.39848034338972));
#62086=CARTESIAN_POINT('Ctrl Pts',(0.822741244675879,0.0515909964307694,
-3.38267345807163));
#62087=CARTESIAN_POINT('Ctrl Pts',(0.698785608665519,0.437336780668508,
-3.36686657275354));
#62088=CARTESIAN_POINT('Ctrl Pts',(0.406021922608743,0.717433610144265,
-3.35105968743544));
#62089=CARTESIAN_POINT('Ctrl Pts',(0.0151741200765717,0.824217527527435,
-3.33525280211735));
#62090=CARTESIAN_POINT('Ctrl Pts',(-0.3793393469878,0.731892373529335,-3.31944591679926));
#62091=CARTESIAN_POINT('Ctrl Pts',(-0.682214499414893,0.46276145409014,
-3.30363903148117));
#62092=CARTESIAN_POINT('Ctrl Pts',(-0.820284741821662,0.0818396538244422,
-3.28783214616308));
#62093=CARTESIAN_POINT('Ctrl Pts',(-0.760195969456813,-0.318852433933235,
-3.27202526084498));
#62094=CARTESIAN_POINT('Ctrl Pts',(-0.516464034345362,-0.642518239298502,
-3.2562183755269));
#62095=CARTESIAN_POINT('Ctrl Pts',(-0.147968100840412,-0.810968697137697,
-3.2404114902088));
#62096=CARTESIAN_POINT('Ctrl Pts',(0.256272997221724,-0.78351064925662,
-3.22460460489071));
#62097=CARTESIAN_POINT('Ctrl Pts',(0.598605343294585,-0.566777231002363,
-3.20879771957262));
#62098=CARTESIAN_POINT('Ctrl Pts',(0.796330531612867,-0.213125481875595,
-3.19299083425453));
#62099=CARTESIAN_POINT('Ctrl Pts',(0.801683406353151,0.19201172511475,-3.17718394893643));
#62100=CARTESIAN_POINT('Ctrl Pts',(0.613370855098921,0.550763997297166,
-3.16137706361834));
#62101=CARTESIAN_POINT('Ctrl Pts',(0.27688419046779,0.776466310713176,-3.14557017830025));
#62102=CARTESIAN_POINT('Ctrl Pts',(-0.126490343206336,0.814594978918406,
-3.12976329298216));
#62103=CARTESIAN_POINT('Ctrl Pts',(-0.499308168325542,0.655939128004212,
-3.11395640766407));
#62104=CARTESIAN_POINT('Ctrl Pts',(-0.751506396787274,0.338825799182031,
-3.09814952234598));
#62105=CARTESIAN_POINT('Ctrl Pts',(-0.822160632548107,-0.0601388467766978,
-3.08234263702788));
#62106=CARTESIAN_POINT('Ctrl Pts',(-0.694202688143384,-0.444575544062011,
-3.06653575170979));
#62107=CARTESIAN_POINT('Ctrl Pts',(-0.39854380561222,-0.72161459354122,
-3.0507288663917));
#62108=CARTESIAN_POINT('Ctrl Pts',(-0.00660732112534875,-0.824330716345741,
-3.03492198107361));
#62109=CARTESIAN_POINT('Ctrl Pts',(0.386925316718677,-0.727910424355693,
-3.01911509575552));
#62110=CARTESIAN_POINT('Ctrl Pts',(0.686987071048648,-0.455646300122731,
-3.00330821043742));
#62111=CARTESIAN_POINT('Ctrl Pts',(0.821090988765058,-0.0733101273519162,
-2.98750132511934));
#62112=CARTESIAN_POINT('Ctrl Pts',(0.75684112385447,0.326735825777088,-2.97169443980124));
#62113=CARTESIAN_POINT('Ctrl Pts',(0.509758537822454,0.647851078351074,
-2.95588755448315));
#62114=CARTESIAN_POINT('Ctrl Pts',(0.139531823323549,0.812462711072661,
-2.94008066916506));
#62115=CARTESIAN_POINT('Ctrl Pts',(-0.264402075070642,0.780804923973891,
-2.92427378384697));
#62116=CARTESIAN_POINT('Ctrl Pts',(-0.604463452097174,0.560525397892281,
-2.90846689852887));
#62117=CARTESIAN_POINT('Ctrl Pts',(-0.798502507817305,0.204837817829157,
-2.89266001321079));
#62118=CARTESIAN_POINT('Ctrl Pts',(-0.799644558175188,-0.200333140504363,
-2.87685312789269));
#62119=CARTESIAN_POINT('Ctrl Pts',(-0.607613714126209,-0.55710893100837,
-2.8610462425746));
#62120=CARTESIAN_POINT('Ctrl Pts',(-0.268799529105187,-0.779301995221598,
-2.84523935725651));
#62121=CARTESIAN_POINT('Ctrl Pts',(0.134949485424267,-0.813236388135246,
-2.82943247193842));
#62122=CARTESIAN_POINT('Ctrl Pts',(0.506098287232193,-0.650714461391611,
-2.81362558662032));
#62123=CARTESIAN_POINT('Ctrl Pts',(0.754987179934878,-0.330997197476829,
-2.79781870130224));
#62124=CARTESIAN_POINT('Ctrl Pts',(0.821491215144233,0.0686802012546899,
-2.78201181598414));
#62125=CARTESIAN_POINT('Ctrl Pts',(0.689544783659541,0.451766286846917,
-2.76620493066606));
#62126=CARTESIAN_POINT('Ctrl Pts',(0.391022640102679,0.725717632092995,
-2.75039804534795));
#62127=CARTESIAN_POINT('Ctrl Pts',(-0.00196019151241356,0.824354865487413,
-2.73459116002987));
#62128=CARTESIAN_POINT('Ctrl Pts',(-0.394469492901894,0.723849850295803,
-2.71878427471178));
#62129=CARTESIAN_POINT('Ctrl Pts',(-0.691685438112023,0.448481929744459,
-2.70297738939368));
#62130=CARTESIAN_POINT('Ctrl Pts',(-0.8218085459694,0.0647726823220635,
-2.68717050407559));
#62131=CARTESIAN_POINT('Ctrl Pts',(-0.753404528430612,-0.33458392541152,
-2.6713636187575));
#62132=CARTESIAN_POINT('Ctrl Pts',(-0.502997979981963,-0.65311394008825,
-2.65555673343941));
#62133=CARTESIAN_POINT('Ctrl Pts',(-0.131080474345465,-0.81386896724774,
-2.63974984812132));
#62134=CARTESIAN_POINT('Ctrl Pts',(0.272502593659544,-0.77801486043157,
-2.62394296280322));
#62135=CARTESIAN_POINT('Ctrl Pts',(0.610256270077472,-0.554213019907206,
-2.60813607748514));
#62136=CARTESIAN_POINT('Ctrl Pts',(0.80058823416634,-0.196528028326635,
-2.59232919216704));
#62137=CARTESIAN_POINT('Ctrl Pts',(0.797519336783819,0.208632917008397,
-2.57652230684895));
#62138=CARTESIAN_POINT('Ctrl Pts',(0.6017909420572,0.56339368887257,-2.56071542153086));
#62139=CARTESIAN_POINT('Ctrl Pts',(0.260685833493737,0.782053503808537,
-2.54490853621277));
#62140=CARTESIAN_POINT('Ctrl Pts',(-0.143394051139944,0.811789956023853,
-2.52910165089467));
#62141=CARTESIAN_POINT('Ctrl Pts',(-0.512833740181423,0.645419508176711,
-2.51329476557658));
#62142=CARTESIAN_POINT('Ctrl Pts',(-0.758386413513802,0.323132843272245,
-2.49748788025849));
#62143=CARTESIAN_POINT('Ctrl Pts',(-0.820733064771053,-0.0772141372745434,
-2.4816809949404));
#62144=CARTESIAN_POINT('Ctrl Pts',(-0.684812398335245,-0.458908232318686,
-2.46587410962231));
#62145=CARTESIAN_POINT('Ctrl Pts',(-0.383459238475105,-0.729742282611901,
-2.45006722430422));
#62146=CARTESIAN_POINT('Ctrl Pts',(0.0105274924210566,-0.824289972343991,
-2.43426033898612));
#62147=CARTESIAN_POINT('Ctrl Pts',(0.401971060656972,-0.719711089950575,
-2.41845345366803));
#62148=CARTESIAN_POINT('Ctrl Pts',(0.69630909311321,-0.441269116811264,
-2.40264656834994));
#62149=CARTESIAN_POINT('Ctrl Pts',(0.822437335928101,-0.0562282409028078,
-2.38683968303185));
#62150=CARTESIAN_POINT('Ctrl Pts',(0.7498865543874,0.342395885127914,-2.37103279771376));
#62151=CARTESIAN_POINT('Ctrl Pts',(0.496183091062214,0.658306256044616,
-2.35522591239567));
#62152=CARTESIAN_POINT('Ctrl Pts',(0.122614966774459,0.815187313766863,
-2.33941902707757));
#62153=CARTESIAN_POINT('Ctrl Pts',(-0.280573678014902,0.775140759996998,
-2.32361214175948));
#62154=CARTESIAN_POINT('Ctrl Pts',(-0.615983171527093,0.547840778875538,
-2.30780525644139));
#62155=CARTESIAN_POINT('Ctrl Pts',(-0.802587485371274,0.188197010945846,
-2.2919983711233));
#62156=CARTESIAN_POINT('Ctrl Pts',(-0.795307971733777,-0.21691015813059,
-2.27619148580521));
#62157=CARTESIAN_POINT('Ctrl Pts',(-0.595903167835748,-0.569617592044745,
-2.26038460048711));
#62158=CARTESIAN_POINT('Ctrl Pts',(-0.252543980030274,-0.784720539271147,
-2.24457771516903));
#62159=CARTESIAN_POINT('Ctrl Pts',(0.151823128217758,-0.810255838819881,
-2.22877082985093));
#62160=CARTESIAN_POINT('Ctrl Pts',(0.519513799646595,-0.640054840291277,
-2.21296394453284));
#62161=CARTESIAN_POINT('Ctrl Pts',(0.761703730357511,-0.315233586032623,
-2.19715705921474));
#62162=CARTESIAN_POINT('Ctrl Pts',(0.819886263319798,0.0857397330473568,
-2.18135017389666));
#62163=CARTESIAN_POINT('Ctrl Pts',(0.680006043336776,0.46600060904359,-2.16554328857856));
#62164=CARTESIAN_POINT('Ctrl Pts',(0.375854417686602,0.733688110377292,
-2.14973640326048));
#62165=CARTESIAN_POINT('Ctrl Pts',(-0.0190936562077946,0.82413604392488,
-2.13392951794238));
#62166=CARTESIAN_POINT('Ctrl Pts',(-0.409429209705767,0.715494590366164,
-2.11812263262429));
#62167=CARTESIAN_POINT('Ctrl Pts',(-0.700857536630393,0.434008640411582,
-2.1023157473062));
#62168=CARTESIAN_POINT('Ctrl Pts',(-0.822977290722719,0.0476777260177834,
-2.08650886198811));
#62169=CARTESIAN_POINT('Ctrl Pts',(-0.746287581717071,-0.350170861121284,
-2.07070197667002));
#62170=CARTESIAN_POINT('Ctrl Pts',(-0.489314607170079,-0.66342746537472,
-2.05489509135192));
#62171=CARTESIAN_POINT('Ctrl Pts',(-0.11413621500816,-0.816417608229481,
-2.03908820603383));
#62172=CARTESIAN_POINT('Ctrl Pts',(0.288614456342509,-0.772182933114719,
-2.02328132071574));
#62173=CARTESIAN_POINT('Ctrl Pts',(0.621643537857595,-0.541409363091763,
-2.00747443539765));
#62174=CARTESIAN_POINT('Ctrl Pts',(0.804500045483962,-0.179845665557549,
-1.99166755007956));
#62175=CARTESIAN_POINT('Ctrl Pts',(0.793010701884583,0.225163969808788,
-1.97586066476146));
#62176=CARTESIAN_POINT('Ctrl Pts',(0.589951027426904,0.575779968253043,
-1.96005377944338));
#62177=CARTESIAN_POINT('Ctrl Pts',(0.244374848153105,0.787302813530905,
-1.94424689412528));
#62178=CARTESIAN_POINT('Ctrl Pts',(-0.160235806195098,0.808634202230244,
-1.92844000880719));
#62179=CARTESIAN_POINT('Ctrl Pts',(-0.526137744084377,0.634621037197269,
-1.9126331234891));
#62180=CARTESIAN_POINT('Ctrl Pts',(-0.764938772147653,0.307300278992347,
-1.89682623817101));
#62181=CARTESIAN_POINT('Ctrl Pts',(-0.818950902257319,-0.0942560676851014,
-1.88101935285291));
#62182=CARTESIAN_POINT('Ctrl Pts',(-0.675126237820197,-0.473042650942049,
-1.86521246753482));
#62183=CARTESIAN_POINT('Ctrl Pts',(-0.368208999168154,-0.737554689182519,
-1.84940558221673));
#62184=CARTESIAN_POINT('Ctrl Pts',(0.0276577576026398,-0.82389309685658,
-1.83359869689864));
#62185=CARTESIAN_POINT('Ctrl Pts',(0.416843134459967,-0.711200806985709,
-1.81779181158055));
#62186=CARTESIAN_POINT('Ctrl Pts',(0.705330277365677,-0.42670128478221,
-1.80198492626245));
#62187=CARTESIAN_POINT('Ctrl Pts',(0.823428352030309,-0.0391220612466472,
-1.78617804094437));
#62188=CARTESIAN_POINT('Ctrl Pts',(0.742607999160884,0.357908013581426,
-1.77037115562627));
#62189=CARTESIAN_POINT('Ctrl Pts',(0.482393270201465,0.668477014913655,
-1.75456427030818));
#62190=CARTESIAN_POINT('Ctrl Pts',(0.105645134874769,0.817559717745943,
-1.73875738499009));
#62191=CARTESIAN_POINT('Ctrl Pts',(-0.296624060121656,0.769141699272949,
-1.722950499672));
#62192=CARTESIAN_POINT('Ctrl Pts',(-0.627236757667293,0.534919467242084,
-1.70714361435391));
#62193=CARTESIAN_POINT('Ctrl Pts',(-0.806325707920169,0.1714748942282,-1.69133672903581));
#62194=CARTESIAN_POINT('Ctrl Pts',(-0.790627775374702,-0.233393460511612,
-1.67552984371772));
#62195=CARTESIAN_POINT('Ctrl Pts',(-0.583935163748167,-0.581880151871441,
-1.65972295839963));
#62196=CARTESIAN_POINT('Ctrl Pts',(-0.236179320246973,-0.789800047664733,
-1.64391607308154));
#62197=CARTESIAN_POINT('Ctrl Pts',(0.16863117638069,-0.806925221415217,
-1.62810918776345));
#62198=CARTESIAN_POINT('Ctrl Pts',(0.532704858012667,-0.629118685824256,
-1.61230230244535));
#62199=CARTESIAN_POINT('Ctrl Pts',(0.768091189452786,-0.299333779063673,
-1.59649541712726));
#62200=CARTESIAN_POINT('Ctrl Pts',(0.817927082616174,0.102762221300083,
-1.58068853180917));
#62201=CARTESIAN_POINT('Ctrl Pts',(0.670173508875303,0.480033597371371,
-1.56488164649108));
#62202=CARTESIAN_POINT('Ctrl Pts',(0.360523808735873,0.741341601380979,
-1.54907476117299));
#62203=CARTESIAN_POINT('Ctrl Pts',(-0.0362188715584176,0.823561157380901,
-1.53326787585489));
#62204=CARTESIAN_POINT('Ctrl Pts',(-0.424212034108152,0.706830203600099,
-1.51746099053681));
#62205=CARTESIAN_POINT('Ctrl Pts',(-0.709726832198183,0.419347839223556,
-1.50165410521871));
#62206=CARTESIAN_POINT('Ctrl Pts',(-0.823790471129699,0.0305621707253191,
-1.48584721990062));
#62207=CARTESIAN_POINT('Ctrl Pts',(-0.738848204167142,-0.365606506783623,
-1.47004033458253));
#62208=CARTESIAN_POINT('Ctrl Pts',(-0.475419827761178,-0.673454359236813,
-1.45423344926444));
#62209=CARTESIAN_POINT('Ctrl Pts',(-0.0971426435341273,-0.818613518951852,
-1.43842656394635));
#62210=CARTESIAN_POINT('Ctrl Pts',(0.304601624198931,-0.766017386969061,
-1.42261967862825));
#62211=CARTESIAN_POINT('Ctrl Pts',(0.632762226807305,-0.528371792329412,
-1.40681279331016));
#62212=CARTESIAN_POINT('Ctrl Pts',(0.808064275481866,-0.163085601122539,
-1.39100590799207));
#62213=CARTESIAN_POINT('Ctrl Pts',(0.788159449594768,0.241597741334656,
-1.37519902267398));
#62214=CARTESIAN_POINT('Ctrl Pts',(0.577856226600103,0.58791748399161,-1.35939213735589));
#62215=CARTESIAN_POINT('Ctrl Pts',(0.227958281547799,0.792211971935104,
-1.34358525203779));
#62216=CARTESIAN_POINT('Ctrl Pts',(-0.177008331952761,0.805129080969527,
-1.32777836671971));
#62217=CARTESIAN_POINT('Ctrl Pts',(-0.53921443208789,0.623548380506011,
-1.31197148140161));
#62218=CARTESIAN_POINT('Ctrl Pts',(-0.771160641766101,0.291334946744169,
-1.29616459608352));
#62219=CARTESIAN_POINT('Ctrl Pts',(-0.816814914983744,-0.111257275104306,
-1.28035771076543));
#62220=CARTESIAN_POINT('Ctrl Pts',(-0.665148391468669,-0.486972693207921,
-1.26455082544734));
#62221=CARTESIAN_POINT('Ctrl Pts',(-0.352799676501823,-0.745048437931215,
-1.24874394012924));
#62222=CARTESIAN_POINT('Ctrl Pts',(0.0447760733506051,-0.823140261352119,
-1.23293705481115));
#62223=CARTESIAN_POINT('Ctrl Pts',(0.431535112702248,-0.702383252297912,
-1.21713016949306));
#62224=CARTESIAN_POINT('Ctrl Pts',(0.714046726236198,-0.411949098014427,
-1.20132328417497));
#62225=CARTESIAN_POINT('Ctrl Pts',(0.824063608906776,-0.0219989790461579,
-1.18551639885688));
#62226=CARTESIAN_POINT('Ctrl Pts',(0.735008602848248,0.373265509178923,
-1.16970951353879));
#62227=CARTESIAN_POINT('Ctrl Pts',(0.468395033082173,0.678358960718796,
-1.1539026282207));
#62228=CARTESIAN_POINT('Ctrl Pts',(0.0886296593786528,0.819578898021391,
-1.1380957429026));
#62229=CARTESIAN_POINT('Ctrl Pts',(-0.312546286881678,0.762810333674112,
-1.12228885758451));
#62230=CARTESIAN_POINT('Ctrl Pts',(-0.638219348446799,0.521767045597627,
-1.10648197226642));
#62231=CARTESIAN_POINT('Ctrl Pts',(-0.809715560378535,0.154678692405936,
-1.09067508694833));
#62232=CARTESIAN_POINT('Ctrl Pts',(-0.785605991159775,-0.249775926096571,
-1.07486820163024));
#62233=CARTESIAN_POINT('Ctrl Pts',(-0.571714872596114,-0.593891312494082,
-1.05906131631214));
#62234=CARTESIAN_POINT('Ctrl Pts',(-0.219712620047033,-0.794538325819216,
-1.04325443099405));
#62235=CARTESIAN_POINT('Ctrl Pts',(0.18536636805697,-0.803245974902395,
-1.02744754567596));
#62236=CARTESIAN_POINT('Ctrl Pts',(0.545665763181605,-0.617910722916321,
-1.01164066035787));
#62237=CARTESIAN_POINT('Ctrl Pts',(0.774146797542223,-0.283304646023772,
-0.995833775039777));
#62238=CARTESIAN_POINT('Ctrl Pts',(0.815614519490262,0.119740311508712,
-0.980026889721687));
#62239=CARTESIAN_POINT('Ctrl Pts',(0.660051428385883,0.493859188928676,
-0.964220004403594));
#62240=CARTESIAN_POINT('Ctrl Pts',(0.345037436784345,0.748674798441101,
-0.948413119085503));
#62241=CARTESIAN_POINT('Ctrl Pts',(-0.0533284386772662,0.822630454233114,
-0.93260623376741));
#62242=CARTESIAN_POINT('Ctrl Pts',(-0.43881157924352,0.697860433414406,
-0.916799348449319));
#62243=CARTESIAN_POINT('Ctrl Pts',(-0.718289492868495,0.404505860326217,
-0.900992463131228));
#62244=CARTESIAN_POINT('Ctrl Pts',(-0.824247735858698,0.0134334111581012,
-0.885185577813136));
#62245=CARTESIAN_POINT('Ctrl Pts',(-0.731089609936848,-0.380884193483954,
-0.869378692495045));
#62246=CARTESIAN_POINT('Ctrl Pts',(-0.461319644944187,-0.683190289591489,
-0.853571807176952));
#62247=CARTESIAN_POINT('Ctrl Pts',(-0.0801071019341396,-0.820455750679614,
-0.837764921858862));
#62248=CARTESIAN_POINT('Ctrl Pts',(0.320457190031065,-0.759520885796387,
-0.82195803654077));
#62249=CARTESIAN_POINT('Ctrl Pts',(0.64360753313747,-0.515105940455199,
-0.806151151222677));
#62250=CARTESIAN_POINT('Ctrl Pts',(0.811279384247447,-0.146255076146497,
-0.790344265904585));
#62251=CARTESIAN_POINT('Ctrl Pts',(0.782967675880284,0.257927131434756,
-0.774537380586495));
#62252=CARTESIAN_POINT('Ctrl Pts',(0.565511765091529,0.599800992118718,
-0.758730495268401));
#62253=CARTESIAN_POINT('Ctrl Pts',(0.211443226395748,0.79677885803709,-0.742923609950311));
#62254=CARTESIAN_POINT('Ctrl Pts',(-0.193704381904162,0.801276106616604,
-0.727116724632219));
#62255=CARTESIAN_POINT('Ctrl Pts',(-0.552058154456458,0.612206322003997,
-0.711309839314127));
#62256=CARTESIAN_POINT('Ctrl Pts',(-0.777049334233002,0.27524374429146,
-0.695502953996036));
#62257=CARTESIAN_POINT('Ctrl Pts',(-0.81432602579586,-0.128210414222302,
-0.679696068677944));
#62258=CARTESIAN_POINT('Ctrl Pts',(-0.654883170172903,-0.50069234069219,
-0.663889183359853));
#62259=CARTESIAN_POINT('Ctrl Pts',(-0.337237928017941,-0.752220291211092,
-0.64808229804176));
#62260=CARTESIAN_POINT('Ctrl Pts',(0.0618750437588687,-0.822031791090449,
-0.632275412723669));
#62261=CARTESIAN_POINT('Ctrl Pts',(0.446040647768021,-0.693262235479634,
-0.616468527405576));
#62262=CARTESIAN_POINT('Ctrl Pts',(0.722454673814721,-0.397018930136584,
-0.600661642087485));
#62263=CARTESIAN_POINT('Ctrl Pts',(0.824342832097085,-0.00486639226674949,
-0.584854756769393));
#62264=CARTESIAN_POINT('Ctrl Pts',(0.727091648741029,0.388461736770279,
-0.569047871451302));
#62265=CARTESIAN_POINT('Ctrl Pts',(0.454194427591786,0.68794782400129,-0.55324098613321));
#62266=CARTESIAN_POINT('Ctrl Pts',(0.0715758917604166,0.821243982213708,
-0.537434100815118));
#62267=CARTESIAN_POINT('Ctrl Pts',(-0.328333479154766,0.756149398643979,
-0.521627215497028));
#62268=CARTESIAN_POINT('Ctrl Pts',(-0.648926198877239,0.508389196398115,
-0.505820330178935));
#62269=CARTESIAN_POINT('Ctrl Pts',(-0.812755578172857,0.137815662216995,
-0.490013444860843));
#62270=CARTESIAN_POINT('Ctrl Pts',(-0.780244788732774,-0.266050476900792,
-0.474206559542751));
#62271=CARTESIAN_POINT('Ctrl Pts',(-0.559247574111642,-0.60564588453435,
-0.45839967422466));
#62272=CARTESIAN_POINT('Ctrl Pts',(-0.203150993809032,-0.798933326578804,
-0.442592788906568));
#62273=CARTESIAN_POINT('Ctrl Pts',(0.202021472869058,-0.799219688886387,
-0.426785903588476));
#62274=CARTESIAN_POINT('Ctrl Pts',(0.558390915439125,-0.60643579392732,
-0.410979018270384));
#62275=CARTESIAN_POINT('Ctrl Pts',(0.779867938326921,-0.267153112241133,
-0.395172132952293));
#62276=CARTESIAN_POINT('Ctrl Pts',(0.812949573067638,0.136666668350266,
-0.379365247634201));
#62277=CARTESIAN_POINT('Ctrl Pts',(0.649644175094028,0.507471410420593,
-0.363558362316109));
#62278=CARTESIAN_POINT('Ctrl Pts',(0.329401992628576,0.755684533273304,
-0.347751476998018));
#62279=CARTESIAN_POINT('Ctrl Pts',(-0.0704149653712633,0.821344336594747,
-0.331944591679926));
#62280=CARTESIAN_POINT('Ctrl Pts',(-0.453221537562226,0.688589155153321,
-0.316137706361834));
#62281=CARTESIAN_POINT('Ctrl Pts',(-0.726541818918978,0.389489116166805,
-0.300330821043743));
#62282=CARTESIAN_POINT('Ctrl Pts',(-0.82434888785108,-0.00370115231292693,
-0.284523935725651));
#62283=CARTESIAN_POINT('Ctrl Pts',(-0.723015150118187,-0.395997320460584,
-0.268717050407559));
#62284=CARTESIAN_POINT('Ctrl Pts',(-0.447020152570759,-0.692631050246883,
-0.252910165089467));
#62285=CARTESIAN_POINT('Ctrl Pts',(-0.0630369465961534,-0.821943507128117,
-0.237103279771376));
#62286=CARTESIAN_POINT('Ctrl Pts',(0.336174296148222,-0.752696237081474,
-0.221296394453284));
#62287=CARTESIAN_POINT('Ctrl Pts',(0.65417478556092,-0.501617537571764,
-0.205489509135192));
#62288=CARTESIAN_POINT('Ctrl Pts',(0.81414395454377,-0.129361364859212,
-0.1896826238171));
#62289=CARTESIAN_POINT('Ctrl Pts',(0.777437678945939,0.274145090266998,
-0.173875738499009));
#62290=CARTESIAN_POINT('Ctrl Pts',(0.552922868401512,0.611425348207658,
-0.158068853180917));
#62291=CARTESIAN_POINT('Ctrl Pts',(0.194837029113287,0.801001518694738,
-0.142261967862825));
#62292=CARTESIAN_POINT('Ctrl Pts',(-0.210317155848737,0.797076904759738,
-0.126455082544734));
#62293=CARTESIAN_POINT('Ctrl Pts',(-0.564662553237619,0.600599838466151,
-0.110648197226641));
#62294=CARTESIAN_POINT('Ctrl Pts',(-0.782603888542138,0.25903347409295,
-0.0948413119085497));
#62295=CARTESIAN_POINT('Ctrl Pts',(-0.811482211068061,-0.14510786755727,
-0.0790344265904577));
#62296=CARTESIAN_POINT('Ctrl Pts',(-0.644341077190917,-0.514196238853462,
-0.0632275412723662));
#62297=CARTESIAN_POINT('Ctrl Pts',(-0.321518569789179,-0.759066033017091,
-0.0474206559542749));
#62298=CARTESIAN_POINT('Ctrl Pts',(0.0789236478635419,-0.820570308434437,
-0.0316137706361836));
#62299=CARTESIAN_POINT('Ctrl Pts',(0.460403265087323,-0.68383797063051,
-0.0158068853180922));
#62300=CARTESIAN_POINT('Ctrl Pts',(0.640409690535753,-0.482558394510364,
-0.0052689617726974));
#62301=CARTESIAN_POINT('Ctrl Pts',(0.701077753000062,-0.366509473613416,
0.));
#62302=CARTESIAN_POINT('Ctrl Pts',(0.437168237015807,-0.613060138694078,
-3.9929325805302));
#62303=CARTESIAN_POINT('Ctrl Pts',(0.538647662423237,-0.540695979456381,
-3.9876636187575));
#62304=CARTESIAN_POINT('Ctrl Pts',(0.704883496066505,-0.344682351697352,
-3.9771256952121));
#62305=CARTESIAN_POINT('Ctrl Pts',(0.783933089179612,0.032840050363104,
-3.96131880989402));
#62306=CARTESIAN_POINT('Ctrl Pts',(0.673610636997511,0.402330693317498,
-3.94551192457592));
#62307=CARTESIAN_POINT('Ctrl Pts',(0.400559534442527,0.674677276843038,
-3.92970503925783));
#62308=CARTESIAN_POINT('Ctrl Pts',(0.0307449597249569,0.784015219631683,
-3.91389815393974));
#62309=CARTESIAN_POINT('Ctrl Pts',(-0.34649732625745,0.703968414056769,
-3.89809126862165));
#62310=CARTESIAN_POINT('Ctrl Pts',(-0.640034779676368,0.45385513875008,
-3.88228438330356));
#62311=CARTESIAN_POINT('Ctrl Pts',(-0.778956965558928,0.0941057773502482,
-3.86647749798546));
#62312=CARTESIAN_POINT('Ctrl Pts',(-0.72970375755886,-0.28837870967082,
-3.85067061266738));
#62313=CARTESIAN_POINT('Ctrl Pts',(-0.504173532714486,-0.601197704596164,
-3.83486372734928));
#62314=CARTESIAN_POINT('Ctrl Pts',(-0.156848349405001,-0.768783731612082,
-3.81905684203119));
#62315=CARTESIAN_POINT('Ctrl Pts',(0.228367221059955,-0.750651798042835,
-3.80324995671309));
#62316=CARTESIAN_POINT('Ctrl Pts',(0.558415339094314,-0.55118243382451,
-3.78744307139501));
#62317=CARTESIAN_POINT('Ctrl Pts',(0.753565134802757,-0.218561969600303,
-3.77163618607691));
#62318=CARTESIAN_POINT('Ctrl Pts',(0.766673602657173,0.166857233904678,
-3.75582930075883));
#62319=CARTESIAN_POINT('Ctrl Pts',(0.594574082907553,0.51196817497967,-3.74002241544072));
#62320=CARTESIAN_POINT('Ctrl Pts',(0.278841251218513,0.733401190170503,
-3.72421553012264));
#62321=CARTESIAN_POINT('Ctrl Pts',(-0.104252223602443,0.777663953837329,
-3.70840864480454));
#62322=CARTESIAN_POINT('Ctrl Pts',(-0.462161129046788,0.634063751490217,
-3.69260175948646));
#62323=CARTESIAN_POINT('Ctrl Pts',(-0.708424176301216,0.33729058243504,
-3.67679487416836));
#62324=CARTESIAN_POINT('Ctrl Pts',(-0.783550751452885,-0.040963036679043,
-3.66098798885027));
#62325=CARTESIAN_POINT('Ctrl Pts',(-0.669392268617226,-0.409321073445001,
-3.64518110353218));
#62326=CARTESIAN_POINT('Ctrl Pts',(-0.393526386281157,-0.678798006624954,
-3.62937421821409));
#62327=CARTESIAN_POINT('Ctrl Pts',(-0.0225949772885551,-0.784295363663123,
-3.61356733289599));
#62328=CARTESIAN_POINT('Ctrl Pts',(0.353794778313819,-0.700327784197924,
-3.59776044757791));
#62329=CARTESIAN_POINT('Ctrl Pts',(0.644717108852341,-0.447179606004612,
-3.58195356225981));
#62330=CARTESIAN_POINT('Ctrl Pts',(0.779892903361764,-0.0860047077880307,
-3.56614667694172));
#62331=CARTESIAN_POINT('Ctrl Pts',(0.726667278853556,0.295946644379268,
-3.55033979162363));
#62332=CARTESIAN_POINT('Ctrl Pts',(0.497898133049898,0.60640514475106,-3.53453290630554));
#62333=CARTESIAN_POINT('Ctrl Pts',(0.148850017674368,0.770372262425151,
-3.51872602098745));
#62334=CARTESIAN_POINT('Ctrl Pts',(-0.236156309950195,0.748237895155053,
-3.50291913566935));
#62335=CARTESIAN_POINT('Ctrl Pts',(-0.564113543125074,0.545349118398842,
-3.48711225035126));
#62336=CARTESIAN_POINT('Ctrl Pts',(-0.755795921696723,0.210718473850929,
-3.47130536503317));
#62337=CARTESIAN_POINT('Ctrl Pts',(-0.764898072237769,-0.174816159328638,
-3.45549847971508));
#62338=CARTESIAN_POINT('Ctrl Pts',(-0.589221156842832,-0.518119849845838,
-3.43969159439699));
#62339=CARTESIAN_POINT('Ctrl Pts',(-0.271204053986564,-0.736259540907092,
-3.42388470907889));
#62340=CARTESIAN_POINT('Ctrl Pts',(0.112328747748483,-0.776538474838649,
-3.40807782376081));
#62341=CARTESIAN_POINT('Ctrl Pts',(0.468725906395819,-0.629226330622686,
-3.39227093844271));
#62342=CARTESIAN_POINT('Ctrl Pts',(0.71189133089794,-0.329909811111817,
-3.37646405312462));
#62343=CARTESIAN_POINT('Ctrl Pts',(0.783082710823891,0.0491041595405024,
-3.36065716780653));
#62344=CARTESIAN_POINT('Ctrl Pts',(0.665102098940099,0.416255868980786,
-3.34485028248844));
#62345=CARTESIAN_POINT('Ctrl Pts',(0.386450478650352,0.682851212217119,
-3.32904339717034));
#62346=CARTESIAN_POINT('Ctrl Pts',(0.0144426831167398,0.784487832525058,
-3.31323651185225));
#62347=CARTESIAN_POINT('Ctrl Pts',(-0.36105408119949,0.696613020926732,
-3.29742962653416));
#62348=CARTESIAN_POINT('Ctrl Pts',(-0.649329765612568,0.4404549987967,-3.28162274121607));
#62349=CARTESIAN_POINT('Ctrl Pts',(-0.78074461859055,0.0778947431947184,
-3.26581585589798));
#62350=CARTESIAN_POINT('Ctrl Pts',(-0.723552300765176,-0.303482814229888,
-3.25000897057988));
#62351=CARTESIAN_POINT('Ctrl Pts',(-0.491568957646624,-0.611546981313525,
-3.2342020852618));
#62352=CARTESIAN_POINT('Ctrl Pts',(-0.14083560569182,-0.771877634502317,
-3.2183951999437));
#62353=CARTESIAN_POINT('Ctrl Pts',(0.243919889362559,-0.745743144821882,
-3.20258831462561));
#62354=CARTESIAN_POINT('Ctrl Pts',(0.569750815307017,-0.53945691109899,
-3.18678142930752));
#62355=CARTESIAN_POINT('Ctrl Pts',(0.757945071360682,-0.202852210427999,
-3.17097454398943));
#62356=CARTESIAN_POINT('Ctrl Pts',(0.763039921885615,0.182756198483848,
-3.15516765867133));
#62357=CARTESIAN_POINT('Ctrl Pts',(0.583804586265094,0.524215562084261,
-3.13936077335325));
#62358=CARTESIAN_POINT('Ctrl Pts',(0.26353756282294,0.739038363995279,-3.12355388803515));
#62359=CARTESIAN_POINT('Ctrl Pts',(-0.120393138780939,0.775329118897226,
-3.10774700271706));
#62360=CARTESIAN_POINT('Ctrl Pts',(-0.475240054536119,0.624320943938275,
-3.09194011739896));
#62361=CARTESIAN_POINT('Ctrl Pts',(-0.715281590908346,0.322493404867603,
-3.07613323208088));
#62362=CARTESIAN_POINT('Ctrl Pts',(-0.782530085898503,-0.057239978504147,
-3.06032634676278));
#62363=CARTESIAN_POINT('Ctrl Pts',(-0.6607400885885,-0.423145702811142,
-3.0445194614447));
#62364=CARTESIAN_POINT('Ctrl Pts',(-0.37933282876056,-0.686830659988315,
-3.0287125761266));
#62365=CARTESIAN_POINT('Ctrl Pts',(-0.00628882892598545,-0.784595565311336,
-3.01290569080852));
#62366=CARTESIAN_POINT('Ctrl Pts',(0.368274385006458,-0.692823013347268,
-2.99709880549042));
#62367=CARTESIAN_POINT('Ctrl Pts',(0.65387228533763,-0.433682816056642,
-2.98129192017233));
#62368=CARTESIAN_POINT('Ctrl Pts',(0.781512002073648,-0.0697763648401949,
-2.96548503485424));
#62369=CARTESIAN_POINT('Ctrl Pts',(0.720359168531101,0.310986203534265,
-2.94967814953614));
#62370=CARTESIAN_POINT('Ctrl Pts',(0.485186685664321,0.616622761929485,
-2.93387126421806));
#62371=CARTESIAN_POINT('Ctrl Pts',(0.132805981420619,0.773299632596821,
-2.91806437889996));
#62372=CARTESIAN_POINT('Ctrl Pts',(-0.251657121888123,0.743167843409859,
-2.90225749358187));
#62373=CARTESIAN_POINT('Ctrl Pts',(-0.575326546135049,0.533506434626413,
-2.88645060826377));
#62374=CARTESIAN_POINT('Ctrl Pts',(-0.760012351960777,0.194964036023375,
-2.87064372294569));
#62375=CARTESIAN_POINT('Ctrl Pts',(-0.761099352151827,-0.190676497318213,
-2.85483683762759));
#62376=CARTESIAN_POINT('Ctrl Pts',(-0.578324956322288,-0.530254651436739,
-2.8390299523095));
#62377=CARTESIAN_POINT('Ctrl Pts',(-0.255842605779168,-0.741737360218292,
-2.82322306699141));
#62378=CARTESIAN_POINT('Ctrl Pts',(0.128444525607754,-0.774036016162602,
-2.80741618167332));
#62379=CARTESIAN_POINT('Ctrl Pts',(0.481702869855816,-0.619348121534364,
-2.79160929635523));
#62380=CARTESIAN_POINT('Ctrl Pts',(0.718594590129734,-0.315042164656976,
-2.77580241103714));
#62381=CARTESIAN_POINT('Ctrl Pts',(0.781892936371006,0.0653696147196846,
-2.75999552571904));
#62382=CARTESIAN_POINT('Ctrl Pts',(0.656306708721413,0.429989830766658,
-2.74418864040095));
#62383=CARTESIAN_POINT('Ctrl Pts',(0.372174205421959,0.690735920083795,
-2.72838175508286));
#62384=CARTESIAN_POINT('Ctrl Pts',(-0.0018657045495305,0.784618550393763,
-2.71257486976477));
#62385=CARTESIAN_POINT('Ctrl Pts',(-0.375454909836976,0.688958170830988,
-2.69676798444668));
#62386=CARTESIAN_POINT('Ctrl Pts',(-0.658344177369592,0.426863789280643,
-2.68096109912859));
#62387=CARTESIAN_POINT('Ctrl Pts',(-0.782194970922462,0.0616504496259641,
-2.66515421381049));
#62388=CARTESIAN_POINT('Ctrl Pts',(-0.717088227055958,-0.318456001816918,
-2.6493473284924));
#62389=CARTESIAN_POINT('Ctrl Pts',(-0.478752006480955,-0.621631938341277,
-2.63354044317431));
#62390=CARTESIAN_POINT('Ctrl Pts',(-0.1247620121767,-0.774638103112089,
-2.61773355785622));
#62391=CARTESIAN_POINT('Ctrl Pts',(0.259367171793516,-0.740512269088977,
-2.60192667253812));
#62392=CARTESIAN_POINT('Ctrl Pts',(0.580840133349348,-0.527498331718864,
-2.58611978722004));
#62393=CARTESIAN_POINT('Ctrl Pts',(0.761997540200711,-0.187054802674346,
-2.57031290190194));
#62394=CARTESIAN_POINT('Ctrl Pts',(0.75907657264609,0.19857620032456,-2.55450601658385));
#62395=CARTESIAN_POINT('Ctrl Pts',(0.572782858893946,0.536236465594007,
-2.53869913126576));
#62396=CARTESIAN_POINT('Ctrl Pts',(0.248120014022245,0.744356238045383,
-2.52289224594767));
#62397=CARTESIAN_POINT('Ctrl Pts',(-0.136482038562351,0.772659306308634,
-2.50708536062958));
#62398=CARTESIAN_POINT('Ctrl Pts',(-0.488113654277092,0.614308400547915,
-2.49127847531148));
#62399=CARTESIAN_POINT('Ctrl Pts',(-0.721829970710122,0.307556895321985,
-2.47547158999339));
#62400=CARTESIAN_POINT('Ctrl Pts',(-0.781171331062794,-0.0734921900684592,
-2.4596647046753));
#62401=CARTESIAN_POINT('Ctrl Pts',(-0.651802438208183,-0.436787513582222,
-2.44385781935721));
#62402=CARTESIAN_POINT('Ctrl Pts',(-0.36497538186972,-0.694566570678812,
-2.42805093403912));
#62403=CARTESIAN_POINT('Ctrl Pts',(0.0100200365018897,-0.784556785289615,
-2.41224404872103));
#62404=CARTESIAN_POINT('Ctrl Pts',(0.382594880090186,-0.685018910836956,
-2.39643716340293));
#62405=CARTESIAN_POINT('Ctrl Pts',(0.662744958679239,-0.419998655022524,
-2.38063027808484));
#62406=CARTESIAN_POINT('Ctrl Pts',(0.782793451366445,-0.053517875268758,
-2.36482339276675));
#62407=CARTESIAN_POINT('Ctrl Pts',(0.713739829648883,0.325891402231261,
-2.34901650744866));
#62408=CARTESIAN_POINT('Ctrl Pts',(0.472265615135225,0.626573969485186,
-2.33320962213057));
#62409=CARTESIAN_POINT('Ctrl Pts',(0.116704566825439,0.775892901473883,
-2.31740273681247));
#62410=CARTESIAN_POINT('Ctrl Pts',(-0.267049206281493,0.737776708699793,
-2.30159585149439));
#62411=CARTESIAN_POINT('Ctrl Pts',(-0.586290981402503,0.521433251338619,
-2.28578896617629));
#62412=CARTESIAN_POINT('Ctrl Pts',(-0.763900421651359,0.179125364692859,
-2.2699820808582));
#62413=CARTESIAN_POINT('Ctrl Pts',(-0.756971801857933,-0.206454454220368,
-2.25417519554011));
#62414=CARTESIAN_POINT('Ctrl Pts',(-0.567178892606987,-0.542160358433354,
-2.23836831022202));
#62415=CARTESIAN_POINT('Ctrl Pts',(-0.240370621704116,-0.746894714599756,
-2.22256142490392));
#62416=CARTESIAN_POINT('Ctrl Pts',(0.144504809476721,-0.771199138039956,
-2.20675453958584));
#62417=CARTESIAN_POINT('Ctrl Pts',(0.494471715342225,-0.609202325341912,
-2.19094765426774));
#62418=CARTESIAN_POINT('Ctrl Pts',(0.724987383181469,-0.300038405380308,
-2.17514076894965));
#62419=CARTESIAN_POINT('Ctrl Pts',(0.780365347917708,0.0816068271944897,
-2.15933388363156));
#62420=CARTESIAN_POINT('Ctrl Pts',(0.647227763575373,0.44353801700947,-2.14352699831347));
#62421=CARTESIAN_POINT('Ctrl Pts',(0.357737135681229,0.698322198007528,
-2.12772011299538));
#62422=CARTESIAN_POINT('Ctrl Pts',(-0.0181732861449447,0.784410276670422,
-2.11191322767728));
#62423=CARTESIAN_POINT('Ctrl Pts',(-0.389693524545723,0.681005658862394,
-2.09610634235919));
#62424=CARTESIAN_POINT('Ctrl Pts',(-0.667074153918342,0.413088154816381,
-2.0802994570411));
#62425=CARTESIAN_POINT('Ctrl Pts',(-0.783307378761029,0.045379520204593,
-2.06449257172301));
#62426=CARTESIAN_POINT('Ctrl Pts',(-0.710314337985374,-0.333291601646179,
-2.04868568640492));
#62427=CARTESIAN_POINT('Ctrl Pts',(-0.4657282122515,-0.631448321550146,
-2.03287880108682));
#62428=CARTESIAN_POINT('Ctrl Pts',(-0.108634515687828,-0.777063892145778,
-2.01707191576873));
#62429=CARTESIAN_POINT('Ctrl Pts',(0.274702395580879,-0.734961457722512,
-2.00126503045064));
#62430=CARTESIAN_POINT('Ctrl Pts',(0.591678501523839,-0.515311848602358,
-1.98545814513255));
#62431=CARTESIAN_POINT('Ctrl Pts',(0.765720790773911,-0.171176578573269,
-1.96965125981446));
#62432=CARTESIAN_POINT('Ctrl Pts',(0.75478526713314,0.214310408039895,-1.95384437449637));
#62433=CARTESIAN_POINT('Ctrl Pts',(0.56151366277109,0.548025690088402,-1.93803748917828));
#62434=CARTESIAN_POINT('Ctrl Pts',(0.232595265871588,0.74935251568911,-1.92223060386018));
#62435=CARTESIAN_POINT('Ctrl Pts',(-0.152511971775213,0.769655669075926,
-1.90642371854209));
#62436=CARTESIAN_POINT('Ctrl Pts',(-0.500776366288377,0.604030447446553,
-1.890616833224));
#62437=CARTESIAN_POINT('Ctrl Pts',(-0.728066486497424,0.292487506937937,
-1.87480994790591));
#62438=CARTESIAN_POINT('Ctrl Pts',(-0.779475073993619,-0.0897126495992436,
-1.85900306258782));
#62439=CARTESIAN_POINT('Ctrl Pts',(-0.642583178954215,-0.450240611896095,
-1.84319617726972));
#62440=CARTESIAN_POINT('Ctrl Pts',(-0.350460248692089,-0.7020023964077,
-1.82738929195163));
#62441=CARTESIAN_POINT('Ctrl Pts',(0.0263245728094266,-0.784179040361239,
-1.81158240663354));
#62442=CARTESIAN_POINT('Ctrl Pts',(0.396750076446984,-0.676918848396753,
-1.79577552131545));
#62443=CARTESIAN_POINT('Ctrl Pts',(0.671331295471004,-0.406133035096502,
-1.77996863599736));
#62444=CARTESIAN_POINT('Ctrl Pts',(0.7837366975946,-0.0372362634938868,
-1.76416175067927));
#62445=CARTESIAN_POINT('Ctrl Pts',(0.706812122068224,0.340655800732772,
-1.74835486536117));
#62446=CARTESIAN_POINT('Ctrl Pts',(0.459140503964136,0.63625446803542,-1.73254798004308));
#62447=CARTESIAN_POINT('Ctrl Pts',(0.100552730446469,0.778150948643792,
-1.71674109472499));
#62448=CARTESIAN_POINT('Ctrl Pts',(-0.2823259130362,0.732066820245085,-1.7009342094069));
#62449=CARTESIAN_POINT('Ctrl Pts',(-0.597002111783026,0.509134784710377,
-1.6851273240888));
#62450=CARTESIAN_POINT('Ctrl Pts',(-0.767458450942094,0.163209302899789,
-1.66932043877072));
#62451=CARTESIAN_POINT('Ctrl Pts',(-0.752517204649186,-0.222143213226177,
-1.65351355345262));
#62452=CARTESIAN_POINT('Ctrl Pts',(-0.555787781313246,-0.553831827018249,
-1.63770666813453));
#62453=CARTESIAN_POINT('Ctrl Pts',(-0.224794786375882,-0.751729375835276,
-1.62189978281644));
#62454=CARTESIAN_POINT('Ctrl Pts',(0.160502660568133,-0.768029066133584,
-1.60609289749835));
#62455=CARTESIAN_POINT('Ctrl Pts',(0.50702692612178,-0.598793325499686,
-1.59028601218026));
#62456=CARTESIAN_POINT('Ctrl Pts',(0.731066948070155,-0.284905015601451,
-1.57447912686216));
#62457=CARTESIAN_POINT('Ctrl Pts',(0.778500605453029,0.0978087817363028,
-1.55867224154408));
#62458=CARTESIAN_POINT('Ctrl Pts',(0.637869186027226,0.456894574264609,
-1.54286535622598));
#62459=CARTESIAN_POINT('Ctrl Pts',(0.343145506911666,0.705606768364512,
-1.52705847090789));
#62460=CARTESIAN_POINT('Ctrl Pts',(-0.0344730160381407,0.783863101338944,
-1.5112515855898));
#62461=CARTESIAN_POINT('Ctrl Pts',(-0.403763773584001,0.67275892087484,
-1.49544470027171));
#62462=CARTESIAN_POINT('Ctrl Pts',(-0.675515923504185,0.399134047116708,
-1.47963781495362));
#62463=CARTESIAN_POINT('Ctrl Pts',(-0.784081361494491,0.0290889847265052,
-1.46383092963552));
#62464=CARTESIAN_POINT('Ctrl Pts',(-0.703233560187567,-0.347983204050704,
-1.44802404431743));
#62465=CARTESIAN_POINT('Ctrl Pts',(-0.452503201841199,-0.640991889807458,
-1.43221715899934));
#62466=CARTESIAN_POINT('Ctrl Pts',(-0.0924600840514184,-0.779153953550054,
-1.41641027368125));
#62467=CARTESIAN_POINT('Ctrl Pts',(0.289918935196972,-0.729093108930353,
-1.40060338836316));
#62468=CARTESIAN_POINT('Ctrl Pts',(0.602261237152921,-0.502902726875197,
-1.38479650304507));
#62469=CARTESIAN_POINT('Ctrl Pts',(0.769113214463401,-0.155224398253779,
-1.36898961772697));
#62470=CARTESIAN_POINT('Ctrl Pts',(0.750167859389718,0.229952023722606,
-1.35318273240888));
#62471=CARTESIAN_POINT('Ctrl Pts',(0.550001866711737,0.559578142075867,
-1.33737584709079));
#62472=CARTESIAN_POINT('Ctrl Pts',(0.216970025781956,0.754025038302873,
-1.3215689617727));
#62473=CARTESIAN_POINT('Ctrl Pts',(-0.168476012745165,0.766319504909646,
-1.30576207645461));
#62474=CARTESIAN_POINT('Ctrl Pts',(-0.513222719691291,0.593491525186458,
-1.28995519113651));
#62475=CARTESIAN_POINT('Ctrl Pts',(-0.733988443806282,0.277291750389919,
-1.27414830581842));
#62476=CARTESIAN_POINT('Ctrl Pts',(-0.77744204755268,-0.105894349105939,
-1.25834142050033));
#62477=CARTESIAN_POINT('Ctrl Pts',(-0.633086293974033,-0.463499185390545,
-1.24253453518224));
#62478=CARTESIAN_POINT('Ctrl Pts',(-0.335793700438192,-0.709134924553501,
-1.22672764986415));
#62479=CARTESIAN_POINT('Ctrl Pts',(0.0426177356809889,-0.783462493729533,
-1.21092076454606));
#62480=CARTESIAN_POINT('Ctrl Pts',(0.410733858375728,-0.668526325629188,
-1.19511387922796));
#62481=CARTESIAN_POINT('Ctrl Pts',(0.67962758601734,-0.392091946869246,
-1.17930699390987));
#62482=CARTESIAN_POINT('Ctrl Pts',(0.784341333232005,-0.0209385639267508,
-1.16350010859178));
#62483=CARTESIAN_POINT('Ctrl Pts',(0.699579038879999,0.355273020134108,
-1.14769322327369));
#62484=CARTESIAN_POINT('Ctrl Pts',(0.445817022807615,0.645660075155983,
-1.1318863379556));
#62485=CARTESIAN_POINT('Ctrl Pts',(0.0843574506258922,0.78007279852548,
-1.1160794526375));
#62486=CARTESIAN_POINT('Ctrl Pts',(-0.297480641906641,0.726040644982282,
-1.10027256731942));
#62487=CARTESIAN_POINT('Ctrl Pts',(-0.607455309571685,0.496616348249473,
-1.08446568200132));
#62488=CARTESIAN_POINT('Ctrl Pts',(-0.770684902599366,0.147222727120785,
-1.06865879668323));
#62489=CARTESIAN_POINT('Ctrl Pts',(-0.747737485118111,-0.237735996064363,
-1.05285191136514));
#62490=CARTESIAN_POINT('Ctrl Pts',(-0.544156543929278,-0.56526401457586,
-1.03704502604705));
#62491=CARTESIAN_POINT('Ctrl Pts',(-0.209121829277477,-0.75623925512705,
-1.02123814072896));
#62492=CARTESIAN_POINT('Ctrl Pts',(0.176431167068596,-0.764527170061526,
-1.00543125541086));
#62493=CARTESIAN_POINT('Ctrl Pts',(0.519363077761318,-0.58812561917822,
-0.989624370092773));
#62494=CARTESIAN_POINT('Ctrl Pts',(0.736830658141882,-0.269648533646439,
-0.973817484774679));
#62495=CARTESIAN_POINT('Ctrl Pts',(0.77629951463218,0.113968478349572,-0.95801059945659));
#62496=CARTESIAN_POINT('Ctrl Pts',(0.628235019416367,0.470053731880079,
-0.942203714138496));
#62497=CARTESIAN_POINT('Ctrl Pts',(0.328405623373425,0.712586483882614,
-0.926396828820405));
#62498=CARTESIAN_POINT('Ctrl Pts',(-0.0507578519900923,0.782977260804441,
-0.910589943502312));
#62499=CARTESIAN_POINT('Ctrl Pts',(-0.417659577951879,0.664221519841486,
-0.894783058184222));
#62500=CARTESIAN_POINT('Ctrl Pts',(-0.683665838891269,0.385007495003111,
-0.87897617286613));
#62501=CARTESIAN_POINT('Ctrl Pts',(-0.78451658472642,0.0127858814583185,
-0.863169287548038));
#62502=CARTESIAN_POINT('Ctrl Pts',(-0.695848952886841,-0.362524461577092,
-0.847362402229947));
#62503=CARTESIAN_POINT('Ctrl Pts',(-0.439082689067719,-0.650258519849247,
-0.831555516911854));
#62504=CARTESIAN_POINT('Ctrl Pts',(-0.0762457053718529,-0.780907384321486,
-0.815748631593763));
#62505=CARTESIAN_POINT('Ctrl Pts',(0.305010216391177,-0.722909758111259,
-0.799941746275672));
#62506=CARTESIAN_POINT('Ctrl Pts',(0.612583768004145,-0.490276327853303,
-0.784134860957579));
#62507=CARTESIAN_POINT('Ctrl Pts',(0.772173345584864,-0.139205153797376,
-0.768327975639488));
#62508=CARTESIAN_POINT('Ctrl Pts',(0.745226344350049,0.245494289469506,
-0.752521090321395));
#62509=CARTESIAN_POINT('Ctrl Pts',(0.538252444345531,0.570888830361512,
-0.736714205003304));
#62510=CARTESIAN_POINT('Ctrl Pts',(0.201251044581531,0.758371787140263,
-0.720907319685213));
#62511=CARTESIAN_POINT('Ctrl Pts',(-0.184367264266346,0.762652255187394,
-0.705100434367121));
#62512=CARTESIAN_POINT('Ctrl Pts',(-0.525447337084102,0.582696187070671,
-0.689293549049029));
#62513=CARTESIAN_POINT('Ctrl Pts',(-0.739593284076573,0.261976190949299,
-0.673486663730938));
#62514=CARTESIAN_POINT('Ctrl Pts',(-0.775073130101659,-0.122030297344106,
-0.657679778412846));
#62515=CARTESIAN_POINT('Ctrl Pts',(-0.623315886362265,-0.476557505747101,
-0.641872893094754));
#62516=CARTESIAN_POINT('Ctrl Pts',(-0.320982073736872,-0.715961073533367,
-0.626066007776662));
#62517=CARTESIAN_POINT('Ctrl Pts',(0.0588924857147926,-0.782407454975863,
-0.610259122458571));
#62518=CARTESIAN_POINT('Ctrl Pts',(0.424540184234268,-0.659844968493212,
-0.594452237140478));
#62519=CARTESIAN_POINT('Ctrl Pts',(0.687630245936072,-0.377881456741887,
-0.578645351822387));
#62520=CARTESIAN_POINT('Ctrl Pts',(0.784607097048036,-0.00463181792919246,
-0.562838466504295));
#62521=CARTESIAN_POINT('Ctrl Pts',(0.692043705111493,0.369736745118777,
-0.547031581186203));
#62522=CARTESIAN_POINT('Ctrl Pts',(0.432300928027253,0.654786727188522,
-0.531224695868112));
#62523=CARTESIAN_POINT('Ctrl Pts',(0.0681257244754544,0.781657620790691,
-0.51541781055002));
#62524=CARTESIAN_POINT('Ctrl Pts',(-0.312506845347284,0.719700786498495,
-0.499610925231929));
#62525=CARTESIAN_POINT('Ctrl Pts',(-0.617646058502423,0.483883350500862,
-0.483804039913837));
#62526=CARTESIAN_POINT('Ctrl Pts',(-0.773578382646387,0.131172544297797,
-0.467997154595745));
#62527=CARTESIAN_POINT('Ctrl Pts',(-0.74263470832531,-0.253226065929806,
-0.452190269277653));
#62528=CARTESIAN_POINT('Ctrl Pts',(-0.532290205688612,-0.576451981871085,
-0.436383383959562));
#62529=CARTESIAN_POINT('Ctrl Pts',(-0.193358521853627,-0.760422403998173,
-0.42057649864147));
#62530=CARTESIAN_POINT('Ctrl Pts',(0.19228344712591,-0.760694962805148,
-0.404769613323378));
#62531=CARTESIAN_POINT('Ctrl Pts',(0.531474840469156,-0.577203815321457,
-0.388962728005286));
#62532=CARTESIAN_POINT('Ctrl Pts',(0.742276023211007,-0.254275551022411,
-0.373155842687195));
#62533=CARTESIAN_POINT('Ctrl Pts',(0.773763026419959,0.130078935295337,
-0.357348957369103));
#62534=CARTESIAN_POINT('Ctrl Pts',(0.618329426166053,0.48300980449125,-0.341542072051011));
#62535=CARTESIAN_POINT('Ctrl Pts',(0.313523853347105,0.719258328998049,
-0.32573518673292));
#62536=CARTESIAN_POINT('Ctrl Pts',(-0.0670207581330449,0.781753137797108,
-0.309928301414828));
#62537=CARTESIAN_POINT('Ctrl Pts',(-0.431374934142047,0.655397144303641,
-0.294121416096737));
#62538=CARTESIAN_POINT('Ctrl Pts',(-0.691520378694679,0.370714601824122,
-0.278314530778645));
#62539=CARTESIAN_POINT('Ctrl Pts',(-0.784612860896982,-0.00352274594854401,
-0.262507645460553));
#62540=CARTESIAN_POINT('Ctrl Pts',(-0.688163705642762,-0.376909091639667,
-0.246700760142461));
#62541=CARTESIAN_POINT('Ctrl Pts',(-0.425472474041242,-0.659244208234394,
-0.230893874824369));
#62542=CARTESIAN_POINT('Ctrl Pts',(-0.0599983814376782,-0.782323426558676,
-0.215086989506278));
#62543=CARTESIAN_POINT('Ctrl Pts',(0.319969712033551,-0.716414077421034,
-0.199280104188185));
#62544=CARTESIAN_POINT('Ctrl Pts',(0.622641647960042,-0.477438105431615,
-0.183473218870094));
#62545=CARTESIAN_POINT('Ctrl Pts',(0.774899835216333,-0.123125768794702,
-0.167666333552002));
#62546=CARTESIAN_POINT('Ctrl Pts',(0.739962909438748,0.260930495261506,
-0.151859448233911));
#62547=CARTESIAN_POINT('Ctrl Pts',(0.526270369288404,0.581952858495042,
-0.136052562915819));
#62548=CARTESIAN_POINT('Ctrl Pts',(0.185445314567899,0.762390903206315,
-0.120245677597727));
#62549=CARTESIAN_POINT('Ctrl Pts',(-0.200179253927746,0.758655467139329,
-0.104438792279636));
#62550=CARTESIAN_POINT('Ctrl Pts',(-0.53744416698625,0.57164916997901,-0.0886319069615434));
#62551=CARTESIAN_POINT('Ctrl Pts',(-0.744880092625389,0.246547303176403,
-0.0728250216434516));
#62552=CARTESIAN_POINT('Ctrl Pts',(-0.772366395559619,-0.138113244016823,
-0.0570181363253598));
#62553=CARTESIAN_POINT('Ctrl Pts',(-0.613281953089182,-0.489410476528923,
-0.0412112510072682));
#62554=CARTESIAN_POINT('Ctrl Pts',(-0.306020434541259,-0.722476830566009,
-0.0254043656891769));
#62555=CARTESIAN_POINT('Ctrl Pts',(0.0751192972481202,-0.781016420057536,
-0.00959748037108558));
#62556=CARTESIAN_POINT('Ctrl Pts',(0.438210481399638,-0.650874980768236,
0.00620940494700578));
#62557=CARTESIAN_POINT('Ctrl Pts',(0.609540070766957,-0.459297668798489,
0.0167473284924006));
#62558=CARTESIAN_POINT('Ctrl Pts',(0.667283755215036,-0.34884264523884,
0.022016290265098));
#62559=CARTESIAN_POINT('Ctrl Pts',(0.415028236876535,-0.582012248186926,
-3.9709162902651));
#62560=CARTESIAN_POINT('Ctrl Pts',(0.511368326205958,-0.513312908027891,
-3.9656473284924));
#62561=CARTESIAN_POINT('Ctrl Pts',(0.669185292538236,-0.327226217723212,
-3.95510940494702));
#62562=CARTESIAN_POINT('Ctrl Pts',(0.744231488665138,0.0311768949505003,
-3.93930251962891));
#62563=CARTESIAN_POINT('Ctrl Pts',(0.639496219859735,0.381955009880642,
-3.92349563431083));
#62564=CARTESIAN_POINT('Ctrl Pts',(0.380273549786177,0.640508840670193,
-3.90768874899273));
#62565=CARTESIAN_POINT('Ctrl Pts',(0.0291879083315599,0.744309459692835,
-3.89188186367465));
#62566=CARTESIAN_POINT('Ctrl Pts',(-0.328949274496042,0.668316554050527,
-3.87607497835654));
#62567=CARTESIAN_POINT('Ctrl Pts',(-0.607620782246216,0.430870045176653,
-3.86026809303846));
#62568=CARTESIAN_POINT('Ctrl Pts',(-0.739507376440356,0.089339873180574,
-3.84446120772036));
#62569=CARTESIAN_POINT('Ctrl Pts',(-0.692748553758454,-0.273774024033415,
-3.82865432240228));
#62570=CARTESIAN_POINT('Ctrl Pts',(-0.478640108418349,-0.570750576610951,
-3.81284743708418));
#62571=CARTESIAN_POINT('Ctrl Pts',(-0.148904902961183,-0.729849356962288,
-3.7970405517661));
#62572=CARTESIAN_POINT('Ctrl Pts',(0.216801764382258,-0.712635699191136,
-3.78123366644799));
#62573=CARTESIAN_POINT('Ctrl Pts',(0.530134886310931,-0.523268285155012,
-3.76542678112992));
#62574=CARTESIAN_POINT('Ctrl Pts',(0.715401492578031,-0.20749309124257,
-3.74961989581181));
#62575=CARTESIAN_POINT('Ctrl Pts',(0.727846093628893,0.158406896325021,
-3.73381301049373));
#62576=CARTESIAN_POINT('Ctrl Pts',(0.564462402406145,0.48603999789451,-3.71800612517562));
#62577=CARTESIAN_POINT('Ctrl Pts',(0.26471958176019,0.696258733153591,-3.70219923985755));
#62578=CARTESIAN_POINT('Ctrl Pts',(-0.0989724616031902,0.73827984815802,
-3.68639235453945));
#62579=CARTESIAN_POINT('Ctrl Pts',(-0.438755385913872,0.60195215152099,
-3.67058546922136));
#62580=CARTESIAN_POINT('Ctrl Pts',(-0.672546658142441,0.320208798101702,
-3.65477858390326));
#62581=CARTESIAN_POINT('Ctrl Pts',(-0.743868514095672,-0.0388884997822909,
-3.63897169858518));
#62582=CARTESIAN_POINT('Ctrl Pts',(-0.635491487028924,-0.388591368366378,
-3.62316481326708));
#62583=CARTESIAN_POINT('Ctrl Pts',(-0.373596589215961,-0.644420879723414,
-3.60735792794899));
#62584=CARTESIAN_POINT('Ctrl Pts',(-0.0214506745740397,-0.74457541607666,
-3.5915510426309));
#62585=CARTESIAN_POINT('Ctrl Pts',(0.335877153523394,-0.66486030068283,
-3.57574415731281));
#62586=CARTESIAN_POINT('Ctrl Pts',(0.612065978987051,-0.424532588904725,
-3.55993727199472));
#62587=CARTESIAN_POINT('Ctrl Pts',(0.7403959144979,-0.0816490751478253,
-3.54413038667662));
#62588=CARTESIAN_POINT('Ctrl Pts',(0.689865854841492,0.280958687357274,
-3.52832350135853));
#62589=CARTESIAN_POINT('Ctrl Pts',(0.472682520840011,0.575694290547901,
-3.51251661604043));
#62590=CARTESIAN_POINT('Ctrl Pts',(0.141311639693069,0.731357438032112,
-3.49670973072235));
#62591=CARTESIAN_POINT('Ctrl Pts',(-0.224196381729249,0.71034404628802,
-3.48090284540425));
#62592=CARTESIAN_POINT('Ctrl Pts',(-0.535544509819703,0.51773039284887,
-3.46509596008617));
#62593=CARTESIAN_POINT('Ctrl Pts',(-0.71751930323548,0.200046822423883,
-3.44928907476807));
#62594=CARTESIAN_POINT('Ctrl Pts',(-0.726160483383015,-0.16596274898414,
-3.43348218944998));
#62595=CARTESIAN_POINT('Ctrl Pts',(-0.559380570565075,-0.491880126607821,
-3.41767530413189));
#62596=CARTESIAN_POINT('Ctrl Pts',(-0.257469163652299,-0.69897232523585,
-3.4018684188138));
#62597=CARTESIAN_POINT('Ctrl Pts',(0.106639957300735,-0.737211368051477,
-3.38606153349571));
#62598=CARTESIAN_POINT('Ctrl Pts',(0.444987695898818,-0.597359717570652,
-3.37025464817761));
#62599=CARTESIAN_POINT('Ctrl Pts',(0.675838221749806,-0.313201819438347,
-3.35444776285952));
#62600=CARTESIAN_POINT('Ctrl Pts',(0.743424176971904,0.0466173226502346,
-3.33864087754143));
#62601=CARTESIAN_POINT('Ctrl Pts',(0.631418589214678,0.395174957293065,
-3.32283399222334));
#62602=CARTESIAN_POINT('Ctrl Pts',(0.366879034691962,0.64826881428997,-3.30702710690524));
#62603=CARTESIAN_POINT('Ctrl Pts',(0.013711246156908,0.744758137522683,
-3.29122022158716));
#62604=CARTESIAN_POINT('Ctrl Pts',(-0.342768815411179,0.661333668324127,
-3.27541333626906));
#62605=CARTESIAN_POINT('Ctrl Pts',(-0.616445031810243,0.418148543503261,
-3.25960645095098));
#62606=CARTESIAN_POINT('Ctrl Pts',(-0.741204495359439,0.0739498325649935,
-3.24379956563288));
#62607=CARTESIAN_POINT('Ctrl Pts',(-0.686908632073539,-0.288113194526541,
-3.22799268031479));
#62608=CARTESIAN_POINT('Ctrl Pts',(-0.466673880947885,-0.58057572332855,
-3.2121857949967));
#62609=CARTESIAN_POINT('Ctrl Pts',(-0.133703110543229,-0.732786571866935,
-3.1963789096786));
#62610=CARTESIAN_POINT('Ctrl Pts',(0.231566781503394,-0.707975640387146,
-3.18057202436052));
#62611=CARTESIAN_POINT('Ctrl Pts',(0.54089628731945,-0.512136591195616,
-3.16476513904242));
#62612=CARTESIAN_POINT('Ctrl Pts',(0.719559611108497,-0.192578938980405,
-3.14895825372433));
#62613=CARTESIAN_POINT('Ctrl Pts',(0.72439643741808,0.173500671852947,-3.13315136840623));
#62614=CARTESIAN_POINT('Ctrl Pts',(0.554238317431266,0.497667126871354,
-3.11734448308815));
#62615=CARTESIAN_POINT('Ctrl Pts',(0.250190935178089,0.701610417277384,
-3.10153759777005));
#62616=CARTESIAN_POINT('Ctrl Pts',(-0.114295934355541,0.736063258876045,
-3.08573071245196));
#62617=CARTESIAN_POINT('Ctrl Pts',(-0.451171940746698,0.592702759872339,
-3.06992382713387));
#62618=CARTESIAN_POINT('Ctrl Pts',(-0.679056785029417,0.306161010553175,
-3.05411694181578));
#62619=CARTESIAN_POINT('Ctrl Pts',(-0.7428995392489,-0.0543411102315957,
-3.03831005649768));
#62620=CARTESIAN_POINT('Ctrl Pts',(-0.627277489033615,-0.401715861560274,
-3.0225031711796));
#62621=CARTESIAN_POINT('Ctrl Pts',(-0.3601218519089,-0.652046726435409,
-3.0066962858615));
#62622=CARTESIAN_POINT('Ctrl Pts',(-0.00597033672662238,-0.744860414276931,
-2.99088940054342));
#62623=CARTESIAN_POINT('Ctrl Pts',(0.34962345329424,-0.657735602338842,
-2.97508251522532));
#62624=CARTESIAN_POINT('Ctrl Pts',(0.620757499626612,-0.411719331990554,
-2.95927562990723));
#62625=CARTESIAN_POINT('Ctrl Pts',(0.741933015382239,-0.0662426023284734,
-2.94346874458914));
#62626=CARTESIAN_POINT('Ctrl Pts',(0.68387721320773,0.295236581291443,-2.92766185927104));
#62627=CARTESIAN_POINT('Ctrl Pts',(0.460614833506189,0.585394445507896,
-2.91185497395296));
#62628=CARTESIAN_POINT('Ctrl Pts',(0.12608013951769,0.734136554120982,-2.89604808863486));
#62629=CARTESIAN_POINT('Ctrl Pts',(-0.238912168705604,0.705530762845827,
-2.88024120331678));
#62630=CARTESIAN_POINT('Ctrl Pts',(-0.546189640172924,0.506487471360546,
-2.86443431799868));
#62631=CARTESIAN_POINT('Ctrl Pts',(-0.721522196104249,0.185090254217592,
-2.84862743268059));
#62632=CARTESIAN_POINT('Ctrl Pts',(-0.722554146128466,-0.181019854132062,
-2.83282054736249));
#62633=CARTESIAN_POINT('Ctrl Pts',(-0.549036198518368,-0.503400371865109,
-2.81701366204441));
#62634=CARTESIAN_POINT('Ctrl Pts',(-0.242885682453148,-0.704172725214985,
-2.80120677672631));
#62635=CARTESIAN_POINT('Ctrl Pts',(0.121939565791243,-0.73483564418996,
-2.78539989140822));
#62636=CARTESIAN_POINT('Ctrl Pts',(0.457307452479438,-0.587981781677116,
-2.76959300609013));
#62637=CARTESIAN_POINT('Ctrl Pts',(0.682202000324592,-0.299087131837123,
-2.75378612077204));
#62638=CARTESIAN_POINT('Ctrl Pts',(0.742294657597777,0.0620590281846798,
-2.73797923545394));
#62639=CARTESIAN_POINT('Ctrl Pts',(0.623068633783288,0.408213374686398,
-2.72217235013586));
#62640=CARTESIAN_POINT('Ctrl Pts',(0.353325770741238,0.655754208074595,
-2.70636546481776));
#62641=CARTESIAN_POINT('Ctrl Pts',(-0.00177121758664689,0.744882235300112,
-2.69055857949967));
#62642=CARTESIAN_POINT('Ctrl Pts',(-0.356440326772058,0.654066491366174,
-2.67475169418158));
#62643=CARTESIAN_POINT('Ctrl Pts',(-0.625002916627162,0.405245648816827,
-2.65894480886349));
#62644=CARTESIAN_POINT('Ctrl Pts',(-0.742581395875524,0.0585282169298649,
-2.64313792354539));
#62645=CARTESIAN_POINT('Ctrl Pts',(-0.680771925681304,-0.302328078222316,
-2.62733103822731));
#62646=CARTESIAN_POINT('Ctrl Pts',(-0.454506032979947,-0.590149936594305,
-2.61152415290921));
#62647=CARTESIAN_POINT('Ctrl Pts',(-0.118443550007935,-0.735407238976439,
-2.59571726759112));
#62648=CARTESIAN_POINT('Ctrl Pts',(0.246231749927488,-0.703009677746384,
-2.57991038227302));
#62649=CARTESIAN_POINT('Ctrl Pts',(0.551423996621224,-0.500783643530524,
-2.56410349695494));
#62650=CARTESIAN_POINT('Ctrl Pts',(0.723406846235083,-0.177581577022058,
-2.54829661163684));
#62651=CARTESIAN_POINT('Ctrl Pts',(0.720633808508361,0.188519483640722,
-2.53248972631875));
#62652=CARTESIAN_POINT('Ctrl Pts',(0.543774775730693,0.509079242315443,
-2.51668284100066));
#62653=CARTESIAN_POINT('Ctrl Pts',(0.235554194550753,0.706658972282229,
-2.50087595568257));
#62654=CARTESIAN_POINT('Ctrl Pts',(-0.129570025984758,0.733528656593414,
-2.48506907036448));
#62655=CARTESIAN_POINT('Ctrl Pts',(-0.463393568372761,0.583197292919119,
-2.46926218504639));
#62656=CARTESIAN_POINT('Ctrl Pts',(-0.685273527906441,0.291980947371725,
-2.4534552997283));
#62657=CARTESIAN_POINT('Ctrl Pts',(-0.741609597354536,-0.0697702428623754,
-2.4376484144102));
#62658=CARTESIAN_POINT('Ctrl Pts',(-0.618792478081121,-0.414666794845758,
-2.42184152909211));
#62659=CARTESIAN_POINT('Ctrl Pts',(-0.346491525264335,-0.659390858745725,
-2.40603464377402));
#62660=CARTESIAN_POINT('Ctrl Pts',(0.00951258058272212,-0.744823598235237,
-2.39022775845593));
#62661=CARTESIAN_POINT('Ctrl Pts',(0.363218699523402,-0.650326731723339,
-2.37442087313784));
#62662=CARTESIAN_POINT('Ctrl Pts',(0.629180824245266,-0.398728193233784,
-2.35861398781975));
#62663=CARTESIAN_POINT('Ctrl Pts',(0.743149566804792,-0.0508075096347088,
-2.34280710250165));
#62664=CARTESIAN_POINT('Ctrl Pts',(0.677593104910366,0.309386919334609,
-2.32700021718356));
#62665=CARTESIAN_POINT('Ctrl Pts',(0.448348139208236,0.594841682925754,
-2.31119333186547));
#62666=CARTESIAN_POINT('Ctrl Pts',(0.11079416687642,0.736598489180904,-2.29538644654737));
#62667=CARTESIAN_POINT('Ctrl Pts',(-0.253524734548086,0.700412657402587,
-2.27957956122929));
#62668=CARTESIAN_POINT('Ctrl Pts',(-0.55659879127791,0.495025723801701,
-2.26377267591119));
#62669=CARTESIAN_POINT('Ctrl Pts',(-0.725213357931446,0.170053718439873,
-2.24796579059311));
#62670=CARTESIAN_POINT('Ctrl Pts',(-0.718635631982085,-0.195998750310146,
-2.23215890527501));
#62671=CARTESIAN_POINT('Ctrl Pts',(-0.538454617378229,-0.514703124821964,
-2.21635201995692));
#62672=CARTESIAN_POINT('Ctrl Pts',(-0.228197263377957,-0.709068889928362,
-2.20054513463883));
#62673=CARTESIAN_POINT('Ctrl Pts',(0.137186490735684,-0.732142437260031,
-2.18473824932073));
#62674=CARTESIAN_POINT('Ctrl Pts',(0.469429631037854,-0.578349810392547,
-2.16893136400265));
#62675=CARTESIAN_POINT('Ctrl Pts',(0.68827103600543,-0.284843224727992,
-2.15312447868455));
#62676=CARTESIAN_POINT('Ctrl Pts',(0.740844432515615,0.0774739213416226,
-2.13731759336646));
#62677=CARTESIAN_POINT('Ctrl Pts',(0.614449483813974,0.421075424975349,
-2.12151070804837));
#62678=CARTESIAN_POINT('Ctrl Pts',(0.339619853675854,0.662956285637765,
-2.10570382273028));
#62679=CARTESIAN_POINT('Ctrl Pts',(-0.0172529160820942,0.744684509415964,
-2.08989693741218));
#62680=CARTESIAN_POINT('Ctrl Pts',(-0.369957839385679,0.646516727358626,
-2.07409005209409));
#62681=CARTESIAN_POINT('Ctrl Pts',(-0.633290771206291,0.392167669221179,
-2.058283166776));
#62682=CARTESIAN_POINT('Ctrl Pts',(-0.743637466799339,0.0430813143914036,
-2.04247628145791));
#62683=CARTESIAN_POINT('Ctrl Pts',(-0.674341094253676,-0.316412342171074,
-2.02666939613982));
#62684=CARTESIAN_POINT('Ctrl Pts',(-0.44214181733292,-0.599469177725571,
-2.01086251082173));
#62685=CARTESIAN_POINT('Ctrl Pts',(-0.103132816367497,-0.737710176062076,
-1.99505562550363));
#62686=CARTESIAN_POINT('Ctrl Pts',(0.26079033481925,-0.697739982330304,
-1.97924874018554));
#62687=CARTESIAN_POINT('Ctrl Pts',(0.561713465190083,-0.489214334112953,
-1.96344185486745));
#62688=CARTESIAN_POINT('Ctrl Pts',(0.72694153606386,-0.162507491588989,
-1.94763496954936));
#62689=CARTESIAN_POINT('Ctrl Pts',(0.716559832381698,0.203456846271001,
-1.93182808423127));
#62690=CARTESIAN_POINT('Ctrl Pts',(0.533076298115275,0.520271411923761,
-1.91602119891318));
#62691=CARTESIAN_POINT('Ctrl Pts',(0.220815683590071,0.711402217847316,
-1.90021431359509));
#62692=CARTESIAN_POINT('Ctrl Pts',(-0.14478813735533,0.730677135921608,
-1.88440742827699));
#62693=CARTESIAN_POINT('Ctrl Pts',(-0.475414988492377,0.573439857695838,
-1.8686005429589));
#62694=CARTESIAN_POINT('Ctrl Pts',(-0.691194200847195,0.277674734883526,
-1.85279365764081));
#62695=CARTESIAN_POINT('Ctrl Pts',(-0.739999245729919,-0.0851692315133856,
-1.83698677232272));
#62696=CARTESIAN_POINT('Ctrl Pts',(-0.610040120088232,-0.42743857285014,
-1.82117988700463));
#62697=CARTESIAN_POINT('Ctrl Pts',(-0.332711498216024,-0.666450103632882,
-1.80537300168654));
#62698=CARTESIAN_POINT('Ctrl Pts',(0.0249913880162134,-0.744464983865897,
-1.78956611636844));
#62699=CARTESIAN_POINT('Ctrl Pts',(0.376657018434001,-0.642636889807798,
-1.77375923105035));
#62700=CARTESIAN_POINT('Ctrl Pts',(0.63733231357633,-0.385564785410793,
-1.75795234573226));
#62701=CARTESIAN_POINT('Ctrl Pts',(0.744045043158892,-0.0353504657411277,
-1.74214546041417));
#62702=CARTESIAN_POINT('Ctrl Pts',(0.671016244975565,0.323403587884121,
-1.72633857509608));
#62703=CARTESIAN_POINT('Ctrl Pts',(0.435887737726806,0.604031921157183,
-1.71053168977799));
#62704=CARTESIAN_POINT('Ctrl Pts',(0.0954603260181704,0.738742179541641,
-1.69472480445989));
#62705=CARTESIAN_POINT('Ctrl Pts',(-0.268027765950747,0.694991941217221,
-1.6789179191418));
#62706=CARTESIAN_POINT('Ctrl Pts',(-0.566767465898757,0.48335010217867,
-1.6631110338237));
#62707=CARTESIAN_POINT('Ctrl Pts',(-0.72859119396402,0.15494371157138,-1.64730414850562));
#62708=CARTESIAN_POINT('Ctrl Pts',(-0.714406633923669,-0.210892965940744,
-1.63149726318752));
#62709=CARTESIAN_POINT('Ctrl Pts',(-0.527640398878327,-0.525783502165053,
-1.61569037786944));
#62710=CARTESIAN_POINT('Ctrl Pts',(-0.21341025250479,-0.713658704005824,
-1.59988349255134));
#62711=CARTESIAN_POINT('Ctrl Pts',(0.152374144755576,-0.729132910851949,
-1.58407660723325));
#62712=CARTESIAN_POINT('Ctrl Pts',(0.481348994230894,-0.568467965175117,
-1.56826972191516));
#62713=CARTESIAN_POINT('Ctrl Pts',(0.694042706687525,-0.270476252139228,
-1.55246283659707));
#62714=CARTESIAN_POINT('Ctrl Pts',(0.739074128289886,0.0928553421725219,
-1.53665595127898));
#62715=CARTESIAN_POINT('Ctrl Pts',(0.605564863179149,0.433755551157848,
-1.52084906596088));
#62716=CARTESIAN_POINT('Ctrl Pts',(0.325767205087459,0.669871935348046,
-1.50504218064279));
#62717=CARTESIAN_POINT('Ctrl Pts',(-0.0327271605178637,0.744165045296987,
-1.4892352953247));
#62718=CARTESIAN_POINT('Ctrl Pts',(-0.383315513059851,0.638687638149583,
-1.47342841000661));
#62719=CARTESIAN_POINT('Ctrl Pts',(-0.641305014810186,0.378920255009859,
-1.45762152468852));
#62720=CARTESIAN_POINT('Ctrl Pts',(-0.744372251859284,0.0276157987276915,
-1.44181463937042));
#62721=CARTESIAN_POINT('Ctrl Pts',(-0.667618916207993,-0.330359901317784,
-1.42600775405234));
#62722=CARTESIAN_POINT('Ctrl Pts',(-0.42958657592122,-0.608529420378104,
-1.41020086873424));
#62723=CARTESIAN_POINT('Ctrl Pts',(-0.0877775245687094,-0.739694388148254,
-1.39439398341615));
#62724=CARTESIAN_POINT('Ctrl Pts',(0.275236246195013,-0.692168830891646,
-1.37858709809806));
#62725=CARTESIAN_POINT('Ctrl Pts',(0.571760247498537,-0.47743366142098,
-1.36278021277997));
#62726=CARTESIAN_POINT('Ctrl Pts',(0.730162153444936,-0.14736319538502,
-1.34697332746187));
#62727=CARTESIAN_POINT('Ctrl Pts',(0.712176269184669,0.218306306110557,
-1.33116644214378));
#62728=CARTESIAN_POINT('Ctrl Pts',(0.522147506823372,0.531238800160123,
-1.31535955682569));
#62729=CARTESIAN_POINT('Ctrl Pts',(0.205981770016112,0.715838104670642,
-1.2995526715076));
#62730=CARTESIAN_POINT('Ctrl Pts',(-0.159943693537569,0.727509928849765,
-1.28374578618951));
#62731=CARTESIAN_POINT('Ctrl Pts',(-0.487231007294692,0.563434669866906,
-1.26793890087142));
#62732=CARTESIAN_POINT('Ctrl Pts',(-0.696816245846464,0.26324855403567,
-1.25213201555333));
#62733=CARTESIAN_POINT('Ctrl Pts',(-0.738069180121617,-0.100531423107573,
-1.23632513023523));
#62734=CARTESIAN_POINT('Ctrl Pts',(-0.601024196479397,-0.440025677573168,
-1.22051824491714));
#62735=CARTESIAN_POINT('Ctrl Pts',(-0.31878772437456,-0.673221411175788,
-1.20471135959905));
#62736=CARTESIAN_POINT('Ctrl Pts',(0.040459398011372,-0.743784726106948,
-1.18890447428096));
#62737=CARTESIAN_POINT('Ctrl Pts',(0.389932604049209,-0.634669398960461,
-1.17309758896287));
#62738=CARTESIAN_POINT('Ctrl Pts',(0.64520844579848,-0.372234795724066,
-1.15729070364477));
#62739=CARTESIAN_POINT('Ctrl Pts',(0.744619057557235,-0.019878148807343,
-1.14148381832669));
#62740=CARTESIAN_POINT('Ctrl Pts',(0.66414947491175,0.337280531089292,-1.12567693300859));
#62741=CARTESIAN_POINT('Ctrl Pts',(0.423239012533058,0.612961189593169,
-1.1098700476905));
#62742=CARTESIAN_POINT('Ctrl Pts',(0.0800852418731312,0.740566699029569,
-1.09406316237241));
#62743=CARTESIAN_POINT('Ctrl Pts',(-0.282414996931603,0.68927095629045,
-1.07825627705432));
#62744=CARTESIAN_POINT('Ctrl Pts',(-0.576691270696571,0.471465650901319,
-1.06244939173622));
#62745=CARTESIAN_POINT('Ctrl Pts',(-0.731654244820196,0.139766761835634,
-1.04664250641813));
#62746=CARTESIAN_POINT('Ctrl Pts',(-0.709868979076448,-0.225696066032155,
-1.03083562110004));
#62747=CARTESIAN_POINT('Ctrl Pts',(-0.516598215262442,-0.536636716657638,
-1.01502873578195));
#62748=CARTESIAN_POINT('Ctrl Pts',(-0.19853103850792,-0.717940184434885,
-0.999221850463857));
#62749=CARTESIAN_POINT('Ctrl Pts',(0.167495966080221,-0.725808365220657,
-0.983414965145765));
#62750=CARTESIAN_POINT('Ctrl Pts',(0.49306039234103,-0.558340515440121,
-0.967608079827675));
#62751=CARTESIAN_POINT('Ctrl Pts',(0.699514518741541,-0.255992421269104,
-0.951801194509581));
#62752=CARTESIAN_POINT('Ctrl Pts',(0.736984509774098,0.108196645190432,
-0.935994309191491));
#62753=CARTESIAN_POINT('Ctrl Pts',(0.596418610446852,0.446248274831483,
-0.920187423873398));
#62754=CARTESIAN_POINT('Ctrl Pts',(0.311773809962505,0.676498169324127,
-0.904380538555308));
#62755=CARTESIAN_POINT('Ctrl Pts',(-0.0481872653029185,0.743324067375768,
-0.888573653237214));
#62756=CARTESIAN_POINT('Ctrl Pts',(-0.396507576660238,0.630582606268565,
-0.872766767919124));
#62757=CARTESIAN_POINT('Ctrl Pts',(-0.649042184914044,0.365509129680006,
-0.856959882601032));
#62758=CARTESIAN_POINT('Ctrl Pts',(-0.744785433594142,0.0121383517585348,
-0.841152997282939));
#62759=CARTESIAN_POINT('Ctrl Pts',(-0.660608295836836,-0.344164729670229,
-0.825346111964851));
#62760=CARTESIAN_POINT('Ctrl Pts',(-0.41684573319125,-0.617326750107006,
-0.809539226646754));
#62761=CARTESIAN_POINT('Ctrl Pts',(-0.0723843088095669,-0.741359017963356,
-0.793732341328667));
#62762=CARTESIAN_POINT('Ctrl Pts',(0.28956324275129,-0.686298630426134,
-0.777925456010572));
#62763=CARTESIAN_POINT('Ctrl Pts',(0.581560002870819,-0.465446715251406,
-0.762118570692483));
#62764=CARTESIAN_POINT('Ctrl Pts',(0.733067306922282,-0.132155231448256,
-0.746311685374389));
#62765=CARTESIAN_POINT('Ctrl Pts',(0.707485012819814,0.233061447504257,
-0.730504800056298));
#62766=CARTESIAN_POINT('Ctrl Pts',(0.510993123599533,0.541976668604306,
-0.714697914738206));
#62767=CARTESIAN_POINT('Ctrl Pts',(0.191058862767314,0.719964716243436,
-0.698891029420114));
#62768=CARTESIAN_POINT('Ctrl Pts',(-0.175030146628531,0.724028403758185,
-0.683084144102023));
#62769=CARTESIAN_POINT('Ctrl Pts',(-0.498836519711745,0.553186052137345,
-0.667277258783931));
#62770=CARTESIAN_POINT('Ctrl Pts',(-0.702137233920144,0.248708637607138,
-0.65147037346584));
#62771=CARTESIAN_POINT('Ctrl Pts',(-0.735820234407457,-0.11585018046591,
-0.635663488147748));
#62772=CARTESIAN_POINT('Ctrl Pts',(-0.591748602551628,-0.452422670802011,
-0.619856602829656));
#62773=CARTESIAN_POINT('Ctrl Pts',(-0.304726219455804,-0.679701855855642,
-0.604049717511565));
#62774=CARTESIAN_POINT('Ctrl Pts',(0.0559099276707165,-0.742783118861276,
-0.588242832193472));
#62775=CARTESIAN_POINT('Ctrl Pts',(0.403039720700516,-0.62642770150679,
-0.57243594687538));
#62776=CARTESIAN_POINT('Ctrl Pts',(0.652805818057422,-0.358743983347191,
-0.55662906155729));
#62777=CARTESIAN_POINT('Ctrl Pts',(0.744871361998988,-0.00439724359163508,
-0.540822176239196));
#62778=CARTESIAN_POINT('Ctrl Pts',(0.656995761481957,0.351011753467274,
-0.525015290921106));
#62779=CARTESIAN_POINT('Ctrl Pts',(0.410407428462719,0.621625630375753,
-0.509208405603014));
#62780=CARTESIAN_POINT('Ctrl Pts',(0.0646755571904924,0.742071259367674,
-0.493401520284922));
#62781=CARTESIAN_POINT('Ctrl Pts',(-0.296680211539802,0.683252174353012,
-0.477594634966831));
#62782=CARTESIAN_POINT('Ctrl Pts',(-0.586365918127607,0.459377504603609,
-0.461787749648739));
#62783=CARTESIAN_POINT('Ctrl Pts',(-0.734401187119916,0.124529426378599,
-0.445980864330647));
#62784=CARTESIAN_POINT('Ctrl Pts',(-0.705024627917847,-0.240401654958819,
-0.430173979012555));
#62785=CARTESIAN_POINT('Ctrl Pts',(-0.505332837265582,-0.547258079207822,
-0.414367093694464));
#62786=CARTESIAN_POINT('Ctrl Pts',(-0.183566049898222,-0.721911481417541,
-0.398560208376372));
#62787=CARTESIAN_POINT('Ctrl Pts',(0.182545421382762,-0.722170236723908,
-0.38275332305828));
#62788=CARTESIAN_POINT('Ctrl Pts',(0.504558765499186,-0.547971836715596,
-0.366946437740188));
#62789=CARTESIAN_POINT('Ctrl Pts',(0.704684108095094,-0.241397989803689,
-0.351139552422097));
#62790=CARTESIAN_POINT('Ctrl Pts',(0.734576479772278,0.123491202240409,
-0.335332667104005));
#62791=CARTESIAN_POINT('Ctrl Pts',(0.587014677238078,0.458548198561907,
-0.319525781785913));
#62792=CARTESIAN_POINT('Ctrl Pts',(0.297645714065633,0.682832124722794,
-0.303718896467822));
#62793=CARTESIAN_POINT('Ctrl Pts',(-0.0636265508948266,0.742161938999467,
-0.28791201114973));
#62794=CARTESIAN_POINT('Ctrl Pts',(-0.409528330721868,0.622205133453962,
-0.272105125831639));
#62795=CARTESIAN_POINT('Ctrl Pts',(-0.656498938470381,0.351940087481438,
-0.256298240513547));
#62796=CARTESIAN_POINT('Ctrl Pts',(-0.744876833942882,-0.00334433958416066,
-0.240491355195455));
#62797=CARTESIAN_POINT('Ctrl Pts',(-0.653312261167338,-0.35782086281875,
-0.224684469877363));
#62798=CARTESIAN_POINT('Ctrl Pts',(-0.403924795511725,-0.625857366221906,
-0.208877584559271));
#62799=CARTESIAN_POINT('Ctrl Pts',(-0.0569598162792036,-0.742703345989235,
-0.19307069924118));
#62800=CARTESIAN_POINT('Ctrl Pts',(0.30376512791888,-0.680131917760592,
-0.177263813923087));
#62801=CARTESIAN_POINT('Ctrl Pts',(0.591108510359164,-0.453258673291466,
-0.161456928604996));
#62802=CARTESIAN_POINT('Ctrl Pts',(0.735655715888896,-0.116890172730191,
-0.145650043286904));
#62803=CARTESIAN_POINT('Ctrl Pts',(0.702488139931555,0.247715900256012,
-0.129843157968813));
#62804=CARTESIAN_POINT('Ctrl Pts',(0.499617870175296,0.552480368782428,
-0.114036272650721));
#62805=CARTESIAN_POINT('Ctrl Pts',(0.176053600022512,0.72378028771789,-0.0982293873326291));
#62806=CARTESIAN_POINT('Ctrl Pts',(-0.190041352006756,0.720234029518921,
-0.0824225020145375));
#62807=CARTESIAN_POINT('Ctrl Pts',(-0.510225780734878,0.542698501491867,
-0.0666156166964455));
#62808=CARTESIAN_POINT('Ctrl Pts',(-0.707156296708642,0.234061132259856,
-0.0508087313783536));
#62809=CARTESIAN_POINT('Ctrl Pts',(-0.733250580051175,-0.131118620476376,
-0.0350018460602618));
#62810=CARTESIAN_POINT('Ctrl Pts',(-0.582222828987448,-0.464624714204384,
-0.0191949607421702));
#62811=CARTESIAN_POINT('Ctrl Pts',(-0.290522299293338,-0.685887628114927,
-0.00338807542407897));
#62812=CARTESIAN_POINT('Ctrl Pts',(0.0713149466326984,-0.741462531680634,
0.0124188098940124));
#62813=CARTESIAN_POINT('Ctrl Pts',(0.416017697711953,-0.617911990905962,
0.0282256952121038));
#62814=CARTESIAN_POINT('Ctrl Pts',(0.57867045099816,-0.436036943086615,
0.0387636187574986));
#62815=CARTESIAN_POINT('Ctrl Pts',(0.63348975743001,-0.331175816864263,
0.044032580530196));
#62816=CARTESIAN_POINT('Ctrl Pts',(0.392888236737263,-0.550964357679773,
-3.9489));
#62817=CARTESIAN_POINT('Ctrl Pts',(0.484088989988678,-0.485929836599401,
-3.9436310382273));
#62818=CARTESIAN_POINT('Ctrl Pts',(0.633487089009969,-0.309770083749072,
-3.93309311468191));
#62819=CARTESIAN_POINT('Ctrl Pts',(0.704529888150662,0.0295137395378967,
-3.91728622936382));
#62820=CARTESIAN_POINT('Ctrl Pts',(0.605381802721961,0.361579326443786,
-3.90147934404573));
#62821=CARTESIAN_POINT('Ctrl Pts',(0.359987565129825,0.606340404497349,
-3.88567245872763));
#62822=CARTESIAN_POINT('Ctrl Pts',(0.0276308569381634,0.704603699753987,
-3.86986557340955));
#62823=CARTESIAN_POINT('Ctrl Pts',(-0.311401222734635,0.632664694044287,
-3.85405868809145));
#62824=CARTESIAN_POINT('Ctrl Pts',(-0.575206784816063,0.407884951603224,
-3.83825180277336));
#62825=CARTESIAN_POINT('Ctrl Pts',(-0.700057787321786,0.0845739690108998,
-3.82244491745527));
#62826=CARTESIAN_POINT('Ctrl Pts',(-0.655793349958048,-0.25916933839601,
-3.80663803213718));
#62827=CARTESIAN_POINT('Ctrl Pts',(-0.453106684122212,-0.54030344862574,
-3.79083114681908));
#62828=CARTESIAN_POINT('Ctrl Pts',(-0.140961456517365,-0.690914982312493,
-3.775024261501));
#62829=CARTESIAN_POINT('Ctrl Pts',(0.205236307704561,-0.674619600339438,
-3.7592173761829));
#62830=CARTESIAN_POINT('Ctrl Pts',(0.501854433527548,-0.495354136485513,
-3.74341049086481));
#62831=CARTESIAN_POINT('Ctrl Pts',(0.677237850353305,-0.196424212884838,
-3.72760360554672));
#62832=CARTESIAN_POINT('Ctrl Pts',(0.689018584600613,0.149956558745365,
-3.71179672022863));
#62833=CARTESIAN_POINT('Ctrl Pts',(0.534350721904737,0.46011182080935,-3.69598983491053));
#62834=CARTESIAN_POINT('Ctrl Pts',(0.250597912301867,0.659116276136679,
-3.68018294959245));
#62835=CARTESIAN_POINT('Ctrl Pts',(-0.0936926996039382,0.698895742478711,
-3.66437606427435));
#62836=CARTESIAN_POINT('Ctrl Pts',(-0.415349642780955,0.569840551551763,
-3.64856917895626));
#62837=CARTESIAN_POINT('Ctrl Pts',(-0.636669139983667,0.303127013768365,
-3.63276229363816));
#62838=CARTESIAN_POINT('Ctrl Pts',(-0.704186276738458,-0.0368139628855383,
-3.61695540832008));
#62839=CARTESIAN_POINT('Ctrl Pts',(-0.601590705440622,-0.367861663287755,
-3.60114852300198));
#62840=CARTESIAN_POINT('Ctrl Pts',(-0.353666792150765,-0.610043752821873,
-3.58534163768389));
#62841=CARTESIAN_POINT('Ctrl Pts',(-0.0203063718595239,-0.704855468490197,
-3.56953475236579));
#62842=CARTESIAN_POINT('Ctrl Pts',(0.317959528732968,-0.629392817167735,
-3.55372786704772));
#62843=CARTESIAN_POINT('Ctrl Pts',(0.579414849121761,-0.401885571804838,
-3.53792098172961));
#62844=CARTESIAN_POINT('Ctrl Pts',(0.700898925634034,-0.0772934425076206,
-3.52211409641153));
#62845=CARTESIAN_POINT('Ctrl Pts',(0.653064430829429,0.265970730335282,
-3.50630721109343));
#62846=CARTESIAN_POINT('Ctrl Pts',(0.447466908630123,0.544983436344741,
-3.49050032577534));
#62847=CARTESIAN_POINT('Ctrl Pts',(0.13377326171177,0.692342613639074,-3.47469344045725));
#62848=CARTESIAN_POINT('Ctrl Pts',(-0.212236453508304,0.672450197420986,
-3.45888655513916));
#62849=CARTESIAN_POINT('Ctrl Pts',(-0.506975476514332,0.490111667298897,
-3.44307966982107));
#62850=CARTESIAN_POINT('Ctrl Pts',(-0.679242684774237,0.189375170996836,
-3.42727278450297));
#62851=CARTESIAN_POINT('Ctrl Pts',(-0.687422894528262,-0.157109338639641,
-3.41146589918489));
#62852=CARTESIAN_POINT('Ctrl Pts',(-0.529539984287318,-0.465640403369804,
-3.39565901386679));
#62853=CARTESIAN_POINT('Ctrl Pts',(-0.243734273318034,-0.661685109564608,
-3.3798521285487));
#62854=CARTESIAN_POINT('Ctrl Pts',(0.100951166852987,-0.697884261264305,
-3.36404524323061));
#62855=CARTESIAN_POINT('Ctrl Pts',(0.421249485401818,-0.565493104518617,
-3.34823835791252));
#62856=CARTESIAN_POINT('Ctrl Pts',(0.639785112601671,-0.296493827764879,
-3.33243147259443));
#62857=CARTESIAN_POINT('Ctrl Pts',(0.703765643119916,0.0441304857599676,
-3.31662458727633));
#62858=CARTESIAN_POINT('Ctrl Pts',(0.597735079489259,0.374094045605343,
-3.30081770195824));
#62859=CARTESIAN_POINT('Ctrl Pts',(0.347307590733571,0.613686416362823,
-3.28501081664015));
#62860=CARTESIAN_POINT('Ctrl Pts',(0.0129798091970768,0.705028442520307,
-3.26920393132206));
#62861=CARTESIAN_POINT('Ctrl Pts',(-0.324483549622869,0.626054315721524,
-3.25339704600396));
#62862=CARTESIAN_POINT('Ctrl Pts',(-0.583560298007917,0.395842088209822,
-3.23759016068587));
#62863=CARTESIAN_POINT('Ctrl Pts',(-0.701664372128327,0.0700049219352693,
-3.22178327536779));
#62864=CARTESIAN_POINT('Ctrl Pts',(-0.650264963381902,-0.272743574823193,
-3.20597639004969));
#62865=CARTESIAN_POINT('Ctrl Pts',(-0.441778804249146,-0.549604465343574,
-3.1901695047316));
#62866=CARTESIAN_POINT('Ctrl Pts',(-0.126570615394638,-0.693695509231553,
-3.17436261941351));
#62867=CARTESIAN_POINT('Ctrl Pts',(0.219213673644229,-0.67020813595241,
-3.15855573409542));
#62868=CARTESIAN_POINT('Ctrl Pts',(0.512041759331881,-0.484816271292242,
-3.14274884877732));
#62869=CARTESIAN_POINT('Ctrl Pts',(0.681174150856313,-0.182305667532811,
-3.12694196345923));
#62870=CARTESIAN_POINT('Ctrl Pts',(0.685752952950544,0.164245145222046,
-3.11113507814114));
#62871=CARTESIAN_POINT('Ctrl Pts',(0.52467204859744,0.471118691658448,-3.09532819282305));
#62872=CARTESIAN_POINT('Ctrl Pts',(0.236844307533238,0.664182470559487,
-3.07952130750496));
#62873=CARTESIAN_POINT('Ctrl Pts',(-0.108198729930143,0.696797398854864,
-3.06371442218686));
#62874=CARTESIAN_POINT('Ctrl Pts',(-0.427103826957276,0.561084575806403,
-3.04790753686878));
#62875=CARTESIAN_POINT('Ctrl Pts',(-0.64283197915049,0.289828616238747,
-3.03210065155068));
#62876=CARTESIAN_POINT('Ctrl Pts',(-0.703268992599295,-0.0514422419590443,
-3.01629376623259));
#62877=CARTESIAN_POINT('Ctrl Pts',(-0.593814889478732,-0.380286020309405,
-3.0004868809145));
#62878=CARTESIAN_POINT('Ctrl Pts',(-0.340910875057239,-0.617262792882503,
-2.98467999559641));
#62879=CARTESIAN_POINT('Ctrl Pts',(-0.0056518445272595,-0.705125263242527,
-2.96887311027831));
#62880=CARTESIAN_POINT('Ctrl Pts',(0.330972521582021,-0.622648191330417,
-2.95306622496023));
#62881=CARTESIAN_POINT('Ctrl Pts',(0.587642713915593,-0.389755847924465,
-2.93725933964213));
#62882=CARTESIAN_POINT('Ctrl Pts',(0.70235402869083,-0.0627088398167523,
-2.92145245432404));
#62883=CARTESIAN_POINT('Ctrl Pts',(0.647395257884359,0.27948695904862,-2.90564556900594));
#62884=CARTESIAN_POINT('Ctrl Pts',(0.436042981348057,0.554166129086307,
-2.88983868368786));
#62885=CARTESIAN_POINT('Ctrl Pts',(0.11935429761476,0.694973475645141,-2.87403179836976));
#62886=CARTESIAN_POINT('Ctrl Pts',(-0.226167215523084,0.667893682281796,
-2.85822491305168));
#62887=CARTESIAN_POINT('Ctrl Pts',(-0.5170527342108,0.479468508094678,-2.84241802773358));
#62888=CARTESIAN_POINT('Ctrl Pts',(-0.683032040247721,0.175216472411809,
-2.82661114241549));
#62889=CARTESIAN_POINT('Ctrl Pts',(-0.684008940105105,-0.171363210945912,
-2.8108042570974));
#62890=CARTESIAN_POINT('Ctrl Pts',(-0.519747440714448,-0.476546092293478,
-2.79499737177931));
#62891=CARTESIAN_POINT('Ctrl Pts',(-0.229928759127129,-0.666608090211678,
-2.77919048646121));
#62892=CARTESIAN_POINT('Ctrl Pts',(0.115434605974731,-0.695635272217317,
-2.76338360114313));
#62893=CARTESIAN_POINT('Ctrl Pts',(0.432912035103061,-0.556615441819869,
-2.74757671582503));
#62894=CARTESIAN_POINT('Ctrl Pts',(0.645809410519448,-0.28313209901727,
-2.73176983050694));
#62895=CARTESIAN_POINT('Ctrl Pts',(0.70269637882455,0.0587484416496746,
-2.71596294518884));
#62896=CARTESIAN_POINT('Ctrl Pts',(0.589830558845161,0.386436918606138,
-2.70015605987076));
#62897=CARTESIAN_POINT('Ctrl Pts',(0.334477336060517,0.620772496065396,
-2.68434917455266));
#62898=CARTESIAN_POINT('Ctrl Pts',(-0.00167673062376321,0.705145920206461,
-2.66854228923458));
#62899=CARTESIAN_POINT('Ctrl Pts',(-0.337425743707141,0.619174811901361,
-2.65273540391648));
#62900=CARTESIAN_POINT('Ctrl Pts',(-0.591661655884731,0.383627508353011,
-2.63692851859839));
#62901=CARTESIAN_POINT('Ctrl Pts',(-0.702967820828586,0.0554059842337657,
-2.6211216332803));
#62902=CARTESIAN_POINT('Ctrl Pts',(-0.64445562430665,-0.286200154627713,
-2.60531474796221));
#62903=CARTESIAN_POINT('Ctrl Pts',(-0.430260059478938,-0.558667934847332,
-2.58950786264411));
#62904=CARTESIAN_POINT('Ctrl Pts',(-0.11212508783917,-0.696176374840788,
-2.57370097732603));
#62905=CARTESIAN_POINT('Ctrl Pts',(0.23309632806146,-0.665507086403793,
-2.55789409200792));
#62906=CARTESIAN_POINT('Ctrl Pts',(0.5220078598931,-0.474068955342181,-2.54208720668984));
#62907=CARTESIAN_POINT('Ctrl Pts',(0.684816152269453,-0.16810835136977,
-2.52628032137174));
#62908=CARTESIAN_POINT('Ctrl Pts',(0.682191044370633,0.178462766956884,
-2.51047343605366));
#62909=CARTESIAN_POINT('Ctrl Pts',(0.514766692567439,0.481922019036879,
-2.49466655073556));
#62910=CARTESIAN_POINT('Ctrl Pts',(0.222988375079262,0.668961706519075,
-2.47885966541747));
#62911=CARTESIAN_POINT('Ctrl Pts',(-0.122658013407166,0.694398006878195,
-2.46305278009938));
#62912=CARTESIAN_POINT('Ctrl Pts',(-0.43867348246843,0.552086185290324,
-2.44724589478129));
#62913=CARTESIAN_POINT('Ctrl Pts',(-0.648717085102761,0.276404999421464,
-2.4314390094632));
#62914=CARTESIAN_POINT('Ctrl Pts',(-0.702047863646276,-0.0660482956562912,
-2.4156321241451));
#62915=CARTESIAN_POINT('Ctrl Pts',(-0.58578251795406,-0.392546076109294,
-2.39982523882701));
#62916=CARTESIAN_POINT('Ctrl Pts',(-0.328007668658949,-0.624215146812637,
-2.38401835350892));
#62917=CARTESIAN_POINT('Ctrl Pts',(0.00900512466355355,-0.70509041118086,
-2.36821146819083));
#62918=CARTESIAN_POINT('Ctrl Pts',(0.343842518956618,-0.61563455260972,
-2.35240458287274));
#62919=CARTESIAN_POINT('Ctrl Pts',(0.595616689811292,-0.377457731445045,
-2.33659769755465));
#62920=CARTESIAN_POINT('Ctrl Pts',(0.703505682243138,-0.0480971440006585,
-2.32079081223656));
#62921=CARTESIAN_POINT('Ctrl Pts',(0.641446380171849,0.292882436437956,
-2.30498392691846));
#62922=CARTESIAN_POINT('Ctrl Pts',(0.424430663281246,0.563109396366323,
-2.28917704160037));
#62923=CARTESIAN_POINT('Ctrl Pts',(0.104883766927401,0.697304076887924,
-2.27337015628228));
#62924=CARTESIAN_POINT('Ctrl Pts',(-0.240000262814678,0.663048606105381,
-2.25756327096419));
#62925=CARTESIAN_POINT('Ctrl Pts',(-0.526906601153319,0.468618196264782,
-2.2417563856461));
#62926=CARTESIAN_POINT('Ctrl Pts',(-0.686526294211532,0.160982072186887,
-2.22594950032801));
#62927=CARTESIAN_POINT('Ctrl Pts',(-0.680299462106238,-0.185543046399923,
-2.21014261500991));
#62928=CARTESIAN_POINT('Ctrl Pts',(-0.509730342149469,-0.487245891210574,
-2.19433572969182));
#62929=CARTESIAN_POINT('Ctrl Pts',(-0.216023905051799,-0.671243065256971,
-2.17852884437373));
#62930=CARTESIAN_POINT('Ctrl Pts',(0.129868171994647,-0.693085736480105,
-2.16272195905564));
#62931=CARTESIAN_POINT('Ctrl Pts',(0.444387546733483,-0.547497295443183,
-2.14691507373755));
#62932=CARTESIAN_POINT('Ctrl Pts',(0.65155468882939,-0.269648044075677,
-2.13110818841945));
#62933=CARTESIAN_POINT('Ctrl Pts',(0.701323517113522,0.0733410154887558,
-2.11530130310137));
#62934=CARTESIAN_POINT('Ctrl Pts',(0.581671204052573,0.398612832941228,
-2.09949441778327));
#62935=CARTESIAN_POINT('Ctrl Pts',(0.321502571670479,0.627590373268003,
-2.08368753246518));
#62936=CARTESIAN_POINT('Ctrl Pts',(-0.0163325460192437,0.704958742161505,
-2.06788064714709));
#62937=CARTESIAN_POINT('Ctrl Pts',(-0.350222154225635,0.612027795854858,
-2.052073761829));
#62938=CARTESIAN_POINT('Ctrl Pts',(-0.599507388494239,0.371247183625977,
-2.03626687651091));
#62939=CARTESIAN_POINT('Ctrl Pts',(-0.70396755483765,0.040783108578214,
-2.02045999119281));
#62940=CARTESIAN_POINT('Ctrl Pts',(-0.638367850521979,-0.299533082695969,
-2.00465310587472));
#62941=CARTESIAN_POINT('Ctrl Pts',(-0.418555422414341,-0.567490033900997,
-1.98884622055663));
#62942=CARTESIAN_POINT('Ctrl Pts',(-0.097631117047166,-0.698356459978373,
-1.97303933523854));
#62943=CARTESIAN_POINT('Ctrl Pts',(0.246878274057621,-0.660518506938096,
-1.95723244992044));
#62944=CARTESIAN_POINT('Ctrl Pts',(0.531748428856327,-0.463116819623548,
-1.94142556460235));
#62945=CARTESIAN_POINT('Ctrl Pts',(0.68816228135381,-0.153838404604709,
-1.92561867928426));
#62946=CARTESIAN_POINT('Ctrl Pts',(0.678334397630255,0.192603284502106,
-1.90981179396617));
#62947=CARTESIAN_POINT('Ctrl Pts',(0.504638933459461,0.49251713375912,-1.89400490864808));
#62948=CARTESIAN_POINT('Ctrl Pts',(0.209036101308555,0.67345192000552,-1.87819802332998));
#62949=CARTESIAN_POINT('Ctrl Pts',(-0.137064302935446,0.691698602767291,
-1.8623911380119));
#62950=CARTESIAN_POINT('Ctrl Pts',(-0.450053610696377,0.542849267945122,
-1.8465842526938));
#62951=CARTESIAN_POINT('Ctrl Pts',(-0.654321915196967,0.262861962829116,
-1.83077736737571));
#62952=CARTESIAN_POINT('Ctrl Pts',(-0.700523417466219,-0.0806258134275274,
-1.81497048205762));
#62953=CARTESIAN_POINT('Ctrl Pts',(-0.577497061222251,-0.404636533804186,
-1.79916359673953));
#62954=CARTESIAN_POINT('Ctrl Pts',(-0.314962747739959,-0.630897810858063,
-1.78335671142144));
#62955=CARTESIAN_POINT('Ctrl Pts',(0.0236582032229997,-0.704750927370557,
-1.76754982610334));
#62956=CARTESIAN_POINT('Ctrl Pts',(0.356563960421018,-0.608354931218841,
-1.75174294078526));
#62957=CARTESIAN_POINT('Ctrl Pts',(0.603333331681656,-0.364996535725085,
-1.73593605546716));
#62958=CARTESIAN_POINT('Ctrl Pts',(0.704353388723183,-0.033464667988367,
-1.72012917014907));
#62959=CARTESIAN_POINT('Ctrl Pts',(0.635220367882906,0.306151375035467,
-1.70432228483098));
#62960=CARTESIAN_POINT('Ctrl Pts',(0.412634971489475,0.571809374278948,
-1.68851539951289));
#62961=CARTESIAN_POINT('Ctrl Pts',(0.0903679215898715,0.69933341043949,
-1.67270851419479));
#62962=CARTESIAN_POINT('Ctrl Pts',(-0.253729618865292,0.657917062189359,
-1.65690162887671));
#62963=CARTESIAN_POINT('Ctrl Pts',(-0.53653282001449,0.457565419646962,
-1.64109474355861));
#62964=CARTESIAN_POINT('Ctrl Pts',(-0.689723936985944,0.14667812024297,
-1.62528785824052));
#62965=CARTESIAN_POINT('Ctrl Pts',(-0.676296063198152,-0.19964271865531,
-1.60948097292243));
#62966=CARTESIAN_POINT('Ctrl Pts',(-0.499493016443407,-0.497735177311859,
-1.59367408760434));
#62967=CARTESIAN_POINT('Ctrl Pts',(-0.202025718633698,-0.67558803217637,
-1.57786720228624));
#62968=CARTESIAN_POINT('Ctrl Pts',(0.144245628943018,-0.690236755570315,
-1.56206031696815));
#62969=CARTESIAN_POINT('Ctrl Pts',(0.455671062340006,-0.538142604850548,
-1.54625343165006));
#62970=CARTESIAN_POINT('Ctrl Pts',(0.657018465304896,-0.256047488677006,
-1.53044654633197));
#62971=CARTESIAN_POINT('Ctrl Pts',(0.69964765112674,0.0879019026087411,
-1.51463966101388));
#62972=CARTESIAN_POINT('Ctrl Pts',(0.573260540331073,0.410616528051086,
-1.49883277569578));
#62973=CARTESIAN_POINT('Ctrl Pts',(0.308388903263251,0.63413710233158,-1.48302589037769));
#62974=CARTESIAN_POINT('Ctrl Pts',(-0.0309813049975863,0.704466989255031,
-1.4672190050596));
#62975=CARTESIAN_POINT('Ctrl Pts',(-0.362867252535701,0.604616355424324,
-1.45141211974151));
#62976=CARTESIAN_POINT('Ctrl Pts',(-0.607094106116187,0.358706462903012,
-1.43560523442342));
#62977=CARTESIAN_POINT('Ctrl Pts',(-0.704663142224076,0.0261426127288773,
-1.41979834910533));
#62978=CARTESIAN_POINT('Ctrl Pts',(-0.632004272228418,-0.312736598584864,
-1.40399146378724));
#62979=CARTESIAN_POINT('Ctrl Pts',(-0.406669950001241,-0.576066950948749,
-1.38818457846914));
#62980=CARTESIAN_POINT('Ctrl Pts',(-0.0830949650860008,-0.700234822746455,
-1.37237769315105));
#62981=CARTESIAN_POINT('Ctrl Pts',(0.260553557193054,-0.655244552852938,
-1.35657080783296));
#62982=CARTESIAN_POINT('Ctrl Pts',(0.541259257844153,-0.451964595966764,
-1.34076392251487));
#62983=CARTESIAN_POINT('Ctrl Pts',(0.69121109242647,-0.13950199251626,-1.32495703719678));
#62984=CARTESIAN_POINT('Ctrl Pts',(0.67418467897962,0.206660588498508,-1.30915015187868));
#62985=CARTESIAN_POINT('Ctrl Pts',(0.494293146935006,0.50289945824438,-1.29334326656059));
#62986=CARTESIAN_POINT('Ctrl Pts',(0.194993514250268,0.677651171038411,
-1.2775363812425));
#62987=CARTESIAN_POINT('Ctrl Pts',(-0.151411374329973,0.688700352789885,
-1.26172949592441));
#62988=CARTESIAN_POINT('Ctrl Pts',(-0.461239294898093,0.533377814547353,
-1.24592261060632));
#62989=CARTESIAN_POINT('Ctrl Pts',(-0.659644047886644,0.24920535768142,
-1.23011572528823));
#62990=CARTESIAN_POINT('Ctrl Pts',(-0.698696312690555,-0.0951684971092057,
-1.21430883997013));
#62991=CARTESIAN_POINT('Ctrl Pts',(-0.568962098984759,-0.416552169755792,
-1.19850195465204));
#62992=CARTESIAN_POINT('Ctrl Pts',(-0.301781748310929,-0.637307897798075,
-1.18269506933395));
#62993=CARTESIAN_POINT('Ctrl Pts',(0.0383010603417563,-0.704106958484362,
-1.16688818401586));
#62994=CARTESIAN_POINT('Ctrl Pts',(0.369131349722688,-0.600812472291737,
-1.15108129869777));
#62995=CARTESIAN_POINT('Ctrl Pts',(0.610789305579622,-0.352377644578884,
-1.13527441337968));
#62996=CARTESIAN_POINT('Ctrl Pts',(0.704896781882463,-0.0188177336879362,
-1.11946752806159));
#62997=CARTESIAN_POINT('Ctrl Pts',(0.628719910943502,0.319288042044476,
-1.10366064274349));
#62998=CARTESIAN_POINT('Ctrl Pts',(0.4006610022585,0.580262304030356,-1.0878537574254));
#62999=CARTESIAN_POINT('Ctrl Pts',(0.0758130331203709,0.701060599533658,
-1.07204687210731));
#63000=CARTESIAN_POINT('Ctrl Pts',(-0.267349351956566,0.65250126759862,
-1.05623998678922));
#63001=CARTESIAN_POINT('Ctrl Pts',(-0.545927231821457,0.446314953553164,
-1.04043310147113));
#63002=CARTESIAN_POINT('Ctrl Pts',(-0.692623587041027,0.132310796550484,
-1.02462621615303));
#63003=CARTESIAN_POINT('Ctrl Pts',(-0.672000473034784,-0.213656135999947,
-1.00881933083494));
#63004=CARTESIAN_POINT('Ctrl Pts',(-0.489039886595606,-0.508009418739415,
-0.99301244551685));
#63005=CARTESIAN_POINT('Ctrl Pts',(-0.187940247738363,-0.67964111374272,
-0.977205560198759));
#63006=CARTESIAN_POINT('Ctrl Pts',(0.158560765091847,-0.687089560379787,
-0.961398674880666));
#63007=CARTESIAN_POINT('Ctrl Pts',(0.466757706920742,-0.528555411702021,
-0.945591789562577));
#63008=CARTESIAN_POINT('Ctrl Pts',(0.662198379341202,-0.242336308891769,
-0.929784904244484));
#63009=CARTESIAN_POINT('Ctrl Pts',(0.697669504916014,0.102424812031291,
-0.913978018926392));
#63010=CARTESIAN_POINT('Ctrl Pts',(0.564602201477338,0.422442817782887,
-0.898171133608301));
#63011=CARTESIAN_POINT('Ctrl Pts',(0.295141996551584,0.640409854765639,
-0.882364248290208));
#63012=CARTESIAN_POINT('Ctrl Pts',(-0.0456166786157439,0.703670873947096,
-0.866557362972117));
#63013=CARTESIAN_POINT('Ctrl Pts',(-0.375355575368597,0.596943692695645,
-0.850750477654026));
#63014=CARTESIAN_POINT('Ctrl Pts',(-0.614418530936816,0.346010764356899,
-0.834943592335933));
#63015=CARTESIAN_POINT('Ctrl Pts',(-0.705054282461865,0.0114908220587519,
-0.819136707017843));
#63016=CARTESIAN_POINT('Ctrl Pts',(-0.62536763878683,-0.325804997763367,
-0.80332982169975));
#63017=CARTESIAN_POINT('Ctrl Pts',(-0.394608777314782,-0.584394980364765,
-0.787522936381659));
#63018=CARTESIAN_POINT('Ctrl Pts',(-0.0685229122472805,-0.701810651605228,
-0.771716051063567));
#63019=CARTESIAN_POINT('Ctrl Pts',(0.274116269111402,-0.649687502741008,
-0.755909165745476));
#63020=CARTESIAN_POINT('Ctrl Pts',(0.550536237737494,-0.440617102649509,
-0.740102280427383));
#63021=CARTESIAN_POINT('Ctrl Pts',(0.6939612682597,-0.125105309099136,-0.724295395109291));
#63022=CARTESIAN_POINT('Ctrl Pts',(0.669743681289579,0.220628605539007,
-0.7084885097912));
#63023=CARTESIAN_POINT('Ctrl Pts',(0.483733802853534,0.513064506847101,
-0.692681624473108));
#63024=CARTESIAN_POINT('Ctrl Pts',(0.180866680953096,0.681557645346608,
-0.676874739155017));
#63025=CARTESIAN_POINT('Ctrl Pts',(-0.165693028990715,0.685404552328976,
-0.661067853836925));
#63026=CARTESIAN_POINT('Ctrl Pts',(-0.47222570233939,0.523675917204019,
-0.645260968518833));
#63027=CARTESIAN_POINT('Ctrl Pts',(-0.664681183763715,0.235441084264976,
-0.629454083200741));
#63028=CARTESIAN_POINT('Ctrl Pts',(-0.696567338713257,-0.109670063587713,
-0.613647197882651));
#63029=CARTESIAN_POINT('Ctrl Pts',(-0.560181318740991,-0.428287835856923,
-0.597840312564558));
#63030=CARTESIAN_POINT('Ctrl Pts',(-0.288470365174735,-0.643442638177916,
-0.582033427246467));
#63031=CARTESIAN_POINT('Ctrl Pts',(0.0529273696266406,-0.703158782746691,
-0.566226541928374));
#63032=CARTESIAN_POINT('Ctrl Pts',(0.381539257166764,-0.593010434520368,
-0.550419656610283));
#63033=CARTESIAN_POINT('Ctrl Pts',(0.617981390178772,-0.339606509952495,
-0.534612771292191));
#63034=CARTESIAN_POINT('Ctrl Pts',(0.70513562694994,-0.00416266925407728,
-0.518805885974099));
#63035=CARTESIAN_POINT('Ctrl Pts',(0.621947817852421,0.33228676181577,-0.502999000656008));
#63036=CARTESIAN_POINT('Ctrl Pts',(0.388513928898186,0.588464533562985,
-0.487192115337916));
#63037=CARTESIAN_POINT('Ctrl Pts',(0.0612253899055303,0.702484897944656,
-0.471385230019824));
#63038=CARTESIAN_POINT('Ctrl Pts',(-0.280853577732319,0.646803562207529,
-0.455578344701733));
#63039=CARTESIAN_POINT('Ctrl Pts',(-0.555085777752791,0.434871658706356,
-0.439771459383642));
#63040=CARTESIAN_POINT('Ctrl Pts',(-0.695223991593445,0.1178863084594,-0.423964574065549));
#63041=CARTESIAN_POINT('Ctrl Pts',(-0.667414547510384,-0.227577243987833,
-0.408157688747458));
#63042=CARTESIAN_POINT('Ctrl Pts',(-0.478375468842551,-0.518064176544559,
-0.392350803429365));
#63043=CARTESIAN_POINT('Ctrl Pts',(-0.173773577942818,-0.683400558836909,
-0.376543918111274));
#63044=CARTESIAN_POINT('Ctrl Pts',(0.172807395639615,-0.68364551064267,
-0.360737032793182));
#63045=CARTESIAN_POINT('Ctrl Pts',(0.477642690529216,-0.518739858109735,
-0.34493014747509));
#63046=CARTESIAN_POINT('Ctrl Pts',(0.667092192979181,-0.228520428584966,
-0.329123262156999));
#63047=CARTESIAN_POINT('Ctrl Pts',(0.695389933124598,0.11690346918548,-0.313316376838907));
#63048=CARTESIAN_POINT('Ctrl Pts',(0.555699928310104,0.434086592632565,
-0.297509491520815));
#63049=CARTESIAN_POINT('Ctrl Pts',(0.281767574784161,0.646405920447539,
-0.281702606202724));
#63050=CARTESIAN_POINT('Ctrl Pts',(-0.0602323436566084,0.702570740201827,
-0.265895720884633));
#63051=CARTESIAN_POINT('Ctrl Pts',(-0.387681727301688,0.589013122604281,
-0.25008883556654));
#63052=CARTESIAN_POINT('Ctrl Pts',(-0.621477498246083,0.333165573138756,
-0.234281950248449));
#63053=CARTESIAN_POINT('Ctrl Pts',(-0.705140806988782,-0.00316593321977806,
-0.218475064930357));
#63054=CARTESIAN_POINT('Ctrl Pts',(-0.618460816691914,-0.338732633997832,
-0.202668179612265));
#63055=CARTESIAN_POINT('Ctrl Pts',(-0.382377116982208,-0.592470524209418,
-0.186861294294173));
#63056=CARTESIAN_POINT('Ctrl Pts',(-0.0539212511207285,-0.703083265419793,
-0.171054408976082));
#63057=CARTESIAN_POINT('Ctrl Pts',(0.287560543804209,-0.643849758100151,
-0.155247523657989));
#63058=CARTESIAN_POINT('Ctrl Pts',(0.559575372758286,-0.429079241151316,
-0.139440638339898));
#63059=CARTESIAN_POINT('Ctrl Pts',(0.696411596561459,-0.110654576665681,
-0.123633753021806));
#63060=CARTESIAN_POINT('Ctrl Pts',(0.665013370424364,0.234501305250519,
-0.107826867703715));
#63061=CARTESIAN_POINT('Ctrl Pts',(0.472965371062188,0.523007879069813,
-0.0920199823856229));
#63062=CARTESIAN_POINT('Ctrl Pts',(0.166661885477124,0.685169672229466,
-0.076213097067531));
#63063=CARTESIAN_POINT('Ctrl Pts',(-0.179903450085766,0.681812591898513,
-0.0604062117494397));
#63064=CARTESIAN_POINT('Ctrl Pts',(-0.483007394483508,0.513747833004724,
-0.0445993264313473));
#63065=CARTESIAN_POINT('Ctrl Pts',(-0.669432500791895,0.221574961343309,
-0.0287924411132557));
#63066=CARTESIAN_POINT('Ctrl Pts',(-0.694134764542732,-0.12412399693593,
-0.0129855557951638));
#63067=CARTESIAN_POINT('Ctrl Pts',(-0.551163704885714,-0.439838951879844,
0.00282132952292781));
#63068=CARTESIAN_POINT('Ctrl Pts',(-0.275024164045417,-0.649298425663846,
0.018628214841019));
#63069=CARTESIAN_POINT('Ctrl Pts',(0.0675105960172764,-0.701908643303733,
0.0344351001591104));
#63070=CARTESIAN_POINT('Ctrl Pts',(0.393824914024269,-0.584949001043688,
0.0502419854772018));
#63071=CARTESIAN_POINT('Ctrl Pts',(0.547800831229363,-0.41277621737474,
0.0607799090225966));
#63072=CARTESIAN_POINT('Ctrl Pts',(0.599695759644983,-0.313508988489687,
0.066048870795294));
#63073=CARTESIAN_POINT('',(0.701077753000062,-0.366509473613416,0.));
#63074=CARTESIAN_POINT('Ctrl Pts',(-0.564218010237599,-0.373640954068625,
7.21644966006352E-16));
#63075=CARTESIAN_POINT('Ctrl Pts',(-0.554510060806831,-0.391301626549833,
7.52778991897534E-16));
#63076=CARTESIAN_POINT('Ctrl Pts',(-0.544024301133767,-0.408498917022784,
8.63432540169627E-16));
#63077=CARTESIAN_POINT('Ctrl Pts',(-0.532788826860589,-0.425178050450441,
1.02695629777827E-15));
#63078=CARTESIAN_POINT('Ctrl Pts',(-0.516678281161148,-0.449094258594393,
1.27490859920589E-15));
#63079=CARTESIAN_POINT('Ctrl Pts',(-0.499027462499214,-0.471945953324106,
4.1283124830284E-16));
#63080=CARTESIAN_POINT('Ctrl Pts',(-0.479984048942617,-0.493634775998338,
5.20417042793042E-16));
#63081=CARTESIAN_POINT('Ctrl Pts',(-0.473276092698443,-0.501274565632376,
5.58313652021744E-16));
#63082=CARTESIAN_POINT('Ctrl Pts',(-0.466395095773147,-0.508769945555998,
3.16844864503691E-16));
#63083=CARTESIAN_POINT('Ctrl Pts',(-0.459346743724129,-0.516116152859011,
1.66533453693773E-16));
#63084=CARTESIAN_POINT('Ctrl Pts',(-0.452846524820441,-0.522891063540167,
2.79113946377707E-17));
#63085=CARTESIAN_POINT('Ctrl Pts',(-0.446209412880882,-0.52953328200918,
7.68010458298948E-16));
#63086=CARTESIAN_POINT('Ctrl Pts',(-0.439445630221723,-0.536034792396529,
7.7715611723761E-16));
#63087=CARTESIAN_POINT('Ctrl Pts',(-0.415262930686365,-0.559279784163135,
8.09854790940117E-16));
#63088=CARTESIAN_POINT('Ctrl Pts',(-0.389445190687811,-0.580748321127649,
2.21695987855779E-15));
#63089=CARTESIAN_POINT('Ctrl Pts',(-0.3622125634703,-0.600285727779798,
2.12330153459561E-15));
#63090=CARTESIAN_POINT('Ctrl Pts',(-0.35033589474735,-0.608806363877806,
2.08245534243448E-15));
#63091=CARTESIAN_POINT('Ctrl Pts',(-0.338189563353738,-0.616959334419476,
1.92489464226297E-15));
#63092=CARTESIAN_POINT('Ctrl Pts',(-0.325789558314903,-0.62472981087111,
1.79023462720806E-15));
#63093=CARTESIAN_POINT('Ctrl Pts',(-0.31703217919042,-0.630217631888256,
1.69513234289035E-15));
#63094=CARTESIAN_POINT('Ctrl Pts',(-0.308144761904281,-0.635516349767648,
1.35230555608436E-15));
#63095=CARTESIAN_POINT('Ctrl Pts',(-0.299156917123911,-0.640607333528386,
1.32532873564628E-15));
#63096=CARTESIAN_POINT('Ctrl Pts',(-0.29169022892703,-0.64483668876156,
1.30291763357715E-15));
#63097=CARTESIAN_POINT('Ctrl Pts',(-0.284151278188811,-0.648924659296807,
1.20875487286781E-15));
#63098=CARTESIAN_POINT('Ctrl Pts',(-0.276543809476503,-0.652868964991246,
1.22124532708767E-15));
#63099=CARTESIAN_POINT('Ctrl Pts',(-0.246334864268026,-0.668531640595291,
1.2639055129074E-15));
#63100=CARTESIAN_POINT('Ctrl Pts',(-0.21504836953113,-0.68193216733753,
1.1331870985744E-15));
#63101=CARTESIAN_POINT('Ctrl Pts',(-0.182960974453157,-0.693063919212634,
7.84095011141517E-16));
#63102=CARTESIAN_POINT('Ctrl Pts',(-0.160488941038507,-0.700859911984657,
5.39612433652176E-16));
#63103=CARTESIAN_POINT('Ctrl Pts',(-0.137623149403411,-0.707542338895848,
9.78508102310067E-16));
#63104=CARTESIAN_POINT('Ctrl Pts',(-0.114450318277965,-0.713096218066307,
1.1518563880486E-15));
#63105=CARTESIAN_POINT('Ctrl Pts',(-0.0964870036737186,-0.717401521905654,
1.28623400362656E-15));
#63106=CARTESIAN_POINT('Ctrl Pts',(-0.0783390261237154,-0.721028460504329,
1.29037321294563E-15));
#63107=CARTESIAN_POINT('Ctrl Pts',(-0.0600452300518944,-0.723965290929148,
9.5062846483529E-16));
#63108=CARTESIAN_POINT('Ctrl Pts',(-0.0528943522626845,-0.725113271117244,
8.17825346022505E-16));
#63109=CARTESIAN_POINT('Ctrl Pts',(-0.0457214326365342,-0.726155578268713,
1.34239484214797E-15));
#63110=CARTESIAN_POINT('Ctrl Pts',(-0.0385427376555631,-0.727089954163797,
1.29757316003065E-15));
#63111=CARTESIAN_POINT('Ctrl Pts',(-0.00231851625636514,-0.73180488346269,
1.07139966459643E-15));
#63112=CARTESIAN_POINT('Ctrl Pts',(0.0341393528175536,-0.73379106608169,
8.24934566925163E-16));
#63113=CARTESIAN_POINT('Ctrl Pts',(0.0705191993603075,-0.733021256094104,
9.36750677027476E-16));
#63114=CARTESIAN_POINT('Ctrl Pts',(0.10157783972999,-0.732364044647945,
1.04023535002902E-15));
#63115=CARTESIAN_POINT('Ctrl Pts',(0.132580760956565,-0.729697475366545,
2.00043039592424E-15));
#63116=CARTESIAN_POINT('Ctrl Pts',(0.163353306654297,-0.725092274746165,
1.85615411929518E-15));
#63117=CARTESIAN_POINT('Ctrl Pts',(0.181654685473116,-0.72235342038169,
1.77034858279218E-15));
#63118=CARTESIAN_POINT('Ctrl Pts',(0.199874675175882,-0.718928222955073,
-3.04629698038031E-17));
#63119=CARTESIAN_POINT('Ctrl Pts',(0.217976303857617,-0.714826100584156,
-1.83880688453542E-16));
#63120=CARTESIAN_POINT('Ctrl Pts',(0.227452922574193,-0.712678545227596,
-2.64198390775961E-16));
#63121=CARTESIAN_POINT('Ctrl Pts',(0.236900911941713,-0.710344158497489,
2.17105674296715E-16));
#63122=CARTESIAN_POINT('Ctrl Pts',(0.246287934957814,-0.707831707209637,
2.4980018054066E-16));
#63123=CARTESIAN_POINT('Ctrl Pts',(0.280987647322768,-0.698544275308181,
3.70657449201143E-16));
#63124=CARTESIAN_POINT('Ctrl Pts',(0.314923694096686,-0.686814217748739,
-5.34659704257165E-17));
#63125=CARTESIAN_POINT('Ctrl Pts',(0.347837497670182,-0.672763584846155,
6.93889390390723E-17));
#63126=CARTESIAN_POINT('Ctrl Pts',(0.37480383187388,-0.661251877857368,
1.70044171418847E-16));
#63127=CARTESIAN_POINT('Ctrl Pts',(0.40108450851066,-0.64818139147437,-3.8699560848025E-16));
#63128=CARTESIAN_POINT('Ctrl Pts',(0.426534291574676,-0.633593383890318,
-6.17561557447743E-16));
#63129=CARTESIAN_POINT('Ctrl Pts',(0.440986713378868,-0.625309146717957,
-7.48495339467814E-16));
#63130=CARTESIAN_POINT('Ctrl Pts',(0.455171082616751,-0.616535108140792,
-8.13090200322811E-16));
#63131=CARTESIAN_POINT('Ctrl Pts',(0.469069700451425,-0.607290200982864,
-8.70831184940357E-16));
#63132=CARTESIAN_POINT('Ctrl Pts',(0.476786897224892,-0.602156973453421,
-9.02891821867551E-16));
#63133=CARTESIAN_POINT('Ctrl Pts',(0.48441597550879,-0.596878537328559,
7.76292981169644E-16));
#63134=CARTESIAN_POINT('Ctrl Pts',(0.491953726322627,-0.591457859074385,
8.95117313604032E-16));
#63135=CARTESIAN_POINT('Ctrl Pts',(0.497924153838461,-0.587164301565985,
9.89234521964725E-16));
#63136=CARTESIAN_POINT('Ctrl Pts',(0.50383604081433,-0.582782248651759,
-6.48491678049708E-16));
#63137=CARTESIAN_POINT('Ctrl Pts',(0.509678190852515,-0.578320977422655,
-6.05418493115906E-16));
#63138=CARTESIAN_POINT('Ctrl Pts',(0.538552106605361,-0.556271839900029,
-3.92535991835301E-16));
#63139=CARTESIAN_POINT('Ctrl Pts',(0.565790235250783,-0.532244703810416,
-1.52188196534005E-15));
#63140=CARTESIAN_POINT('Ctrl Pts',(0.591234871672643,-0.506472330067542,
-1.00874170128051E-15));
#63141=CARTESIAN_POINT('Ctrl Pts',(0.616885738234245,-0.480491069856402,
-4.91442407922625E-16));
#63142=CARTESIAN_POINT('Ctrl Pts',(0.64071489582184,-0.452735434439652,
-5.70549400489371E-16));
#63143=CARTESIAN_POINT('Ctrl Pts',(0.662534433530974,-0.423398860723195,
-6.21464685268691E-16));
#63144=CARTESIAN_POINT('Ctrl Pts',(0.676187576319825,-0.405042081802127,
-6.53323914483071E-16));
#63145=CARTESIAN_POINT('Ctrl Pts',(0.689053304273939,-0.386065449904219,
-6.46391670435626E-17));
#63146=CARTESIAN_POINT('Ctrl Pts',(0.701077753000062,-0.366509473613416,
-3.46944695195361E-18));
#63147=CARTESIAN_POINT('Ctrl Pts',(0.701077753000062,-0.366509473613416,
-3.14469315649998E-20));
#63148=CARTESIAN_POINT('Ctrl Pts',(0.640409690535754,-0.482558394510364,
-0.00526896177269737));
#63149=CARTESIAN_POINT('Ctrl Pts',(0.550406477811535,-0.583198182570441,
-0.010537923545395));
#63150=CARTESIAN_POINT('Ctrl Pts',(0.44182493524546,-0.656306799567799,
-0.0158068853180924));
#63151=CARTESIAN_POINT('Ctrl Pts',(0.333243392679392,-0.729415416565154,
-0.0210758470907895));
#63152=CARTESIAN_POINT('Ctrl Pts',(0.206083520271465,-0.774992862499796,
-0.0263448088634866));
#63153=CARTESIAN_POINT('Ctrl Pts',(0.0757632144587173,-0.787530872897559,
-0.0316137706361836));
#63154=CARTESIAN_POINT('Ctrl Pts',(-0.0545570913540345,-0.800068883295322,
-0.0368827324088808));
#63155=CARTESIAN_POINT('Ctrl Pts',(-0.188037830571603,-0.779567458156207,
-0.0421516941815777));
#63156=CARTESIAN_POINT('Ctrl Pts',(-0.308581951414016,-0.728505113226044,
-0.0474206559542749));
#63157=CARTESIAN_POINT('Ctrl Pts',(-0.429126072256424,-0.677442768295882,
-0.0526896177269719));
#63158=CARTESIAN_POINT('Ctrl Pts',(-0.536733574723672,-0.595819503574671,
-0.0579585794996691));
#63159=CARTESIAN_POINT('Ctrl Pts',(-0.618394181603484,-0.493493142664703,
-0.0632275412723662));
#63160=CARTESIAN_POINT('Ctrl Pts',(-0.700054788483297,-0.391166781754735,
-0.0684965030450632));
#63161=CARTESIAN_POINT('Ctrl Pts',(-0.755768499775678,-0.268137324656005,
-0.0737654648177603));
#63162=CARTESIAN_POINT('Ctrl Pts',(-0.778812301667548,-0.139265705831607,
-0.0790344265904574));
#63163=CARTESIAN_POINT('Ctrl Pts',(-0.787023434197926,-0.0933452476304458,
-0.0809119007857365));
#63164=CARTESIAN_POINT('Ctrl Pts',(-0.791086499485871,-0.0466830157260825,
-0.0827893749810157));
#63165=CARTESIAN_POINT('Ctrl Pts',(-0.791053952037979,-1.51658468628413E-5,
-0.0846668491762948));
#63166=CARTESIAN_POINT('Origin',(0.,0.,0.914655896708346));
#63167=CARTESIAN_POINT('',(1.2,-0.692820323027552,0.858179306876173));
#63168=CARTESIAN_POINT('',(-2.54538057293978E-16,-1.3856406460551,0.858179306876173));
#63169=CARTESIAN_POINT('Ctrl Pts',(1.2,-0.692820323027552,0.858179306876173));
#63170=CARTESIAN_POINT('Ctrl Pts',(0.599999999999999,-1.03923048454133,
1.05817930687617));
#63171=CARTESIAN_POINT('Ctrl Pts',(-2.54538057293978E-16,-1.3856406460551,
0.858179306876173));
#63172=CARTESIAN_POINT('',(1.2,0.692820323027551,0.858179306876173));
#63173=CARTESIAN_POINT('Ctrl Pts',(1.2,0.692820323027551,0.858179306876173));
#63174=CARTESIAN_POINT('Ctrl Pts',(1.2,-6.66133814775094E-16,1.05817930687617));
#63175=CARTESIAN_POINT('Ctrl Pts',(1.2,-0.692820323027552,0.858179306876173));
#63176=CARTESIAN_POINT('',(8.48460190979925E-17,1.3856406460551,0.858179306876173));
#63177=CARTESIAN_POINT('Ctrl Pts',(8.48460190979925E-17,1.3856406460551,
0.858179306876173));
#63178=CARTESIAN_POINT('Ctrl Pts',(0.6,1.03923048454133,1.05817930687617));
#63179=CARTESIAN_POINT('Ctrl Pts',(1.2,0.692820323027551,0.858179306876173));
#63180=CARTESIAN_POINT('',(-1.2,0.692820323027551,0.858179306876173));
#63181=CARTESIAN_POINT('Ctrl Pts',(-1.2,0.692820323027551,0.858179306876173));
#63182=CARTESIAN_POINT('Ctrl Pts',(-0.600000000000001,1.03923048454133,
1.05817930687617));
#63183=CARTESIAN_POINT('Ctrl Pts',(8.48460190979925E-17,1.3856406460551,
0.858179306876173));
#63184=CARTESIAN_POINT('',(-1.2,-1.11389921653139E-16,0.965358983848622));
#63185=CARTESIAN_POINT('Ctrl Pts',(-1.2,-7.58222274085957E-17,0.965358983848622));
#63186=CARTESIAN_POINT('Ctrl Pts',(-1.2,0.321539030917347,0.965358983848622));
#63187=CARTESIAN_POINT('Ctrl Pts',(-1.2,0.692820323027551,0.858179306876173));
#63188=CARTESIAN_POINT('',(-1.14,-1.39609735102798E-16,1.));
#63189=CARTESIAN_POINT('',(-1.28782032302755,-1.5771250364726E-16,0.914655896708346));
#63190=CARTESIAN_POINT('Origin',(0.,0.,1.));
#63191=CARTESIAN_POINT('',(-1.2,-0.692820323027551,0.858179306876173));
#63192=CARTESIAN_POINT('Ctrl Pts',(-1.2,-0.692820323027551,0.858179306876173));
#63193=CARTESIAN_POINT('Ctrl Pts',(-1.2,-0.321539030917347,0.965358983848622));
#63194=CARTESIAN_POINT('Ctrl Pts',(-1.2,-7.58222274085957E-17,0.965358983848622));
#63195=CARTESIAN_POINT('Ctrl Pts',(-2.54538057293978E-16,-1.3856406460551,
0.858179306876173));
#63196=CARTESIAN_POINT('Ctrl Pts',(-0.599999999999999,-1.03923048454133,
1.05817930687617));
#63197=CARTESIAN_POINT('Ctrl Pts',(-1.2,-0.692820323027551,0.858179306876173));
#63198=CARTESIAN_POINT('Origin',(8.48460190979926E-17,1.3856406460551,0.05));
#63199=CARTESIAN_POINT('',(8.48460190979926E-17,1.3856406460551,0.05));
#63200=CARTESIAN_POINT('',(8.48460190979926E-17,1.3856406460551,0.05));
#63201=CARTESIAN_POINT('',(-1.2,0.692820323027551,0.05));
#63202=CARTESIAN_POINT('',(8.48460190979926E-17,1.3856406460551,0.05));
#63203=CARTESIAN_POINT('',(-1.2,0.692820323027551,0.05));
#63204=CARTESIAN_POINT('Origin',(1.2,0.692820323027551,0.05));
#63205=CARTESIAN_POINT('',(1.2,0.692820323027551,0.05));
#63206=CARTESIAN_POINT('',(1.2,0.692820323027551,0.05));
#63207=CARTESIAN_POINT('',(1.2,0.692820323027551,0.05));
#63208=CARTESIAN_POINT('Origin',(1.2,-0.692820323027552,0.05));
#63209=CARTESIAN_POINT('',(1.2,-0.692820323027552,0.05));
#63210=CARTESIAN_POINT('',(1.2,-0.692820323027552,0.05));
#63211=CARTESIAN_POINT('',(1.2,-0.692820323027552,0.05));
#63212=CARTESIAN_POINT('Origin',(0.,0.,0.05));
#63213=CARTESIAN_POINT('',(-2.54538057293978E-16,-1.3856406460551,0.05));
#63214=CARTESIAN_POINT('',(-2.54538057293978E-16,-1.3856406460551,0.05));
#63215=CARTESIAN_POINT('',(-1.2,-0.692820323027551,0.05));
#63216=CARTESIAN_POINT('',(-1.2,-0.692820323027551,0.05));
#63217=CARTESIAN_POINT('',(-1.2,0.692820323027551,0.05));
#63218=CARTESIAN_POINT('',(-1.125,-1.37772764904077E-16,0.05));
#63219=CARTESIAN_POINT('Origin',(0.,0.,0.05));
#63220=CARTESIAN_POINT('Origin',(-2.54538057293978E-16,-1.3856406460551,
0.05));
#63221=CARTESIAN_POINT('',(-2.54538057293978E-16,-1.3856406460551,0.05));
#63222=CARTESIAN_POINT('Origin',(-1.2,-0.692820323027551,0.05));
#63223=CARTESIAN_POINT('',(-1.2,-0.692820323027551,0.05));
#63224=CARTESIAN_POINT('Origin',(-1.2,0.692820323027551,0.05));
#63225=CARTESIAN_POINT('Origin',(0.,0.,1.));
#63226=CARTESIAN_POINT('Origin',(0.74,0.,-4.));
#63227=CARTESIAN_POINT('',(-0.74,-9.06238631369041E-17,-4.));
#63228=CARTESIAN_POINT('Origin',(0.,0.,-4.));
#63229=CARTESIAN_POINT('Origin',(0.,0.,-3.97));
#63230=CARTESIAN_POINT('',(-0.77,-9.42978035343462E-17,-3.97));
#63231=CARTESIAN_POINT('Origin',(0.,0.,-1.97));
#63232=CARTESIAN_POINT('Origin',(0.,0.,0.));
#63233=CARTESIAN_POINT('Origin',(1.125,0.,0.));
#63234=CARTESIAN_POINT('',(-1.125,-1.37772764904077E-16,0.));
#63235=CARTESIAN_POINT('Origin',(0.,0.,0.));
#63236=CARTESIAN_POINT('Origin',(0.,0.,0.025));
#63237=CARTESIAN_POINT('',(-1.125,-1.37772764904077E-16,0.025));
#76632=UNCERTAINTY_MEASURE_WITH_UNIT(LENGTH_MEASURE(0.001),#76661,
'DISTANCE_ACCURACY_VALUE',
'Maximum model space distance between geometric entities at asserted c
onnectivities');
#76638=UNCERTAINTY_MEASURE_WITH_UNIT(LENGTH_MEASURE(0.001),#76661,
'DISTANCE_ACCURACY_VALUE',
'Maximum model space distance between geometric entities at asserted c
onnectivities');
#76654=(
GEOMETRIC_REPRESENTATION_CONTEXT(3)
GLOBAL_UNCERTAINTY_ASSIGNED_CONTEXT((#76632))
GLOBAL_UNIT_ASSIGNED_CONTEXT((#76661,#76663,#76664))
REPRESENTATION_CONTEXT('','3D')
);
#76660=(
GEOMETRIC_REPRESENTATION_CONTEXT(3)
GLOBAL_UNCERTAINTY_ASSIGNED_CONTEXT((#76638))
GLOBAL_UNIT_ASSIGNED_CONTEXT((#76661,#76663,#76664))
REPRESENTATION_CONTEXT('','3D')
);
#76661=(
LENGTH_UNIT()
NAMED_UNIT(*)
SI_UNIT(.CENTI.,.METRE.)
);
#76663=(
NAMED_UNIT(*)
PLANE_ANGLE_UNIT()
SI_UNIT($,.RADIAN.)
);
#76664=(
NAMED_UNIT(*)
SI_UNIT($,.STERADIAN.)
SOLID_ANGLE_UNIT()
);
#76680=SHAPE_DEFINITION_REPRESENTATION(#76701,#76750);
#76701=PRODUCT_DEFINITION_SHAPE('',$,#76772);
#76750=SHAPE_REPRESENTATION('',(#28363),#76654);
#76756=PRODUCT_DEFINITION_CONTEXT('part definition',#76821,'design');
#76772=PRODUCT_DEFINITION('2026-10-26-11-13-34-711',
'17_Bed_Clamping_Bolt_ISO_4017_M16x40',#76793,#76756);
#76793=PRODUCT_DEFINITION_FORMATION('',$,#76838);
#76821=APPLICATION_CONTEXT(
'Core Data for Automotive Mechanical Design Process');
#76822=PRODUCT_CONTEXT('part definition',#76821,'mechanical');
#76838=PRODUCT('2026-10-26-11-13-34-711',
'17_Bed_Clamping_Bolt_ISO_4017_M16x40',$,(#76822));
#76907=COLOUR_RGB('Black',0.12,0.14,0.17);
#76908=FILL_AREA_STYLE_COLOUR('',#76907);
#76909=FILL_AREA_STYLE('',(#76908));
#76910=SURFACE_STYLE_FILL_AREA(#76909);
#76911=SURFACE_SIDE_STYLE('',(#76910));
#76912=SURFACE_STYLE_USAGE(.BOTH.,#76911);
#76913=PRESENTATION_STYLE_ASSIGNMENT((#76912));
ENDSEC;
END-ISO-10303-21;
